ISO-10303-21;
HEADER;
FILE_DESCRIPTION (('STEP AP214'),
    '1' );
FILE_NAME ('Cylinder Spindle Drive Pinion.step',
    '2026-10-09T09:51:18',
    ( '' ),
    ( '' ),
    'SwSTEP 2.0',
    'SolidWorks 2026',
    '' );
FILE_SCHEMA (( 'AUTOMOTIVE_DESIGN' ));
ENDSEC;

DATA;
#6=ORIENTED_EDGE ( 'NONE', *, *, #28225, .T. ) ;
#12=CIRCLE ( 'NONE', #29107, 1.999999999999999556 ) ;
#23=ORIENTED_EDGE ( 'NONE', *, *, #45455, .T. ) ;
#39=DIRECTION ( 'NONE',  ( -3.071710424422018668E-17, 6.404604876783312462E-16, 1.000000000000000000 ) ) ;
#45=ORIENTED_EDGE ( 'NONE', *, *, #29252, .T. ) ;
#56=AXIS2_PLACEMENT_3D ( 'NONE', #16644, #27734, #1141 ) ;
#65=DIRECTION ( 'NONE',  ( -3.071710424422018668E-17, 6.404604876783312462E-16, 1.000000000000000000 ) ) ;
#70=VERTEX_POINT ( 'NONE', #18679 ) ;
#80=AXIS2_PLACEMENT_3D ( 'NONE', #16934, #39604, #9337 ) ;
#84=VECTOR ( 'NONE', #15701, 1000.000000000000000 ) ;
#99=LINE ( 'NONE', #37740, #35189 ) ;
#105=CYLINDRICAL_SURFACE ( 'NONE', #29747, 1.999999999999999556 ) ;
#116=CARTESIAN_POINT ( 'NONE',  ( -22.09321184435721719, -14.28490438881294189, 52.02966884056656482 ) ) ;
#127=AXIS2_PLACEMENT_3D ( 'NONE', #27305, #34688, #22905 ) ;
#140=AXIS2_PLACEMENT_3D ( 'NONE', #24664, #2235, #44833 ) ;
#141=DIRECTION ( 'NONE',  ( -3.071710424422018668E-17, 6.404604876783312462E-16, 1.000000000000000000 ) ) ;
#155=EDGE_CURVE ( 'NONE', #5150, #6817, #26237, .T. ) ;
#156=CARTESIAN_POINT ( 'NONE',  ( -18.50517187854146783, -19.38160480531894692, 49.52966884056656482 ) ) ;
#159=ADVANCED_FACE ( 'NONE', ( #34099 ), #4325, .T. ) ;
#176=ORIENTED_EDGE ( 'NONE', *, *, #45315, .T. ) ;
#177=CARTESIAN_POINT ( 'NONE',  ( -13.74654679279883851, -11.90422292133819582, 49.52966884056655772 ) ) ;
#186=EDGE_CURVE ( 'NONE', #10333, #39489, #16571, .T. ) ;
#208=DIRECTION ( 'NONE',  ( -0.9757441136919990932, -0.2189141945955432600, 0.000000000000000000 ) ) ;
#217=EDGE_CURVE ( 'NONE', #27248, #30011, #26822, .T. ) ;
#222=ORIENTED_EDGE ( 'NONE', *, *, #28530, .T. ) ;
#237=ORIENTED_EDGE ( 'NONE', *, *, #40366, .T. ) ;
#241=VERTEX_POINT ( 'NONE', #4094 ) ;
#242=ORIENTED_EDGE ( 'NONE', *, *, #46764, .F. ) ;
#281=DIRECTION ( 'NONE',  ( -3.071710424422018668E-17, 6.404604876783312462E-16, 1.000000000000000000 ) ) ;
#296=ORIENTED_EDGE ( 'NONE', *, *, #4735, .T. ) ;
#309=DIRECTION ( 'NONE',  ( -3.071710424422018668E-17, 6.404604876783312462E-16, 1.000000000000000000 ) ) ;
#318=CIRCLE ( 'NONE', #2655, 2.000000000000002220 ) ;
#348=FACE_OUTER_BOUND ( 'NONE', #44342, .T. ) ;
#358=ADVANCED_FACE ( 'NONE', ( #45878 ), #45160, .T. ) ;
#360=ADVANCED_FACE ( 'NONE', ( #45647 ), #22994, .T. ) ;
#369=DIRECTION ( 'NONE',  ( -3.071710424422018668E-17, 6.404604876783312462E-16, 1.000000000000000000 ) ) ;
#370=ORIENTED_EDGE ( 'NONE', *, *, #6560, .T. ) ;
#371=EDGE_LOOP ( 'NONE', ( #15592, #28628, #42332, #39991 ) ) ;
#373=DIRECTION ( 'NONE',  ( 0.9687793358424821033, -0.2479245821708677133, 0.000000000000000000 ) ) ;
#376=CIRCLE ( 'NONE', #29497, 4.686499999999999666 ) ;
#379=AXIS2_PLACEMENT_3D ( 'NONE', #38542, #5309, #35336 ) ;
#380=FACE_OUTER_BOUND ( 'NONE', #43337, .T. ) ;
#409=ADVANCED_FACE ( 'NONE', ( #15316 ), #30378, .T. ) ;
#413=DIRECTION ( 'NONE',  ( -0.9687793358424822143, 0.2479245821708672415, 0.000000000000000000 ) ) ;
#416=ORIENTED_EDGE ( 'NONE', *, *, #43313, .F. ) ;
#421=CIRCLE ( 'NONE', #10633, 5.249999999999998224 ) ;
#423=EDGE_LOOP ( 'NONE', ( #39334, #48242, #40910, #3394 ) ) ;
#452=EDGE_CURVE ( 'NONE', #42348, #36826, #9530, .T. ) ;
#467=VERTEX_POINT ( 'NONE', #16535 ) ;
#485=AXIS2_PLACEMENT_3D ( 'NONE', #1699, #42596, #17174 ) ;
#489=ADVANCED_FACE ( 'NONE', ( #27872 ), #24911, .T. ) ;
#491=ORIENTED_EDGE ( 'NONE', *, *, #37482, .F. ) ;
#494=ORIENTED_EDGE ( 'NONE', *, *, #28708, .F. ) ;
#499=DIRECTION ( 'NONE',  ( -3.071710424422018668E-17, 6.404604876783312462E-16, 1.000000000000000000 ) ) ;
#507=VECTOR ( 'NONE', #676, 1000.000000000000000 ) ;
#517=DIRECTION ( 'NONE',  ( -0.9687793358424819923, 0.2479245821708678243, 0.000000000000000000 ) ) ;
#518=ORIENTED_EDGE ( 'NONE', *, *, #23883, .T. ) ;
#536=CARTESIAN_POINT ( 'NONE',  ( -13.14551704304688684, -16.75068433397604295, 49.52966884056655772 ) ) ;
#546=VECTOR ( 'NONE', #17475, 1000.000000000000000 ) ;
#547=ORIENTED_EDGE ( 'NONE', *, *, #3362, .T. ) ;
#550=EDGE_CURVE ( 'NONE', #44867, #2342, #18143, .T. ) ;
#576=DIRECTION ( 'NONE',  ( -3.071710424422018668E-17, 6.404604876783312462E-16, 1.000000000000000000 ) ) ;
#578=AXIS2_PLACEMENT_3D ( 'NONE', #35667, #10320, #47006 ) ;
#583=ORIENTED_EDGE ( 'NONE', *, *, #25130, .F. ) ;
#595=DIRECTION ( 'NONE',  ( -3.071710424422018668E-17, 6.404604876783312462E-16, 1.000000000000000000 ) ) ;
#599=CARTESIAN_POINT ( 'NONE',  ( -17.42409385541299471, -14.80920654474435771, 49.52966884056655772 ) ) ;
#600=DIRECTION ( 'NONE',  ( -3.071710424422018668E-17, 6.404604876783312462E-16, 1.000000000000000000 ) ) ;
#611=CIRCLE ( 'NONE', #9265, 4.686499999999997890 ) ;
#621=AXIS2_PLACEMENT_3D ( 'NONE', #36417, #14242, #14973 ) ;
#630=CARTESIAN_POINT ( 'NONE',  ( -22.09908899289463591, -14.48102562737866528, 52.02966884056656482 ) ) ;
#632=ORIENTED_EDGE ( 'NONE', *, *, #1271, .F. ) ;
#646=CIRCLE ( 'NONE', #21865, 5.249999999999998224 ) ;
#666=ORIENTED_EDGE ( 'NONE', *, *, #47788, .F. ) ;
#675=EDGE_CURVE ( 'NONE', #38177, #26989, #12019, .T. ) ;
#676=DIRECTION ( 'NONE',  ( -3.071710424422018668E-17, 6.404604876783312462E-16, 1.000000000000000000 ) ) ;
#687=AXIS2_PLACEMENT_3D ( 'NONE', #47065, #9654, #39670 ) ;
#690=ORIENTED_EDGE ( 'NONE', *, *, #34751, .F. ) ;
#696=ORIENTED_EDGE ( 'NONE', *, *, #27077, .F. ) ;
#703=ADVANCED_FACE ( 'NONE', ( #935 ), #12739, .T. ) ;
#705=CARTESIAN_POINT ( 'NONE',  ( -15.18259368501833784, -19.55664553709809539, 52.02966884056656482 ) ) ;
#708=LINE ( 'NONE', #44800, #84 ) ;
#716=DIRECTION ( 'NONE',  ( 0.9687793358424819923, -0.2479245821708680464, 0.000000000000000000 ) ) ;
#722=ORIENTED_EDGE ( 'NONE', *, *, #23758, .T. ) ;
#725=AXIS2_PLACEMENT_3D ( 'NONE', #31292, #46326, #12580 ) ;
#742=CARTESIAN_POINT ( 'NONE',  ( -21.95370832667365235, -13.56094844357179774, 49.52966884056655772 ) ) ;
#743=DIRECTION ( 'NONE',  ( 0.9687793358424819923, -0.2479245821708680464, 0.000000000000000000 ) ) ;
#751=AXIS2_PLACEMENT_3D ( 'NONE', #19117, #9016, #23303 ) ;
#756=EDGE_LOOP ( 'NONE', ( #42117, #32142, #13196, #23124 ) ) ;
#758=ADVANCED_FACE ( 'NONE', ( #8328 ), #38334, .T. ) ;
#787=CARTESIAN_POINT ( 'NONE',  ( -17.42409385541299471, -14.80920654474435594, 52.02966884056656482 ) ) ;
#792=ORIENTED_EDGE ( 'NONE', *, *, #5799, .F. ) ;
#803=EDGE_LOOP ( 'NONE', ( #15438, #5843, #2592, #2224 ) ) ;
#804=DIRECTION ( 'NONE',  ( -3.071710424422018668E-17, 6.404604876783312462E-16, 1.000000000000000000 ) ) ;
#809=DIRECTION ( 'NONE',  ( 0.9687793358424821033, -0.2479245821708679909, 0.000000000000000000 ) ) ;
#816=CIRCLE ( 'NONE', #45654, 5.249999999999998224 ) ;
#821=AXIS2_PLACEMENT_3D ( 'NONE', #16794, #39462, #35026 ) ;
#822=DIRECTION ( 'NONE',  ( -3.071710424422018668E-17, 6.404604876783312462E-16, 1.000000000000000000 ) ) ;
#836=ADVANCED_FACE ( 'NONE', ( #24317 ), #20622, .T. ) ;
#838=ORIENTED_EDGE ( 'NONE', *, *, #11852, .F. ) ;
#839=CARTESIAN_POINT ( 'NONE',  ( -20.50876352152090121, -19.05741946913900620, 50.77966884056655772 ) ) ;
#842=CARTESIAN_POINT ( 'NONE',  ( -17.97037870217379307, -19.46375863019785513, 49.52966884056656482 ) ) ;
#846=FACE_OUTER_BOUND ( 'NONE', #41853, .T. ) ;
#857=DIRECTION ( 'NONE',  ( -3.071710424422018668E-17, 6.404604876783312462E-16, 1.000000000000000000 ) ) ;
#858=AXIS2_PLACEMENT_3D ( 'NONE', #11219, #22052, #3330 ) ;
#859=PRODUCT ( 'Cylinder Spindle Drive Pinion', 'Cylinder Spindle Drive Pinion', '', ( #38787 ) ) ;
#885=CIRCLE ( 'NONE', #32357, 5.249999999999998224 ) ;
#888=LINE ( 'NONE', #11475, #13733 ) ;
#889=ADVANCED_FACE ( 'NONE', ( #13916 ), #6318, .T. ) ;
#905=VECTOR ( 'NONE', #30121, 1000.000000000000000 ) ;
#908=ADVANCED_FACE ( 'NONE', ( #25035 ), #21350, .T. ) ;
#933=CARTESIAN_POINT ( 'NONE',  ( -13.16616306552584525, -16.76709000361798729, 52.02966884056656482 ) ) ;
#935=FACE_OUTER_BOUND ( 'NONE', #23114, .T. ) ;
#939=CARTESIAN_POINT ( 'NONE',  ( -22.10931616815485512, -14.45671906187057765, 49.52966884056655772 ) ) ;
#940=CARTESIAN_POINT ( 'NONE',  ( -13.08950423898529891, -12.99622877252704001, 49.52966884056655772 ) ) ;
#947=CYLINDRICAL_SURFACE ( 'NONE', #43357, 2.000000000000001776 ) ;
#949=LINE ( 'NONE', #16675, #21144 ) ;
#951=CARTESIAN_POINT ( 'NONE',  ( -17.42409385541299471, -14.80920654474435771, 49.52966884056655772 ) ) ;
#953=CARTESIAN_POINT ( 'NONE',  ( -17.42409385541299471, -14.80920654474435771, 49.52966884056655772 ) ) ;
#960=LINE ( 'NONE', #19181, #25787 ) ;
#978=VERTEX_POINT ( 'NONE', #4100 ) ;
#979=CARTESIAN_POINT ( 'NONE',  ( -22.10931616815485512, -14.45671906187057765, 49.52966884056655772 ) ) ;
#988=CARTESIAN_POINT ( 'NONE',  ( -18.53667165497532920, -10.24437071140731170, 49.52966884056655772 ) ) ;
#993=LINE ( 'NONE', #12790, #23602 ) ;
#1006=CARTESIAN_POINT ( 'NONE',  ( -14.49326647312024896, -18.48150914673672673, 49.52966884056656482 ) ) ;
#1031=EDGE_CURVE ( 'NONE', #44193, #26463, #2448, .T. ) ;
#1038=EDGE_CURVE ( 'NONE', #14018, #36826, #27456, .T. ) ;
#1052=LINE ( 'NONE', #8439, #21248 ) ;
#1062=DIRECTION ( 'NONE',  ( -3.071710424422018668E-17, 6.404604876783312462E-16, 1.000000000000000000 ) ) ;
#1108=DIRECTION ( 'NONE',  ( -3.071710424422018668E-17, 6.404604876783312462E-16, 1.000000000000000000 ) ) ;
#1117=DIRECTION ( 'NONE',  ( -3.071710424422018668E-17, 6.404604876783312462E-16, 1.000000000000000000 ) ) ;
#1121=EDGE_LOOP ( 'NONE', ( #5972, #21631, #1124, #13446 ) ) ;
#1124=ORIENTED_EDGE ( 'NONE', *, *, #155, .F. ) ;
#1130=DIRECTION ( 'NONE',  ( -0.2189141945955536406, 0.9757441136919965397, 0.000000000000000000 ) ) ;
#1135=CARTESIAN_POINT ( 'NONE',  ( -12.82148049030644366, -13.86501071932494789, 49.52966884056655772 ) ) ;
#1141=DIRECTION ( 'NONE',  ( -0.09332174201254904433, -0.9956360040033421788, 0.000000000000000000 ) ) ;
#1168=VERTEX_POINT ( 'NONE', #5556 ) ;
#1186=LINE ( 'NONE', #15957, #1307 ) ;
#1196=LINE ( 'NONE', #8854, #39902 ) ;
#1198=CARTESIAN_POINT ( 'NONE',  ( -16.89979169948162863, -10.14008855580012636, 49.52966884056655772 ) ) ;
#1202=ORIENTED_EDGE ( 'NONE', *, *, #29445, .F. ) ;
#1203=FACE_OUTER_BOUND ( 'NONE', #17281, .T. ) ;
#1206=ADVANCED_FACE ( 'NONE', ( #27938 ), #17572, .T. ) ;
#1265=VERTEX_POINT ( 'NONE', #7739 ) ;
#1266=DIRECTION ( 'NONE',  ( -3.071710424422018668E-17, 6.404604876783312462E-16, 1.000000000000000000 ) ) ;
#1267=AXIS2_PLACEMENT_3D ( 'NONE', #12783, #38885, #1708 ) ;
#1268=EDGE_CURVE ( 'NONE', #978, #24257, #7995, .T. ) ;
#1271=EDGE_CURVE ( 'NONE', #45644, #6216, #9567, .T. ) ;
#1281=ORIENTED_EDGE ( 'NONE', *, *, #13800, .T. ) ;
#1282=CARTESIAN_POINT ( 'NONE',  ( -16.31151605585062825, -19.37404237808139484, 49.52966884056656482 ) ) ;
#1285=LINE ( 'NONE', #6453, #24285 ) ;
#1298=FACE_OUTER_BOUND ( 'NONE', #39040, .T. ) ;
#1307=VECTOR ( 'NONE', #19676, 1000.000000000000000 ) ;
#1323=DIRECTION ( 'NONE',  ( 0.6607190350373968180, 0.7506333037770515082, 0.000000000000000000 ) ) ;
#1337=DIRECTION ( 'NONE',  ( -0.9687793358424822143, 0.2479245821708672415, 0.000000000000000000 ) ) ;
#1346=DIRECTION ( 'NONE',  ( 0.9294853595766541243, 0.3688590060343629462, 0.000000000000000000 ) ) ;
#1351=CARTESIAN_POINT ( 'NONE',  ( -12.91230480768039790, -16.07689808402359688, 49.52966884056655772 ) ) ;
#1353=LINE ( 'NONE', #27468, #17228 ) ;
#1359=ORIENTED_EDGE ( 'NONE', *, *, #45101, .T. ) ;
#1361=EDGE_CURVE ( 'NONE', #18903, #14963, #11138, .T. ) ;
#1367=FACE_OUTER_BOUND ( 'NONE', #6278, .T. ) ;
#1394=CARTESIAN_POINT ( 'NONE',  ( -16.36862302632751209, -10.24310716135927812, 49.52966884056655772 ) ) ;
#1400=CARTESIAN_POINT ( 'NONE',  ( -17.42409385541299471, -14.80920654474435771, 49.52966884056655772 ) ) ;
#1404=VECTOR ( 'NONE', #1062, 1000.000000000000000 ) ;
#1414=DIRECTION ( 'NONE',  ( -3.071710424422018668E-17, 6.404604876783312462E-16, 1.000000000000000000 ) ) ;
#1423=EDGE_CURVE ( 'NONE', #36239, #45570, #4083, .T. ) ;
#1426=ORIENTED_EDGE ( 'NONE', *, *, #7501, .T. ) ;
#1432=EDGE_CURVE ( 'NONE', #39290, #30479, #14258, .T. ) ;
#1435=LINE ( 'NONE', #31729, #4314 ) ;
#1438=ORIENTED_EDGE ( 'NONE', *, *, #37978, .T. ) ;
#1460=VERTEX_POINT ( 'NONE', #47088 ) ;
#1462=ORIENTED_EDGE ( 'NONE', *, *, #34088, .F. ) ;
#1471=ORIENTED_EDGE ( 'NONE', *, *, #41370, .T. ) ;
#1474=AXIS2_PLACEMENT_3D ( 'NONE', #30595, #38435, #12586 ) ;
#1482=DIRECTION ( 'NONE',  ( 0.9687793358424821033, -0.2479245821708677133, 0.000000000000000000 ) ) ;
#1491=CARTESIAN_POINT ( 'NONE',  ( -15.04196850781542594, -10.13074752191075234, 52.02966884056656482 ) ) ;
#1493=VECTOR ( 'NONE', #7923, 1000.000000000000000 ) ;
#1500=ADVANCED_FACE ( 'NONE', ( #20981 ), #32543, .T. ) ;
#1506=EDGE_CURVE ( 'NONE', #21704, #39406, #13569, .T. ) ;
#1509=VERTEX_POINT ( 'NONE', #6205 ) ;
#1516=CIRCLE ( 'NONE', #751, 5.249999999999998224 ) ;
#1521=CIRCLE ( 'NONE', #10982, 4.686499999999998778 ) ;
#1525=DIRECTION ( 'NONE',  ( 0.9687793358424821033, -0.2479245821708680464, 0.000000000000000000 ) ) ;
#1539=DIRECTION ( 'NONE',  ( -0.6380325334150318550, 0.7700094066334490783, 0.000000000000000000 ) ) ;
#1546=ORIENTED_EDGE ( 'NONE', *, *, #18949, .F. ) ;
#1553=DIRECTION ( 'NONE',  ( 0.2189141945955469237, -0.9757441136919980940, 0.000000000000000000 ) ) ;
#1564=DIRECTION ( 'NONE',  ( -3.071710424422018668E-17, 6.404604876783312462E-16, 1.000000000000000000 ) ) ;
#1570=EDGE_LOOP ( 'NONE', ( #22090, #16579, #22831, #22061 ) ) ;
#1576=ADVANCED_FACE ( 'NONE', ( #3229 ), #6684, .T. ) ;
#1583=CIRCLE ( 'NONE', #36959, 1.999999999999999556 ) ;
#1590=VERTEX_POINT ( 'NONE', #47801 ) ;
#1593=ORIENTED_EDGE ( 'NONE', *, *, #25907, .F. ) ;
#1605=CYLINDRICAL_SURFACE ( 'NONE', #36816, 1.999999999999999556 ) ;
#1608=EDGE_LOOP ( 'NONE', ( #37377, #5794, #41248, #33507 ) ) ;
#1621=VECTOR ( 'NONE', #33239, 1000.000000000000000 ) ;
#1627=CIRCLE ( 'NONE', #22876, 4.686499999999998778 ) ;
#1628=VERTEX_POINT ( 'NONE', #29831 ) ;
#1630=CYLINDRICAL_SURFACE ( 'NONE', #47769, 2.000000000000001332 ) ;
#1682=DIRECTION ( 'NONE',  ( -0.09332174201254901658, -0.9956360040033421788, 0.000000000000000000 ) ) ;
#1699=CARTESIAN_POINT ( 'NONE',  ( -17.42409385541299471, -14.80920654474435594, 52.02966884056656482 ) ) ;
#1708=DIRECTION ( 'NONE',  ( 0.9687793358424819923, -0.2479245821708680464, 0.000000000000000000 ) ) ;
#1709=AXIS2_PLACEMENT_3D ( 'NONE', #47970, #2666, #17905 ) ;
#1714=DIRECTION ( 'NONE',  ( 0.9687793358424819923, -0.2479245821708680464, 0.000000000000000000 ) ) ;
#1715=AXIS2_PLACEMENT_3D ( 'NONE', #16235, #38165, #8642 ) ;
#1716=EDGE_CURVE ( 'NONE', #43657, #11090, #15757, .T. ) ;
#1721=ORIENTED_EDGE ( 'NONE', *, *, #16188, .T. ) ;
#1723=ORIENTED_EDGE ( 'NONE', *, *, #13237, .T. ) ;
#1726=EDGE_LOOP ( 'NONE', ( #16385, #30504, #28035, #30614 ) ) ;
#1740=DIRECTION ( 'NONE',  ( -3.071710424422018668E-17, 6.404604876783312462E-16, 1.000000000000000000 ) ) ;
#1750=DIRECTION ( 'NONE',  ( -3.071710424422018668E-17, 6.404604876783312462E-16, 1.000000000000000000 ) ) ;
#1752=VERTEX_POINT ( 'NONE', #34962 ) ;
#1757=DIRECTION ( 'NONE',  ( 0.9687793358424821033, -0.2479245821708679909, 0.000000000000000000 ) ) ;
#1774=EDGE_CURVE ( 'NONE', #32600, #15426, #22965, .T. ) ;
#1775=ORIENTED_EDGE ( 'NONE', *, *, #19161, .T. ) ;
#1785=CARTESIAN_POINT ( 'NONE',  ( -17.42409385541299471, -14.80920654474434883, 62.02966884056656482 ) ) ;
#1794=CARTESIAN_POINT ( 'NONE',  ( -16.34301583228449317, -10.23680828416977384, 52.02966884056656482 ) ) ;
#1817=ORIENTED_EDGE ( 'NONE', *, *, #39548, .T. ) ;
#1825=DIRECTION ( 'NONE',  ( -3.071710424422018668E-17, 6.404604876783312462E-16, 1.000000000000000000 ) ) ;
#1829=CARTESIAN_POINT ( 'NONE',  ( -14.33701861991839976, -19.05567172067550530, 49.52966884056656482 ) ) ;
#1832=ORIENTED_EDGE ( 'NONE', *, *, #10446, .F. ) ;
#1842=DIRECTION ( 'NONE',  ( -3.071710424422018668E-17, 6.404604876783312462E-16, 1.000000000000000000 ) ) ;
#1856=ORIENTED_EDGE ( 'NONE', *, *, #41314, .F. ) ;
#1857=CARTESIAN_POINT ( 'NONE',  ( -14.49326647312024896, -18.48150914673672673, 49.52966884056656482 ) ) ;
#1858=DIRECTION ( 'NONE',  ( 0.09332174201254166135, 0.9956360040033429559, 0.000000000000000000 ) ) ;
#1859=DIRECTION ( 'NONE',  ( -3.071710424422018668E-17, 6.404604876783312462E-16, 1.000000000000000000 ) ) ;
#1861=ORIENTED_EDGE ( 'NONE', *, *, #24474, .T. ) ;
#1867=FACE_OUTER_BOUND ( 'NONE', #22414, .T. ) ;
#1878=ORIENTED_EDGE ( 'NONE', *, *, #30425, .T. ) ;
#1888=CYLINDRICAL_SURFACE ( 'NONE', #42878, 2.000000000000003553 ) ;
#1893=EDGE_CURVE ( 'NONE', #11361, #36726, #22032, .T. ) ;
#1912=EDGE_CURVE ( 'NONE', #25645, #15953, #40864, .T. ) ;
#1942=VERTEX_POINT ( 'NONE', #33426 ) ;
#1947=AXIS2_PLACEMENT_3D ( 'NONE', #16013, #22706, #31057 ) ;
#1954=ORIENTED_EDGE ( 'NONE', *, *, #19326, .T. ) ;
#1963=CARTESIAN_POINT ( 'NONE',  ( -17.42409385541299471, -14.80920654474435594, 52.02966884056656482 ) ) ;
#1966=LINE ( 'NONE', #9125, #9036 ) ;
#1973=ORIENTED_EDGE ( 'NONE', *, *, #7462, .F. ) ;
#1975=CARTESIAN_POINT ( 'NONE',  ( -12.76954176995949197, -15.35549139150514186, 49.52966884056655772 ) ) ;
#1989=CIRCLE ( 'NONE', #28737, 5.249999999999998224 ) ;
#1993=DIRECTION ( 'NONE',  ( -3.071710424422018668E-17, 6.404604876783312462E-16, 1.000000000000000000 ) ) ;
#2001=ORIENTED_EDGE ( 'NONE', *, *, #34563, .T. ) ;
#2006=CARTESIAN_POINT ( 'NONE',  ( -12.23849770038826534, -15.62901903366650025, 52.02966884056656482 ) ) ;
#2012=ORIENTED_EDGE ( 'NONE', *, *, #20395, .T. ) ;
#2036=CARTESIAN_POINT ( 'NONE',  ( -22.60922486080212934, -15.63195587288279675, 49.52966884056655772 ) ) ;
#2037=CARTESIAN_POINT ( 'NONE',  ( -21.99019323879806365, -13.75373571565882713, 49.52966884056655772 ) ) ;
#2053=CARTESIAN_POINT ( 'NONE',  ( -18.47956468449850931, -19.37530592812942842, 49.52966884056656482 ) ) ;
#2064=DIRECTION ( 'NONE',  ( 0.9687793358424819923, -0.2479245821708676023, 0.000000000000000000 ) ) ;
#2076=CARTESIAN_POINT ( 'NONE',  ( -13.07710726710083193, -16.59225537930583982, 52.02966884056656482 ) ) ;
#2085=AXIS2_PLACEMENT_3D ( 'NONE', #979, #11565, #27073 ) ;
#2087=CYLINDRICAL_SURFACE ( 'NONE', #28208, 1.999999999999999112 ) ;
#2091=LINE ( 'NONE', #32840, #26751 ) ;
#2121=CIRCLE ( 'NONE', #44582, 1.999999999999999556 ) ;
#2122=ORIENTED_EDGE ( 'NONE', *, *, #47124, .F. ) ;
#2129=ORIENTED_EDGE ( 'NONE', *, *, #8208, .T. ) ;
#2131=EDGE_CURVE ( 'NONE', #42275, #26781, #2091, .T. ) ;
#2134=DIRECTION ( 'NONE',  ( -3.071710424422018668E-17, 6.404604876783312462E-16, 1.000000000000000000 ) ) ;
#2139=CARTESIAN_POINT ( 'NONE',  ( -14.35043204381087101, -18.34698626059704551, 49.52966884056656482 ) ) ;
#2143=ORIENTED_EDGE ( 'NONE', *, *, #2952, .T. ) ;
#2146=FACE_OUTER_BOUND ( 'NONE', #41416, .T. ) ;
#2154=CARTESIAN_POINT ( 'NONE',  ( -17.42409385541299471, -14.80920654474435594, 52.02966884056656482 ) ) ;
#2156=ADVANCED_FACE ( 'NONE', ( #20141 ), #39760, .T. ) ;
#2172=ADVANCED_FACE ( 'NONE', ( #12508 ), #24758, .T. ) ;
#2178=CARTESIAN_POINT ( 'NONE',  ( -22.10679845867080928, -14.99777973644470919, 52.02966884056656482 ) ) ;
#2181=EDGE_CURVE ( 'NONE', #46754, #13759, #44059, .T. ) ;
#2206=CARTESIAN_POINT ( 'NONE',  ( -21.13745558015973103, -11.09794736473739718, 50.77966884056655772 ) ) ;
#2209=CARTESIAN_POINT ( 'NONE',  ( -19.07667242297576138, -10.41096375660395168, 49.52966884056655772 ) ) ;
#2214=VERTEX_POINT ( 'NONE', #21052 ) ;
#2217=DIRECTION ( 'NONE',  ( -0.9979768094191907579, -0.06357898915123130767, 0.000000000000000000 ) ) ;
#2224=ORIENTED_EDGE ( 'NONE', *, *, #20934, .T. ) ;
#2227=CARTESIAN_POINT ( 'NONE',  ( -21.57657733182563931, -11.59682721189464871, 52.02966884056656482 ) ) ;
#2232=ORIENTED_EDGE ( 'NONE', *, *, #6046, .T. ) ;
#2233=DIRECTION ( 'NONE',  ( 0.9687793358424821033, -0.2479245821708679909, 0.000000000000000000 ) ) ;
#2235=DIRECTION ( 'NONE',  ( 3.071710424422018668E-17, -6.404604876783312462E-16, -1.000000000000000000 ) ) ;
#2237=ORIENTED_EDGE ( 'NONE', *, *, #23244, .T. ) ;
#2239=DIRECTION ( 'NONE',  ( -3.071710424422018668E-17, 6.404604876783312462E-16, 1.000000000000000000 ) ) ;
#2259=LINE ( 'NONE', #42431, #35652 ) ;
#2266=ORIENTED_EDGE ( 'NONE', *, *, #29882, .F. ) ;
#2267=CARTESIAN_POINT ( 'NONE',  ( -21.44055400477819973, -12.39439182751215718, 49.52966884056655772 ) ) ;
#2273=CARTESIAN_POINT ( 'NONE',  ( -19.07667242297576138, -10.41096375660394990, 52.02966884056656482 ) ) ;
#2278=ORIENTED_EDGE ( 'NONE', *, *, #38859, .T. ) ;
#2290=EDGE_CURVE ( 'NONE', #38294, #3327, #43871, .T. ) ;
#2297=AXIS2_PLACEMENT_3D ( 'NONE', #33032, #47367, #13596 ) ;
#2298=AXIS2_PLACEMENT_3D ( 'NONE', #46917, #1859, #6283 ) ;
#2299=EDGE_LOOP ( 'NONE', ( #26074, #31385, #6841, #23143 ) ) ;
#2300=VERTEX_POINT ( 'NONE', #3302 ) ;
#2329=CIRCLE ( 'NONE', #25920, 4.686500000000000554 ) ;
#2342=VERTEX_POINT ( 'NONE', #11667 ) ;
#2343=CYLINDRICAL_SURFACE ( 'NONE', #8224, 2.000000000000001776 ) ;
#2352=ORIENTED_EDGE ( 'NONE', *, *, #41187, .T. ) ;
#2363=ADVANCED_FACE ( 'NONE', ( #1298 ), #12634, .T. ) ;
#2366=AXIS2_PLACEMENT_3D ( 'NONE', #41844, #37890, #716 ) ;
#2400=AXIS2_PLACEMENT_3D ( 'NONE', #13486, #16931, #43054 ) ;
#2402=ORIENTED_EDGE ( 'NONE', *, *, #40804, .F. ) ;
#2407=AXIS2_PLACEMENT_3D ( 'NONE', #1400, #15688, #34398 ) ;
#2428=CARTESIAN_POINT ( 'NONE',  ( -15.46621039653938112, -10.55127575485719760, 49.52966884056655772 ) ) ;
#2433=VECTOR ( 'NONE', #11280, 1000.000000000000000 ) ;
#2447=DIRECTION ( 'NONE',  ( -3.071710424422018668E-17, 6.404604876783312462E-16, 1.000000000000000000 ) ) ;
#2448=CIRCLE ( 'NONE', #37844, 1.999999999999999778 ) ;
#2456=CYLINDRICAL_SURFACE ( 'NONE', #14455, 1.999999999999999556 ) ;
#2458=DIRECTION ( 'NONE',  ( -3.071710424422018668E-17, 6.404604876783312462E-16, 1.000000000000000000 ) ) ;
#2459=VECTOR ( 'NONE', #6899, 1000.000000000000000 ) ;
#2475=FACE_OUTER_BOUND ( 'NONE', #30961, .T. ) ;
#2481=EDGE_LOOP ( 'NONE', ( #42885, #32173, #36088, #32848 ) ) ;
#2486=SHAPE_REPRESENTATION ( 'Cylinder Spindle Drive Pinion', ( #29031 ), #29815 ) ;
#2487=ORIENTED_EDGE ( 'NONE', *, *, #13354, .T. ) ;
#2499=ORIENTED_EDGE ( 'NONE', *, *, #10108, .F. ) ;
#2513=ORIENTED_EDGE ( 'NONE', *, *, #46170, .F. ) ;
#2521=ORIENTED_EDGE ( 'NONE', *, *, #26961, .F. ) ;
#2541=ORIENTED_EDGE ( 'NONE', *, *, #32856, .F. ) ;
#2557=ADVANCED_FACE ( 'NONE', ( #10156 ), #25178, .T. ) ;
#2561=CARTESIAN_POINT ( 'NONE',  ( -19.23707162763026801, -10.47461692831663882, 52.02966884056656482 ) ) ;
#2563=LINE ( 'NONE', #25213, #6871 ) ;
#2564=CYLINDRICAL_SURFACE ( 'NONE', #33770, 4.686499999999997002 ) ;
#2568=CARTESIAN_POINT ( 'NONE',  ( -13.02585106727260822, -13.15662797718154131, 52.02966884056656482 ) ) ;
#2578=CARTESIAN_POINT ( 'NONE',  ( -17.42409385541299471, -14.80920654474435771, 49.52966884056655772 ) ) ;
#2582=ORIENTED_EDGE ( 'NONE', *, *, #34712, .T. ) ;
#2592=ORIENTED_EDGE ( 'NONE', *, *, #16262, .T. ) ;
#2599=EDGE_LOOP ( 'NONE', ( #20684, #13603, #13294, #28141 ) ) ;
#2609=DIRECTION ( 'NONE',  ( -3.071710424422018668E-17, 6.404604876783312462E-16, 1.000000000000000000 ) ) ;
#2610=EDGE_LOOP ( 'NONE', ( #24201, #43210, #17542, #32687 ) ) ;
#2614=FACE_OUTER_BOUND ( 'NONE', #17833, .T. ) ;
#2627=CARTESIAN_POINT ( 'NONE',  ( -17.42409385541299471, -14.80920654474435594, 52.02966884056656482 ) ) ;
#2638=CARTESIAN_POINT ( 'NONE',  ( -22.58237342315448615, -13.83214364962418230, 49.52966884056655772 ) ) ;
#2655=AXIS2_PLACEMENT_3D ( 'NONE', #29899, #15091, #3297 ) ;
#2664=CARTESIAN_POINT ( 'NONE',  ( -16.60428136649079534, -9.623610389719635450, 52.02966884056656482 ) ) ;
#2666=DIRECTION ( 'NONE',  ( -3.071710424422018668E-17, 6.404604876783312462E-16, 1.000000000000000000 ) ) ;
#2677=LINE ( 'NONE', #25574, #27360 ) ;
#2680=CARTESIAN_POINT ( 'NONE',  ( -15.80316865820435446, -9.815700611529285524, 50.77966884056655772 ) ) ;
#2681=CIRCLE ( 'NONE', #6599, 4.686499999999999666 ) ;
#2683=VERTEX_POINT ( 'NONE', #10406 ) ;
#2686=DIRECTION ( 'NONE',  ( -3.071710424422018668E-17, 6.404604876783312462E-16, 1.000000000000000000 ) ) ;
#2688=ORIENTED_EDGE ( 'NONE', *, *, #29882, .T. ) ;
#2713=FACE_OUTER_BOUND ( 'NONE', #32187, .T. ) ;
#2725=ORIENTED_EDGE ( 'NONE', *, *, #22932, .F. ) ;
#2734=DIRECTION ( 'NONE',  ( -0.06357898915124167438, 0.9979768094191900918, 0.000000000000000000 ) ) ;
#2736=EDGE_CURVE ( 'NONE', #5301, #18974, #20280, .T. ) ;
#2737=DIRECTION ( 'NONE',  ( -3.071710424422018668E-17, 6.404604876783312462E-16, 1.000000000000000000 ) ) ;
#2739=CARTESIAN_POINT ( 'NONE',  ( -17.03658212107600534, -14.90837637761270251, 52.02966884056656482 ) ) ;
#2742=DIRECTION ( 'NONE',  ( -0.9979768094191906469, -0.06357898915123129380, 0.000000000000000000 ) ) ;
#2747=AXIS2_PLACEMENT_3D ( 'NONE', #9139, #5447, #2217 ) ;
#2773=ORIENTED_EDGE ( 'NONE', *, *, #23450, .T. ) ;
#2794=DIRECTION ( 'NONE',  ( -3.071710424422018668E-17, 6.404604876783312462E-16, 1.000000000000000000 ) ) ;
#2799=DIRECTION ( 'NONE',  ( -3.071710424422018668E-17, 6.404604876783312462E-16, 1.000000000000000000 ) ) ;
#2809=CARTESIAN_POINT ( 'NONE',  ( -17.42409385541299471, -14.80920654474434883, 62.02966884056656482 ) ) ;
#2810=VERTEX_POINT ( 'NONE', #1975 ) ;
#2836=CARTESIAN_POINT ( 'NONE',  ( -17.42409385541299471, -14.80920654474435771, 49.52966884056655772 ) ) ;
#2840=VECTOR ( 'NONE', #5845, 1000.000000000000000 ) ;
#2841=CIRCLE ( 'NONE', #45330, 0.3999999999999978018 ) ;
#2859=EDGE_LOOP ( 'NONE', ( #7531, #28675, #40101, #15893 ) ) ;
#2865=DIRECTION ( 'NONE',  ( 0.9687793358424821033, -0.2479245821708680464, 0.000000000000000000 ) ) ;
#2879=DIRECTION ( 'NONE',  ( -3.071710424422018668E-17, 6.404604876783312462E-16, 1.000000000000000000 ) ) ;
#2892=ORIENTED_EDGE ( 'NONE', *, *, #31131, .F. ) ;
#2914=EDGE_CURVE ( 'NONE', #29156, #19709, #25018, .T. ) ;
#2918=CIRCLE ( 'NONE', #46976, 5.249999999999998224 ) ;
#2930=DIRECTION ( 'NONE',  ( 3.071710424422018668E-17, -6.404604876783312462E-16, -1.000000000000000000 ) ) ;
#2936=FACE_OUTER_BOUND ( 'NONE', #31371, .T. ) ;
#2945=CIRCLE ( 'NONE', #25732, 1.999999999999999112 ) ;
#2952=EDGE_CURVE ( 'NONE', #21408, #38015, #5341, .T. ) ;
#2954=ORIENTED_EDGE ( 'NONE', *, *, #42838, .F. ) ;
#2967=ORIENTED_EDGE ( 'NONE', *, *, #28625, .T. ) ;
#2971=CARTESIAN_POINT ( 'NONE',  ( -14.33942418930512019, -10.56099362034968614, 49.52966884056655772 ) ) ;
#2978=DIRECTION ( 'NONE',  ( -3.071710424422018668E-17, 6.404604876783312462E-16, 1.000000000000000000 ) ) ;
#2983=CARTESIAN_POINT ( 'NONE',  ( -19.66559402580761784, -10.06176755239059872, 49.52966884056655772 ) ) ;
#2995=CARTESIAN_POINT ( 'NONE',  ( -17.42260713176972686, -20.05920633423509258, 49.52966884056656482 ) ) ;
#3010=DIRECTION ( 'NONE',  ( -0.9687793358424822143, 0.2479245821708672415, 0.000000000000000000 ) ) ;
#3012=ORIENTED_EDGE ( 'NONE', *, *, #1432, .T. ) ;
#3016=CIRCLE ( 'NONE', #47036, 4.686499999999998778 ) ;
#3026=FACE_OUTER_BOUND ( 'NONE', #16486, .T. ) ;
#3041=EDGE_LOOP ( 'NONE', ( #23030, #43391, #22933, #19767 ) ) ;
#3058=CIRCLE ( 'NONE', #47886, 2.000000000000000000 ) ;
#3069=ORIENTED_EDGE ( 'NONE', *, *, #19985, .F. ) ;
#3070=ORIENTED_EDGE ( 'NONE', *, *, #9498, .F. ) ;
#3073=EDGE_CURVE ( 'NONE', #15483, #2214, #960, .T. ) ;
#3080=DIRECTION ( 'NONE',  ( -3.071710424422018668E-17, 6.404604876783312462E-16, 1.000000000000000000 ) ) ;
#3085=CIRCLE ( 'NONE', #12553, 2.000000000000000444 ) ;
#3086=CIRCLE ( 'NONE', #29819, 2.000000000000001332 ) ;
#3087=VERTEX_POINT ( 'NONE', #34426 ) ;
#3107=DIRECTION ( 'NONE',  ( -0.9687793358424819923, 0.2479245821708680464, 0.000000000000000000 ) ) ;
#3112=ORIENTED_EDGE ( 'NONE', *, *, #48606, .F. ) ;
#3117=DIRECTION ( 'NONE',  ( -3.071710424422018668E-17, 6.404604876783312462E-16, 1.000000000000000000 ) ) ;
#3128=CARTESIAN_POINT ( 'NONE',  ( -17.42409385541299471, -14.80920654474435594, 52.02966884056656482 ) ) ;
#3131=AXIS2_PLACEMENT_3D ( 'NONE', #27483, #24540, #9261 ) ;
#3133=ORIENTED_EDGE ( 'NONE', *, *, #452, .F. ) ;
#3134=ORIENTED_EDGE ( 'NONE', *, *, #8371, .F. ) ;
#3137=EDGE_CURVE ( 'NONE', #26463, #45860, #35232, .T. ) ;
#3141=CIRCLE ( 'NONE', #33821, 4.686500000000000554 ) ;
#3151=ORIENTED_EDGE ( 'NONE', *, *, #21193, .F. ) ;
#3154=EDGE_CURVE ( 'NONE', #1265, #20388, #5384, .T. ) ;
#3158=CIRCLE ( 'NONE', #47216, 4.686499999999997002 ) ;
#3167=CARTESIAN_POINT ( 'NONE',  ( -12.82148049030644366, -13.86501071932494789, 49.52966884056655772 ) ) ;
#3170=VERTEX_POINT ( 'NONE', #17416 ) ;
#3172=AXIS2_PLACEMENT_3D ( 'NONE', #9459, #20774, #31855 ) ;
#3173=DIRECTION ( 'NONE',  ( 3.071710424422018668E-17, -6.404604876783312462E-16, -1.000000000000000000 ) ) ;
#3180=ORIENTED_EDGE ( 'NONE', *, *, #33371, .T. ) ;
#3188=CARTESIAN_POINT ( 'NONE',  ( -16.56761320685650318, -19.87745396966068157, 49.52966884056656482 ) ) ;
#3198=EDGE_CURVE ( 'NONE', #8796, #35282, #41543, .T. ) ;
#3199=EDGE_CURVE ( 'NONE', #18527, #28383, #21124, .T. ) ;
#3205=LINE ( 'NONE', #32751, #31154 ) ;
#3219=AXIS2_PLACEMENT_3D ( 'NONE', #25851, #22167, #29797 ) ;
#3227=CARTESIAN_POINT ( 'NONE',  ( -12.85925802207596114, -13.69662874518197171, 49.52966884056655772 ) ) ;
#3229=FACE_OUTER_BOUND ( 'NONE', #21351, .T. ) ;
#3235=FACE_OUTER_BOUND ( 'NONE', #13514, .T. ) ;
#3239=ORIENTED_EDGE ( 'NONE', *, *, #45854, .T. ) ;
#3245=DIRECTION ( 'NONE',  ( 0.9180681052388950381, -0.3964226963016435068, 0.000000000000000000 ) ) ;
#3266=VERTEX_POINT ( 'NONE', #14414 ) ;
#3267=VERTEX_POINT ( 'NONE', #7333 ) ;
#3275=EDGE_CURVE ( 'NONE', #19030, #5150, #28945, .T. ) ;
#3280=DIRECTION ( 'NONE',  ( 3.071710424422018668E-17, -6.404604876783312462E-16, -1.000000000000000000 ) ) ;
#3291=AXIS2_PLACEMENT_3D ( 'NONE', #17017, #17514, #28126 ) ;
#3297=DIRECTION ( 'NONE',  ( -0.5351595679979678222, -0.8447509909909716175, 0.000000000000000000 ) ) ;
#3302=CARTESIAN_POINT ( 'NONE',  ( -19.04501905262167227, -19.80271247795941392, 52.02966884056656482 ) ) ;
#3307=EDGE_CURVE ( 'NONE', #39007, #38050, #6825, .T. ) ;
#3317=DIRECTION ( 'NONE',  ( -0.9687793358424822143, 0.2479245821708672415, 0.000000000000000000 ) ) ;
#3327=VERTEX_POINT ( 'NONE', #44758 ) ;
#3330=DIRECTION ( 'NONE',  ( 0.5351595679979626041, 0.8447509909909748371, 0.000000000000000000 ) ) ;
#3359=DIRECTION ( 'NONE',  ( -3.071710424422018668E-17, 6.404604876783312462E-16, 1.000000000000000000 ) ) ;
#3362=EDGE_CURVE ( 'NONE', #39489, #13083, #27262, .T. ) ;
#3380=CARTESIAN_POINT ( 'NONE',  ( -19.71801720247071543, -10.72249662993225883, 52.02966884056656482 ) ) ;
#3389=CIRCLE ( 'NONE', #33237, 1.999999999999999112 ) ;
#3391=CARTESIAN_POINT ( 'NONE',  ( -17.61266704711333375, -10.12650194148654137, 52.02966884056656482 ) ) ;
#3394=ORIENTED_EDGE ( 'NONE', *, *, #36523, .T. ) ;
#3411=DIRECTION ( 'NONE',  ( 0.5097212845717493668, -0.8603395911234852367, 0.000000000000000000 ) ) ;
#3421=CIRCLE ( 'NONE', #19955, 4.686499999999999666 ) ;
#3436=CARTESIAN_POINT ( 'NONE',  ( -17.63665770386090514, -10.11555421891856099, 49.52966884056655772 ) ) ;
#3438=ORIENTED_EDGE ( 'NONE', *, *, #2290, .F. ) ;
#3456=ORIENTED_EDGE ( 'NONE', *, *, #1423, .F. ) ;
#3468=ORIENTED_EDGE ( 'NONE', *, *, #4108, .F. ) ;
#3472=EDGE_CURVE ( 'NONE', #12455, #16401, #16233, .T. ) ;
#3513=ORIENTED_EDGE ( 'NONE', *, *, #20645, .F. ) ;
#3520=DIRECTION ( 'NONE',  ( -3.071710424422018668E-17, 6.404604876783312462E-16, 1.000000000000000000 ) ) ;
#3532=DIRECTION ( 'NONE',  ( -3.071710424422018668E-17, 6.404604876783312462E-16, 1.000000000000000000 ) ) ;
#3533=DIRECTION ( 'NONE',  ( 0.3964226963016399541, 0.9180681052388965924, 0.000000000000000000 ) ) ;
#3539=ADVANCED_FACE ( 'NONE', ( #30971 ), #45986, .T. ) ;
#3546=LINE ( 'NONE', #25713, #7764 ) ;
#3561=ORIENTED_EDGE ( 'NONE', *, *, #31459, .T. ) ;
#3565=DIRECTION ( 'NONE',  ( -3.071710424422018668E-17, 6.404604876783312462E-16, 1.000000000000000000 ) ) ;
#3573=DIRECTION ( 'NONE',  ( 3.071710424422018668E-17, -6.404604876783312462E-16, -1.000000000000000000 ) ) ;
#3589=CARTESIAN_POINT ( 'NONE',  ( -17.42409385541299471, -14.80920654474435771, 49.52966884056655772 ) ) ;
#3601=ORIENTED_EDGE ( 'NONE', *, *, #34070, .T. ) ;
#3603=EDGE_CURVE ( 'NONE', #47392, #27894, #17614, .T. ) ;
#3607=CARTESIAN_POINT ( 'NONE',  ( -22.60922486080212934, -15.63195587288279320, 50.77966884056655772 ) ) ;
#3610=ADVANCED_FACE ( 'NONE', ( #21088 ), #21338, .T. ) ;
#3612=ORIENTED_EDGE ( 'NONE', *, *, #7248, .F. ) ;
#3632=VECTOR ( 'NONE', #10931, 1000.000000000000000 ) ;
#3641=DIRECTION ( 'NONE',  ( -0.9687793358424822143, 0.2479245821708672415, 0.000000000000000000 ) ) ;
#3649=ORIENTED_EDGE ( 'NONE', *, *, #1506, .F. ) ;
#3698=ORIENTED_EDGE ( 'NONE', *, *, #13348, .F. ) ;
#3700=DIRECTION ( 'NONE',  ( 0.3964226963016398431, 0.9180681052388965924, 0.000000000000000000 ) ) ;
#3705=AXIS2_PLACEMENT_3D ( 'NONE', #27574, #8870, #46293 ) ;
#3712=CARTESIAN_POINT ( 'NONE',  ( -17.42409385541299471, -14.80920654474435771, 49.52966884056655772 ) ) ;
#3715=CARTESIAN_POINT ( 'NONE',  ( -17.42409385541299471, -14.80920654474435594, 52.02966884056656482 ) ) ;
#3728=DIRECTION ( 'NONE',  ( -3.071710424422018668E-17, 6.404604876783312462E-16, 1.000000000000000000 ) ) ;
#3746=CARTESIAN_POINT ( 'NONE',  ( -12.82148049030644366, -13.86501071932494789, 52.02966884056656482 ) ) ;
#3753=EDGE_CURVE ( 'NONE', #19773, #8811, #47716, .T. ) ;
#3762=CARTESIAN_POINT ( 'NONE',  ( -14.23827708255551627, -10.77544123782542407, 49.52966884056655772 ) ) ;
#3817=ORIENTED_EDGE ( 'NONE', *, *, #35766, .T. ) ;
#3828=DIRECTION ( 'NONE',  ( 3.071710424422018668E-17, -6.404604876783312462E-16, -1.000000000000000000 ) ) ;
#3831=EDGE_CURVE ( 'NONE', #12002, #2683, #8426, .T. ) ;
#3843=LINE ( 'NONE', #18588, #13906 ) ;
#3844=AXIS2_PLACEMENT_3D ( 'NONE', #25632, #2978, #17989 ) ;
#3851=DIRECTION ( 'NONE',  ( -3.071710424422018668E-17, 6.404604876783312462E-16, 1.000000000000000000 ) ) ;
#3859=DIRECTION ( 'NONE',  ( -3.071710424422018668E-17, 6.404604876783312462E-16, 1.000000000000000000 ) ) ;
#3860=DIRECTION ( 'NONE',  ( -3.071710424422018668E-17, 6.404604876783312462E-16, 1.000000000000000000 ) ) ;
#3864=CIRCLE ( 'NONE', #37648, 1.999999999999999778 ) ;
#3871=CARTESIAN_POINT ( 'NONE',  ( -17.42409385541299471, -14.80920654474435594, 52.02966884056656482 ) ) ;
#3883=ORIENTED_EDGE ( 'NONE', *, *, #22351, .T. ) ;
#3894=AXIS2_PLACEMENT_3D ( 'NONE', #39149, #4954, #16728 ) ;
#3932=AXIS2_PLACEMENT_3D ( 'NONE', #22458, #10886, #25908 ) ;
#3941=DIRECTION ( 'NONE',  ( 0.9687793358424819923, -0.2479245821708678243, 0.000000000000000000 ) ) ;
#3942=CARTESIAN_POINT ( 'NONE',  ( -17.42409385541299471, -14.80920654474435771, 49.52966884056655772 ) ) ;
#3948=CARTESIAN_POINT ( 'NONE',  ( -16.75933984047804515, -20.01695097968237036, 49.52966884056656482 ) ) ;
#3953=CIRCLE ( 'NONE', #25952, 4.686499999999999666 ) ;
#3955=EDGE_CURVE ( 'NONE', #39108, #36314, #2563, .T. ) ;
#3967=CARTESIAN_POINT ( 'NONE',  ( -17.77658133828675702, -19.49442885748621990, 49.52966884056656482 ) ) ;
#4003=LINE ( 'NONE', #30840, #11372 ) ;
#4024=CARTESIAN_POINT ( 'NONE',  ( -21.95370832667365235, -13.56094844357179596, 52.02966884056656482 ) ) ;
#4027=VECTOR ( 'NONE', #41306, 1000.000000000000000 ) ;
#4038=FACE_OUTER_BOUND ( 'NONE', #2610, .T. ) ;
#4041=CARTESIAN_POINT ( 'NONE',  ( -21.32332200014554857, -12.20934075487643966, 49.52966884056655772 ) ) ;
#4048=EDGE_CURVE ( 'NONE', #30036, #14018, #22591, .T. ) ;
#4053=ORIENTED_EDGE ( 'NONE', *, *, #46462, .F. ) ;
#4062=DIRECTION ( 'NONE',  ( 3.071710424422018668E-17, -6.404604876783312462E-16, -1.000000000000000000 ) ) ;
#4068=AXIS2_PLACEMENT_3D ( 'NONE', #38487, #35277, #20029 ) ;
#4069=DIRECTION ( 'NONE',  ( -3.071710424422018668E-17, 6.404604876783312462E-16, 1.000000000000000000 ) ) ;
#4079=AXIS2_PLACEMENT_3D ( 'NONE', #4309, #857, #15608 ) ;
#4083=CIRCLE ( 'NONE', #45778, 2.000000000000000444 ) ;
#4090=VERTEX_POINT ( 'NONE', #45156 ) ;
#4094=CARTESIAN_POINT ( 'NONE',  ( -19.18086540149941399, -19.15397765319887569, 52.02966884056656482 ) ) ;
#4100=CARTESIAN_POINT ( 'NONE',  ( -19.83890857264518104, -18.82566669410956806, 49.52966884056656482 ) ) ;
#4104=DIRECTION ( 'NONE',  ( -3.071710424422018668E-17, 6.404604876783312462E-16, 1.000000000000000000 ) ) ;
#4108=EDGE_CURVE ( 'NONE', #9874, #48505, #21012, .T. ) ;
#4111=DIRECTION ( 'NONE',  ( -3.071710424422018668E-17, 6.404604876783312462E-16, 1.000000000000000000 ) ) ;
#4144=CARTESIAN_POINT ( 'NONE',  ( -15.00927913818083859, -10.79274639537912606, 52.02966884056656482 ) ) ;
#4146=CARTESIAN_POINT ( 'NONE',  ( -22.01964724813734620, -15.72799447708766962, 49.52966884056655772 ) ) ;
#4151=CARTESIAN_POINT ( 'NONE',  ( -14.24626305875727184, -11.36469298288595731, 49.52966884056655772 ) ) ;
#4189=VECTOR ( 'NONE', #3080, 1000.000000000000000 ) ;
#4192=ORIENTED_EDGE ( 'NONE', *, *, #45315, .F. ) ;
#4201=ORIENTED_EDGE ( 'NONE', *, *, #34363, .T. ) ;
#4208=ORIENTED_EDGE ( 'NONE', *, *, #22295, .T. ) ;
#4215=AXIS2_PLACEMENT_3D ( 'NONE', #30627, #11904, #23474 ) ;
#4225=CARTESIAN_POINT ( 'NONE',  ( -17.58219478024370730, -20.05682544264153933, 52.02966884056656482 ) ) ;
#4240=EDGE_CURVE ( 'NONE', #12698, #19689, #2918, .T. ) ;
#4253=DIRECTION ( 'NONE',  ( -3.071710424422018668E-17, 6.404604876783312462E-16, 1.000000000000000000 ) ) ;
#4254=AXIS2_PLACEMENT_3D ( 'NONE', #39696, #28617, #43647 ) ;
#4265=DIRECTION ( 'NONE',  ( 0.9687793358424821033, -0.2479245821708679909, 0.000000000000000000 ) ) ;
#4278=CARTESIAN_POINT ( 'NONE',  ( -17.42409385541299471, -14.80920654474435594, 52.02966884056656482 ) ) ;
#4281=CARTESIAN_POINT ( 'NONE',  ( -12.21634942047498384, -14.14445252980938683, 52.02966884056656482 ) ) ;
#4286=DIRECTION ( 'NONE',  ( -3.071710424422018668E-17, 6.404604876783312462E-16, 1.000000000000000000 ) ) ;
#4288=ORIENTED_EDGE ( 'NONE', *, *, #17444, .T. ) ;
#4289=DIRECTION ( 'NONE',  ( 0.9687793358424817702, -0.2479245821708686570, 0.000000000000000000 ) ) ;
#4299=EDGE_CURVE ( 'NONE', #6587, #15782, #32803, .T. ) ;
#4304=DIRECTION ( 'NONE',  ( -0.2189141945955536406, 0.9757441136919965397, 0.000000000000000000 ) ) ;
#4309=CARTESIAN_POINT ( 'NONE',  ( -17.42409385541299471, -14.80920654474435771, 49.52966884056655772 ) ) ;
#4314=VECTOR ( 'NONE', #4658, 1000.000000000000000 ) ;
#4325=CYLINDRICAL_SURFACE ( 'NONE', #37014, 4.686499999999997002 ) ;
#4347=VERTEX_POINT ( 'NONE', #36674 ) ;
#4359=ORIENTED_EDGE ( 'NONE', *, *, #43943, .F. ) ;
#4374=AXIS2_PLACEMENT_3D ( 'NONE', #7215, #65, #29860 ) ;
#4376=CARTESIAN_POINT ( 'NONE',  ( -16.15640231613377154, -10.29741749701175202, 52.02966884056656482 ) ) ;
#4383=ORIENTED_EDGE ( 'NONE', *, *, #30565, .T. ) ;
#4417=ORIENTED_EDGE ( 'NONE', *, *, #26961, .T. ) ;
#4423=ORIENTED_EDGE ( 'NONE', *, *, #28900, .T. ) ;
#4437=AXIS2_PLACEMENT_3D ( 'NONE', #41356, #22656, #28036 ) ;
#4438=ORIENTED_EDGE ( 'NONE', *, *, #25544, .F. ) ;
#4448=CYLINDRICAL_SURFACE ( 'NONE', #12479, 2.000000000000001776 ) ;
#4453=CARTESIAN_POINT ( 'NONE',  ( -20.49775566701509177, -11.27142682889164327, 52.02966884056656482 ) ) ;
#4454=CYLINDRICAL_SURFACE ( 'NONE', #12114, 5.249999999999998224 ) ;
#4459=ORIENTED_EDGE ( 'NONE', *, *, #44297, .F. ) ;
#4463=CARTESIAN_POINT ( 'NONE',  ( -20.63647318826268773, -18.96169002115701119, 49.52966884056656482 ) ) ;
#4478=ORIENTED_EDGE ( 'NONE', *, *, #29302, .F. ) ;
#4479=AXIS2_PLACEMENT_3D ( 'NONE', #47855, #24964, #6256 ) ;
#4485=AXIS2_PLACEMENT_3D ( 'NONE', #27264, #8557, #32417 ) ;
#4491=DIRECTION ( 'NONE',  ( 0.9687793358424821033, -0.2479245821708679909, 0.000000000000000000 ) ) ;
#4501=CARTESIAN_POINT ( 'NONE',  ( -20.43749099114212342, -18.39845715627588874, 49.52966884056656482 ) ) ;
#4502=ORIENTED_EDGE ( 'NONE', *, *, #7749, .T. ) ;
#4506=DIRECTION ( 'NONE',  ( -3.071710424422018668E-17, 6.404604876783312462E-16, 1.000000000000000000 ) ) ;
#4516=CYLINDRICAL_SURFACE ( 'NONE', #10192, 5.249999999999998224 ) ;
#4529=EDGE_CURVE ( 'NONE', #1590, #24111, #11576, .T. ) ;
#4533=ORIENTED_EDGE ( 'NONE', *, *, #30160, .F. ) ;
#4535=DIRECTION ( 'NONE',  ( -3.071710424422018668E-17, 6.404604876783312462E-16, 1.000000000000000000 ) ) ;
#4537=CIRCLE ( 'NONE', #31289, 2.000000000000002220 ) ;
#4544=ADVANCED_FACE ( 'NONE', ( #15984 ), #27086, .T. ) ;
#4546=CIRCLE ( 'NONE', #32084, 2.000000000000001332 ) ;
#4556=CARTESIAN_POINT ( 'NONE',  ( -13.02884944951828494, -13.18282747993466941, 49.52966884056655772 ) ) ;
#4563=CARTESIAN_POINT ( 'NONE',  ( -21.57657733182563931, -11.59682721189464871, 50.77966884056655772 ) ) ;
#4567=CYLINDRICAL_SURFACE ( 'NONE', #28957, 4.686499999999997002 ) ;
#4585=AXIS2_PLACEMENT_3D ( 'NONE', #22619, #7861, #11534 ) ;
#4619=DIRECTION ( 'NONE',  ( -3.071710424422018668E-17, 6.404604876783312462E-16, 1.000000000000000000 ) ) ;
#4625=CARTESIAN_POINT ( 'NONE',  ( -17.42409385541299471, -14.80920654474435771, 49.52966884056655772 ) ) ;
#4631=ORIENTED_EDGE ( 'NONE', *, *, #34946, .F. ) ;
#4658=DIRECTION ( 'NONE',  ( -3.071710424422018668E-17, 6.404604876783312462E-16, 1.000000000000000000 ) ) ;
#4661=DIRECTION ( 'NONE',  ( 0.9687793358424819923, -0.2479245821708678243, 0.000000000000000000 ) ) ;
#4686=VECTOR ( 'NONE', #45794, 1000.000000000000000 ) ;
#4688=CARTESIAN_POINT ( 'NONE',  ( -17.42409385541299471, -14.80920654474435771, 49.52966884056655772 ) ) ;
#4690=ORIENTED_EDGE ( 'NONE', *, *, #34712, .F. ) ;
#4697=DIRECTION ( 'NONE',  ( -3.071710424422018668E-17, 6.404604876783312462E-16, 1.000000000000000000 ) ) ;
#4705=ADVANCED_FACE ( 'NONE', ( #19096 ), #15625, .F. ) ;
#4715=FACE_OUTER_BOUND ( 'NONE', #37569, .T. ) ;
#4725=FACE_OUTER_BOUND ( 'NONE', #23559, .T. ) ;
#4726=AXIS2_PLACEMENT_3D ( 'NONE', #45386, #41688, #7724 ) ;
#4732=EDGE_LOOP ( 'NONE', ( #42030, #33199, #2012, #12171 ) ) ;
#4735=EDGE_CURVE ( 'NONE', #70, #34400, #3843, .T. ) ;
#4743=VERTEX_POINT ( 'NONE', #26973 ) ;
#4756=AXIS2_PLACEMENT_3D ( 'NONE', #22611, #44790, #25812 ) ;
#4757=AXIS2_PLACEMENT_3D ( 'NONE', #3712, #41631, #36679 ) ;
#4773=AXIS2_PLACEMENT_3D ( 'NONE', #1135, #38812, #24774 ) ;
#4792=CIRCLE ( 'NONE', #3219, 1.999999999999999112 ) ;
#4806=DIRECTION ( 'NONE',  ( 0.9687793358424821033, -0.2479245821708680464, 0.000000000000000000 ) ) ;
#4812=AXIS2_PLACEMENT_3D ( 'NONE', #41441, #48590, #40715 ) ;
#4821=CARTESIAN_POINT ( 'NONE',  ( -17.03658212107600534, -14.90837637761273449, 2.029618040566568027 ) ) ;
#4824=AXIS2_PLACEMENT_3D ( 'NONE', #44459, #18326, #17836 ) ;
#4826=CARTESIAN_POINT ( 'NONE',  ( -21.67055903134415473, -17.89628178023893668, 49.52966884056656482 ) ) ;
#4827=AXIS2_PLACEMENT_3D ( 'NONE', #47691, #47938, #10278 ) ;
#4835=DIRECTION ( 'NONE',  ( -3.071710424422018668E-17, 6.404604876783312462E-16, 1.000000000000000000 ) ) ;
#4841=ADVANCED_FACE ( 'NONE', ( #31879 ), #42730, .T. ) ;
#4844=AXIS2_PLACEMENT_3D ( 'NONE', #30854, #45865, #23452 ) ;
#4845=EDGE_CURVE ( 'NONE', #28161, #14388, #14672, .T. ) ;
#4859=ORIENTED_EDGE ( 'NONE', *, *, #1268, .F. ) ;
#4860=EDGE_CURVE ( 'NONE', #38039, #48382, #9998, .T. ) ;
#4876=AXIS2_PLACEMENT_3D ( 'NONE', #11695, #30668, #26960 ) ;
#4902=AXIS2_PLACEMENT_3D ( 'NONE', #599, #26216, #37270 ) ;
#4913=ORIENTED_EDGE ( 'NONE', *, *, #43854, .F. ) ;
#4933=CYLINDRICAL_SURFACE ( 'NONE', #45620, 1.999999999999999556 ) ;
#4934=EDGE_CURVE ( 'NONE', #29084, #10945, #28437, .T. ) ;
#4948=DIRECTION ( 'NONE',  ( -3.071710424422018668E-17, 6.404604876783312462E-16, 1.000000000000000000 ) ) ;
#4954=DIRECTION ( 'NONE',  ( -3.071710424422018668E-17, 6.404604876783312462E-16, 1.000000000000000000 ) ) ;
#4968=DIRECTION ( 'NONE',  ( -3.071710424422018668E-17, 6.404604876783312462E-16, 1.000000000000000000 ) ) ;
#4971=EDGE_CURVE ( 'NONE', #2683, #42051, #29396, .T. ) ;
#4986=CARTESIAN_POINT ( 'NONE',  ( -16.34301583228449317, -10.23680828416977739, 49.52966884056655772 ) ) ;
#5010=DIRECTION ( 'NONE',  ( -0.9687793358424821033, 0.2479245821708679909, 0.000000000000000000 ) ) ;
#5015=EDGE_CURVE ( 'NONE', #20388, #19733, #28907, .T. ) ;
#5030=CARTESIAN_POINT ( 'NONE',  ( -18.08884787034790875, -9.601462109806339740, 50.77966884056655772 ) ) ;
#5043=ORIENTED_EDGE ( 'NONE', *, *, #10709, .F. ) ;
#5046=ORIENTED_EDGE ( 'NONE', *, *, #24633, .T. ) ;
#5064=EDGE_LOOP ( 'NONE', ( #19498, #22237, #1721, #47699 ) ) ;
#5065=DIRECTION ( 'NONE',  ( -3.071710424422018668E-17, 6.404604876783312462E-16, 1.000000000000000000 ) ) ;
#5068=CARTESIAN_POINT ( 'NONE',  ( -22.60969001043771698, -13.98939405582217255, 50.77966884056655772 ) ) ;
#5087=CARTESIAN_POINT ( 'NONE',  ( -22.09321184435721719, -14.28490438881294367, 49.52966884056655772 ) ) ;
#5091=ORIENTED_EDGE ( 'NONE', *, *, #48551, .T. ) ;
#5110=EDGE_CURVE ( 'NONE', #15426, #6917, #99, .T. ) ;
#5118=EDGE_LOOP ( 'NONE', ( #9798, #41670, #35586, #18025 ) ) ;
#5124=CARTESIAN_POINT ( 'NONE',  ( -21.76243611580424897, -17.76577320756515022, 50.77966884056655772 ) ) ;
#5126=CIRCLE ( 'NONE', #37324, 5.249999999999998224 ) ;
#5127=DIRECTION ( 'NONE',  ( -3.071710424422018668E-17, 6.404604876783312462E-16, 1.000000000000000000 ) ) ;
#5138=ORIENTED_EDGE ( 'NONE', *, *, #5336, .F. ) ;
#5139=ORIENTED_EDGE ( 'NONE', *, *, #16358, .T. ) ;
#5150=VERTEX_POINT ( 'NONE', #30871 ) ;
#5153=CARTESIAN_POINT ( 'NONE',  ( -20.96187357126569850, -17.88286835634646721, 49.52966884056655772 ) ) ;
#5158=AXIS2_PLACEMENT_3D ( 'NONE', #3436, #36911, #32513 ) ;
#5159=ORIENTED_EDGE ( 'NONE', *, *, #20645, .T. ) ;
#5169=ADVANCED_FACE ( 'NONE', ( #20504 ), #46841, .T. ) ;
#5188=DIRECTION ( 'NONE',  ( 0.9687793358424821033, -0.2479245821708677133, 0.000000000000000000 ) ) ;
#5190=CIRCLE ( 'NONE', #26452, 5.249999999999998224 ) ;
#5195=ORIENTED_EDGE ( 'NONE', *, *, #40804, .T. ) ;
#5200=FACE_OUTER_BOUND ( 'NONE', #2859, .T. ) ;
#5209=CARTESIAN_POINT ( 'NONE',  ( -15.59410181515468530, -19.12364873146922051, 49.52966884056656482 ) ) ;
#5211=DIRECTION ( 'NONE',  ( 0.9687793358424822143, -0.2479245821708672415, 0.000000000000000000 ) ) ;
#5249=ORIENTED_EDGE ( 'NONE', *, *, #40239, .F. ) ;
#5266=EDGE_CURVE ( 'NONE', #32811, #12742, #6902, .T. ) ;
#5270=VECTOR ( 'NONE', #17881, 1000.000000000000000 ) ;
#5290=CIRCLE ( 'NONE', #11571, 1.999999999999999556 ) ;
#5291=AXIS2_PLACEMENT_3D ( 'NONE', #16464, #16215, #8866 ) ;
#5301=VERTEX_POINT ( 'NONE', #2971 ) ;
#5309=DIRECTION ( 'NONE',  ( -3.071710424422018668E-17, 6.404604876783312462E-16, 1.000000000000000000 ) ) ;
#5316=ORIENTED_EDGE ( 'NONE', *, *, #11805, .T. ) ;
#5322=ORIENTED_EDGE ( 'NONE', *, *, #29235, .T. ) ;
#5329=( GEOMETRIC_REPRESENTATION_CONTEXT ( 3 ) GLOBAL_UNCERTAINTY_ASSIGNED_CONTEXT ( ( #9070 ) ) GLOBAL_UNIT_ASSIGNED_CONTEXT ( ( #22723, #41915, #30847 ) ) REPRESENTATION_CONTEXT ( 'NONE', 'WORKASPACE' ) );
#5336=EDGE_CURVE ( 'NONE', #10683, #26257, #4546, .T. ) ;
#5338=DIRECTION ( 'NONE',  ( -0.9180681052388980357, 0.3964226963016364014, 0.000000000000000000 ) ) ;
#5339=AXIS2_PLACEMENT_3D ( 'NONE', #33672, #29514, #3411 ) ;
#5341=CIRCLE ( 'NONE', #621, 1.999999999999999556 ) ;
#5363=CARTESIAN_POINT ( 'NONE',  ( -15.80034074178659331, -19.80179363221599687, 49.52966884056656482 ) ) ;
#5366=LINE ( 'NONE', #5124, #18733 ) ;
#5384=LINE ( 'NONE', #24338, #13975 ) ;
#5399=AXIS2_PLACEMENT_3D ( 'NONE', #34988, #23201, #22966 ) ;
#5403=DIRECTION ( 'NONE',  ( -3.071710424422018668E-17, 6.404604876783312462E-16, 1.000000000000000000 ) ) ;
#5407=CIRCLE ( 'NONE', #15609, 2.000000000000001776 ) ;
#5409=ORIENTED_EDGE ( 'NONE', *, *, #35700, .T. ) ;
#5420=LINE ( 'NONE', #20441, #20327 ) ;
#5426=ORIENTED_EDGE ( 'NONE', *, *, #3472, .F. ) ;
#5436=CIRCLE ( 'NONE', #23507, 5.249999999999998224 ) ;
#5440=CARTESIAN_POINT ( 'NONE',  ( -17.42409385541299471, -14.80920654474435594, 52.02966884056656482 ) ) ;
#5441=CARTESIAN_POINT ( 'NONE',  ( -17.42409385541299471, -14.80920654474434883, 62.02966884056656482 ) ) ;
#5442=ORIENTED_EDGE ( 'NONE', *, *, #39587, .T. ) ;
#5444=DIRECTION ( 'NONE',  ( -3.071710424422018668E-17, 6.404604876783312462E-16, 1.000000000000000000 ) ) ;
#5447=DIRECTION ( 'NONE',  ( -3.071710424422018668E-17, 6.404604876783312462E-16, 1.000000000000000000 ) ) ;
#5451=DIRECTION ( 'NONE',  ( -3.071710424422018668E-17, 6.404604876783312462E-16, 1.000000000000000000 ) ) ;
#5459=FACE_OUTER_BOUND ( 'NONE', #2481, .T. ) ;
#5463=EDGE_CURVE ( 'NONE', #8478, #30371, #20276, .T. ) ;
#5465=CYLINDRICAL_SURFACE ( 'NONE', #28026, 4.686499999999997002 ) ;
#5467=DIRECTION ( 'NONE',  ( -0.9180681052388980357, 0.3964226963016366789, 0.000000000000000000 ) ) ;
#5469=ORIENTED_EDGE ( 'NONE', *, *, #40024, .F. ) ;
#5471=CIRCLE ( 'NONE', #40847, 2.000000000000001776 ) ;
#5483=DIRECTION ( 'NONE',  ( 0.9687793358424821033, -0.2479245821708677133, 0.000000000000000000 ) ) ;
#5489=APPLICATION_CONTEXT ( 'automotive_design' ) ;
#5491=EDGE_CURVE ( 'NONE', #42196, #38954, #26559, .T. ) ;
#5504=EDGE_LOOP ( 'NONE', ( #32077, #46966, #14256, #11104 ) ) ;
#5506=DIRECTION ( 'NONE',  ( 0.9687793358424819923, -0.2479245821708680464, 0.000000000000000000 ) ) ;
#5515=ORIENTED_EDGE ( 'NONE', *, *, #2181, .T. ) ;
#5538=VECTOR ( 'NONE', #26425, 1000.000000000000000 ) ;
#5542=EDGE_CURVE ( 'NONE', #13202, #1590, #21039, .T. ) ;
#5549=EDGE_CURVE ( 'NONE', #26266, #43656, #19405, .T. ) ;
#5553=ADVANCED_FACE ( 'NONE', ( #9065 ), #38845, .T. ) ;
#5556=CARTESIAN_POINT ( 'NONE',  ( -17.03658212107600534, -14.90837637761270429, 49.52966884056655772 ) ) ;
#5564=CARTESIAN_POINT ( 'NONE',  ( -21.39914427356725213, -17.29159580171669219, 49.52966884056655772 ) ) ;
#5567=DIRECTION ( 'NONE',  ( -3.071710424422018668E-17, 6.404604876783312462E-16, 1.000000000000000000 ) ) ;
#5580=CYLINDRICAL_SURFACE ( 'NONE', #30675, 5.249999999999998224 ) ;
#5587=DIRECTION ( 'NONE',  ( -3.071710424422018668E-17, 6.404604876783312462E-16, 1.000000000000000000 ) ) ;
#5588=AXIS2_PLACEMENT_3D ( 'NONE', #29671, #7282, #40276 ) ;
#5600=AXIS2_PLACEMENT_3D ( 'NONE', #36912, #29541, #10826 ) ;
#5616=EDGE_CURVE ( 'NONE', #38015, #35776, #34905, .T. ) ;
#5625=CIRCLE ( 'NONE', #4079, 4.686499999999999666 ) ;
#5641=CARTESIAN_POINT ( 'NONE',  ( -16.15640231613377154, -10.29741749701175380, 49.52966884056655772 ) ) ;
#5648=CARTESIAN_POINT ( 'NONE',  ( -17.42409385541299471, -14.80920654474435594, 52.02966884056656482 ) ) ;
#5651=DIRECTION ( 'NONE',  ( 0.9687793358424819923, -0.2479245821708680464, 0.000000000000000000 ) ) ;
#5657=EDGE_LOOP ( 'NONE', ( #7722, #2967, #2725, #12120 ) ) ;
#5697=DIRECTION ( 'NONE',  ( 0.9687793358424821033, -0.2479245821708677133, 0.000000000000000000 ) ) ;
#5706=ORIENTED_EDGE ( 'NONE', *, *, #12386, .F. ) ;
#5707=ORIENTED_EDGE ( 'NONE', *, *, #2290, .T. ) ;
#5731=FACE_OUTER_BOUND ( 'NONE', #5504, .T. ) ;
#5774=ADVANCED_FACE ( 'NONE', ( #22316 ), #14400, .T. ) ;
#5775=CYLINDRICAL_SURFACE ( 'NONE', #30051, 2.000000000000003109 ) ;
#5780=ORIENTED_EDGE ( 'NONE', *, *, #46869, .T. ) ;
#5782=EDGE_CURVE ( 'NONE', #26257, #23869, #33632, .T. ) ;
#5792=DIRECTION ( 'NONE',  ( -3.071710424422018668E-17, 6.404604876783312462E-16, 1.000000000000000000 ) ) ;
#5794=ORIENTED_EDGE ( 'NONE', *, *, #47178, .T. ) ;
#5796=CARTESIAN_POINT ( 'NONE',  ( -17.42409385541299471, -14.80920654474435594, 52.02966884056656482 ) ) ;
#5799=EDGE_CURVE ( 'NONE', #30955, #22574, #39954, .T. ) ;
#5819=ORIENTED_EDGE ( 'NONE', *, *, #6876, .T. ) ;
#5840=CARTESIAN_POINT ( 'NONE',  ( -20.59270190486383356, -18.27842527154038521, 49.52966884056656482 ) ) ;
#5842=CARTESIAN_POINT ( 'NONE',  ( -13.17588093101833557, -17.89387621085224822, 49.52966884056656482 ) ) ;
#5843=ORIENTED_EDGE ( 'NONE', *, *, #20324, .T. ) ;
#5845=DIRECTION ( 'NONE',  ( 3.071710424422018668E-17, -6.404604876783312462E-16, -1.000000000000000000 ) ) ;
#5860=AXIS2_PLACEMENT_3D ( 'NONE', #953, #42073, #15951 ) ;
#5899=DIRECTION ( 'NONE',  ( -3.071710424422018668E-17, 6.404604876783312462E-16, 1.000000000000000000 ) ) ;
#5913=CARTESIAN_POINT ( 'NONE',  ( -17.42409385541299471, -14.80920654474435771, 49.52966884056655772 ) ) ;
#5914=ORIENTED_EDGE ( 'NONE', *, *, #16358, .F. ) ;
#5932=ORIENTED_EDGE ( 'NONE', *, *, #42350, .T. ) ;
#5943=CARTESIAN_POINT ( 'NONE',  ( -17.42409385541299471, -14.80920654474435771, 49.52966884056655772 ) ) ;
#5953=VECTOR ( 'NONE', #8014, 1000.000000000000000 ) ;
#5961=DIRECTION ( 'NONE',  ( -0.5097212845717550289, 0.8603395911234820170, 0.000000000000000000 ) ) ;
#5972=ORIENTED_EDGE ( 'NONE', *, *, #20383, .T. ) ;
#5992=AXIS2_PLACEMENT_3D ( 'NONE', #20121, #30497, #38586 ) ;
#5994=AXIS2_PLACEMENT_3D ( 'NONE', #15546, #4253, #19262 ) ;
#5999=EDGE_CURVE ( 'NONE', #16677, #19285, #38387, .T. ) ;
#6005=EDGE_CURVE ( 'NONE', #35820, #17561, #36947, .T. ) ;
#6020=DIRECTION ( 'NONE',  ( 3.071710424422018668E-17, -6.404604876783312462E-16, -1.000000000000000000 ) ) ;
#6028=DIRECTION ( 'NONE',  ( 3.071710424422018668E-17, -6.404604876783312462E-16, -1.000000000000000000 ) ) ;
#6042=FACE_OUTER_BOUND ( 'NONE', #16859, .T. ) ;
#6046=EDGE_CURVE ( 'NONE', #10797, #43519, #32862, .T. ) ;
#6052=CIRCLE ( 'NONE', #33551, 2.000000000000001332 ) ;
#6071=VERTEX_POINT ( 'NONE', #29341 ) ;
#6083=CARTESIAN_POINT ( 'NONE',  ( -14.96223302779666398, -10.63593772014186101, 52.02966884056656482 ) ) ;
#6087=ADVANCED_FACE ( 'NONE', ( #48530 ), #29581, .T. ) ;
#6096=DIRECTION ( 'NONE',  ( 0.9687793358424821033, -0.2479245821708677133, 0.000000000000000000 ) ) ;
#6097=DIRECTION ( 'NONE',  ( 0.9687793358424804380, -0.2479245821708741804, 0.000000000000000000 ) ) ;
#6109=DIRECTION ( 'NONE',  ( 0.3688590060343583388, -0.9294853595766559007, 0.000000000000000000 ) ) ;
#6111=CARTESIAN_POINT ( 'NONE',  ( -12.43058792219793141, -16.43013174195301218, 49.52966884056655772 ) ) ;
#6118=LINE ( 'NONE', #2428, #31611 ) ;
#6121=AXIS2_PLACEMENT_3D ( 'NONE', #21531, #40466, #37237 ) ;
#6122=DIRECTION ( 'NONE',  ( -3.071710424422018668E-17, 6.404604876783312462E-16, 1.000000000000000000 ) ) ;
#6124=CIRCLE ( 'NONE', #11613, 4.686499999999997890 ) ;
#6134=DIRECTION ( 'NONE',  ( -3.071710424422018668E-17, 6.404604876783312462E-16, 1.000000000000000000 ) ) ;
#6146=ORIENTED_EDGE ( 'NONE', *, *, #41113, .F. ) ;
#6173=AXIS2_PLACEMENT_3D ( 'NONE', #39512, #9240, #13863 ) ;
#6184=EDGE_LOOP ( 'NONE', ( #38419, #5706, #45178, #34527 ) ) ;
#6192=AXIS2_PLACEMENT_3D ( 'NONE', #4986, #1266, #27141 ) ;
#6205=CARTESIAN_POINT ( 'NONE',  ( -14.82422806554511929, -10.90997840001177366, 52.02966884056656482 ) ) ;
#6213=DIRECTION ( 'NONE',  ( 0.3688590060343584498, -0.9294853595766556786, 0.000000000000000000 ) ) ;
#6216=VERTEX_POINT ( 'NONE', #42859 ) ;
#6222=DIRECTION ( 'NONE',  ( -3.071710424422018668E-17, 6.404604876783312462E-16, 1.000000000000000000 ) ) ;
#6233=ADVANCED_FACE ( 'NONE', ( #31529 ), #19963, .T. ) ;
#6235=CARTESIAN_POINT ( 'NONE',  ( -21.42170527289675164, -17.27794275993632667, 52.02966884056656482 ) ) ;
#6236=CARTESIAN_POINT ( 'NONE',  ( -12.17409406592225629, -14.80771982110106677, 52.02966884056656482 ) ) ;
#6237=CIRCLE ( 'NONE', #34545, 1.999999999999998446 ) ;
#6244=CIRCLE ( 'NONE', #33726, 4.686499999999998778 ) ;
#6256=DIRECTION ( 'NONE',  ( 0.9687793358424819923, -0.2479245821708678243, 0.000000000000000000 ) ) ;
#6269=DIRECTION ( 'NONE',  ( -3.071710424422018668E-17, 6.404604876783312462E-16, 1.000000000000000000 ) ) ;
#6272=CARTESIAN_POINT ( 'NONE',  ( -15.04196850781542771, -10.13074752191075234, 49.52966884056655772 ) ) ;
#6278=EDGE_LOOP ( 'NONE', ( #2688, #43633, #31732, #30855 ) ) ;
#6279=CARTESIAN_POINT ( 'NONE',  ( -17.42409385541299471, -14.80920654474435771, 49.52966884056655772 ) ) ;
#6280=CIRCLE ( 'NONE', #34591, 4.686499999999999666 ) ;
#6283=DIRECTION ( 'NONE',  ( 0.9687793358424822143, -0.2479245821708672415, 0.000000000000000000 ) ) ;
#6285=ORIENTED_EDGE ( 'NONE', *, *, #4971, .F. ) ;
#6295=VERTEX_POINT ( 'NONE', #16496 ) ;
#6303=CIRCLE ( 'NONE', #33806, 5.249999999999998224 ) ;
#6318=CYLINDRICAL_SURFACE ( 'NONE', #33101, 2.000000000000000000 ) ;
#6319=ORIENTED_EDGE ( 'NONE', *, *, #36631, .F. ) ;
#6320=DIRECTION ( 'NONE',  ( -0.7506333037770539507, 0.6607190350373940424, 0.000000000000000000 ) ) ;
#6336=DIRECTION ( 'NONE',  ( -3.071710424422018668E-17, 6.404604876783312462E-16, 1.000000000000000000 ) ) ;
#6337=VERTEX_POINT ( 'NONE', #20198 ) ;
#6380=DIRECTION ( 'NONE',  ( 0.9687793358424819923, -0.2479245821708676023, 0.000000000000000000 ) ) ;
#6396=DIRECTION ( 'NONE',  ( 0.9687793358424821033, -0.2479245821708679909, 0.000000000000000000 ) ) ;
#6405=CARTESIAN_POINT ( 'NONE',  ( -17.26599293058224305, -9.561587646847176103, 49.52966884056655772 ) ) ;
#6406=EDGE_CURVE ( 'NONE', #33723, #43487, #21114, .T. ) ;
#6415=CIRCLE ( 'NONE', #32366, 4.686499999999997002 ) ;
#6417=CARTESIAN_POINT ( 'NONE',  ( -17.42409385541299471, -14.80920654474434883, 62.02966884056656482 ) ) ;
#6419=ADVANCED_FACE ( 'NONE', ( #7597 ), #23334, .T. ) ;
#6422=ORIENTED_EDGE ( 'NONE', *, *, #42768, .F. ) ;
#6453=CARTESIAN_POINT ( 'NONE',  ( -13.16616306552584525, -16.76709000361798729, 49.52966884056655772 ) ) ;
#6459=CARTESIAN_POINT ( 'NONE',  ( -17.42409385541299471, -14.80920654474435771, 49.52966884056655772 ) ) ;
#6466=CARTESIAN_POINT ( 'NONE',  ( -13.27161037900033058, -18.02158587759403829, 52.02966884056656482 ) ) ;
#6468=EDGE_LOOP ( 'NONE', ( #44910, #38367, #1438, #38617 ) ) ;
#6484=CARTESIAN_POINT ( 'NONE',  ( -18.50517187854146783, -19.38160480531894692, 49.52966884056656482 ) ) ;
#6487=ADVANCED_FACE ( 'NONE', ( #15427 ), #41815, .T. ) ;
#6489=EDGE_LOOP ( 'NONE', ( #5469, #11006, #33117, #30223 ) ) ;
#6493=ADVANCED_FACE ( 'NONE', ( #17389 ), #40521, .T. ) ;
#6503=ORIENTED_EDGE ( 'NONE', *, *, #15362, .F. ) ;
#6509=DIRECTION ( 'NONE',  ( 0.9687793358424817702, -0.2479245821708686570, 0.000000000000000000 ) ) ;
#6529=ORIENTED_EDGE ( 'NONE', *, *, #41927, .F. ) ;
#6530=CARTESIAN_POINT ( 'NONE',  ( -17.42409385541299471, -14.80920654474435771, 49.52966884056655772 ) ) ;
#6531=VERTEX_POINT ( 'NONE', #17129 ) ;
#6533=EDGE_LOOP ( 'NONE', ( #40539, #26938, #25202, #33566 ) ) ;
#6553=ORIENTED_EDGE ( 'NONE', *, *, #22371, .F. ) ;
#6555=ORIENTED_EDGE ( 'NONE', *, *, #9154, .F. ) ;
#6560=EDGE_CURVE ( 'NONE', #18524, #44188, #29692, .T. ) ;
#6561=AXIS2_PLACEMENT_3D ( 'NONE', #27093, #37420, #18718 ) ;
#6576=DIRECTION ( 'NONE',  ( 0.9687793358424817702, -0.2479245821708688791, 0.000000000000000000 ) ) ;
#6583=DIRECTION ( 'NONE',  ( -3.071710424422018668E-17, 6.404604876783312462E-16, 1.000000000000000000 ) ) ;
#6587=VERTEX_POINT ( 'NONE', #41257 ) ;
#6594=FACE_OUTER_BOUND ( 'NONE', #1570, .T. ) ;
#6599=AXIS2_PLACEMENT_3D ( 'NONE', #30930, #42495, #26980 ) ;
#6606=ORIENTED_EDGE ( 'NONE', *, *, #41925, .F. ) ;
#6624=CARTESIAN_POINT ( 'NONE',  ( -17.42409385541299471, -14.80920654474435594, 52.02966884056656482 ) ) ;
#6628=VECTOR ( 'NONE', #39400, 1000.000000000000000 ) ;
#6630=ORIENTED_EDGE ( 'NONE', *, *, #22871, .T. ) ;
#6636=DIRECTION ( 'NONE',  ( -3.071710424422018668E-17, 6.404604876783312462E-16, 1.000000000000000000 ) ) ;
#6646=EDGE_CURVE ( 'NONE', #6817, #36333, #5407, .T. ) ;
#6653=DIRECTION ( 'NONE',  ( -0.9687793358424822143, 0.2479245821708672415, 0.000000000000000000 ) ) ;
#6678=ORIENTED_EDGE ( 'NONE', *, *, #5336, .T. ) ;
#6684=CYLINDRICAL_SURFACE ( 'NONE', #33144, 2.000000000000001776 ) ;
#6701=ORIENTED_EDGE ( 'NONE', *, *, #26798, .F. ) ;
#6722=ORIENTED_EDGE ( 'NONE', *, *, #35766, .F. ) ;
#6729=AXIS2_PLACEMENT_3D ( 'NONE', #17775, #29365, #32804 ) ;
#6747=CYLINDRICAL_SURFACE ( 'NONE', #31735, 4.686499999999997002 ) ;
#6751=ORIENTED_EDGE ( 'NONE', *, *, #9565, .F. ) ;
#6753=CARTESIAN_POINT ( 'NONE',  ( -14.36038767613011302, -18.37140530287405582, 49.52966884056656482 ) ) ;
#6769=ORIENTED_EDGE ( 'NONE', *, *, #11670, .T. ) ;
#6783=VERTEX_POINT ( 'NONE', #630 ) ;
#6785=EDGE_CURVE ( 'NONE', #40811, #48635, #11967, .T. ) ;
#6803=LINE ( 'NONE', #18859, #34437 ) ;
#6804=DIRECTION ( 'NONE',  ( 0.5351595679979623821, 0.8447509909909748371, 0.000000000000000000 ) ) ;
#6816=CARTESIAN_POINT ( 'NONE',  ( -17.42409385541299471, -14.80920654474435771, 49.52966884056655772 ) ) ;
#6817=VERTEX_POINT ( 'NONE', #39751 ) ;
#6819=EDGE_CURVE ( 'NONE', #3087, #16476, #9346, .T. ) ;
#6820=ADVANCED_FACE ( 'NONE', ( #32129 ), #9489, .T. ) ;
#6825=LINE ( 'NONE', #18374, #5270 ) ;
#6841=ORIENTED_EDGE ( 'NONE', *, *, #45027, .F. ) ;
#6855=EDGE_CURVE ( 'NONE', #12959, #27894, #19565, .T. ) ;
#6865=EDGE_LOOP ( 'NONE', ( #36834, #32445, #18625, #13590 ) ) ;
#6871=VECTOR ( 'NONE', #17068, 1000.000000000000000 ) ;
#6875=DIRECTION ( 'NONE',  ( -3.071710424422018668E-17, 6.404604876783312462E-16, 1.000000000000000000 ) ) ;
#6876=EDGE_CURVE ( 'NONE', #30431, #29199, #35567, .T. ) ;
#6877=CARTESIAN_POINT ( 'NONE',  ( -21.82233664355339542, -16.46178511230714037, 49.52966884056655772 ) ) ;
#6878=CARTESIAN_POINT ( 'NONE',  ( -17.42409385541299471, -14.80920654474435771, 49.52966884056655772 ) ) ;
#6879=ORIENTED_EDGE ( 'NONE', *, *, #5549, .T. ) ;
#6882=CARTESIAN_POINT ( 'NONE',  ( -15.80034074178659331, -19.80179363221599687, 50.77966884056656482 ) ) ;
#6891=ORIENTED_EDGE ( 'NONE', *, *, #23324, .F. ) ;
#6899=DIRECTION ( 'NONE',  ( -3.071710424422018668E-17, 6.404604876783312462E-16, 1.000000000000000000 ) ) ;
#6902=CIRCLE ( 'NONE', #18666, 1.999999999999999112 ) ;
#6903=ORIENTED_EDGE ( 'NONE', *, *, #9565, .T. ) ;
#6909=CARTESIAN_POINT ( 'NONE',  ( -21.73853604213786639, -16.63919858500264937, 49.52966884056655772 ) ) ;
#6917=VERTEX_POINT ( 'NONE', #35801 ) ;
#6921=CIRCLE ( 'NONE', #21094, 5.249999999999998224 ) ;
#6932=DIRECTION ( 'NONE',  ( -3.071710424422018668E-17, 6.404604876783312462E-16, 1.000000000000000000 ) ) ;
#6940=DIRECTION ( 'NONE',  ( -3.071710424422018668E-17, 6.404604876783312462E-16, 1.000000000000000000 ) ) ;
#6959=ADVANCED_FACE ( 'NONE', ( #4038 ), #7249, .T. ) ;
#6978=DIRECTION ( 'NONE',  ( -3.071710424422018668E-17, 6.404604876783312462E-16, 1.000000000000000000 ) ) ;
#6984=CYLINDRICAL_SURFACE ( 'NONE', #6121, 5.249999999999998224 ) ;
#6991=ORIENTED_EDGE ( 'NONE', *, *, #15656, .T. ) ;
#7009=AXIS2_PLACEMENT_3D ( 'NONE', #12401, #47830, #28407 ) ;
#7022=CARTESIAN_POINT ( 'NONE',  ( -12.17409406592225629, -14.80771982110106677, 50.77966884056655772 ) ) ;
#7079=AXIS2_PLACEMENT_3D ( 'NONE', #988, #27804, #1714 ) ;
#7093=DIRECTION ( 'NONE',  ( -0.5097212845717553620, 0.8603395911234816840, 0.000000000000000000 ) ) ;
#7102=DIRECTION ( 'NONE',  ( -3.071710424422018668E-17, 6.404604876783312462E-16, 1.000000000000000000 ) ) ;
#7104=ORIENTED_EDGE ( 'NONE', *, *, #24891, .F. ) ;
#7113=DIRECTION ( 'NONE',  ( -3.071710424422018668E-17, 6.404604876783312462E-16, 1.000000000000000000 ) ) ;
#7119=CYLINDRICAL_SURFACE ( 'NONE', #17133, 1.999999999999999556 ) ;
#7130=ORIENTED_EDGE ( 'NONE', *, *, #31131, .T. ) ;
#7148=DIRECTION ( 'NONE',  ( -3.071710424422018668E-17, 6.404604876783312462E-16, 1.000000000000000000 ) ) ;
#7149=DIRECTION ( 'NONE',  ( 3.071710424422018668E-17, -6.404604876783312462E-16, -1.000000000000000000 ) ) ;
#7164=EDGE_CURVE ( 'NONE', #37281, #44219, #1285, .T. ) ;
#7167=VERTEX_POINT ( 'NONE', #43889 ) ;
#7184=CIRCLE ( 'NONE', #34695, 1.999999999999999112 ) ;
#7186=CARTESIAN_POINT ( 'NONE',  ( -14.33942418930512019, -10.56099362034968614, 50.77966884056655772 ) ) ;
#7215=CARTESIAN_POINT ( 'NONE',  ( -17.42409385541299471, -14.80920654474435771, 49.52966884056655772 ) ) ;
#7225=EDGE_LOOP ( 'NONE', ( #44234, #33031, #9235, #41281 ) ) ;
#7230=CARTESIAN_POINT ( 'NONE',  ( -17.42409385541299471, -14.80920654474435594, 52.02966884056656482 ) ) ;
#7234=CIRCLE ( 'NONE', #34744, 5.249999999999998224 ) ;
#7248=EDGE_CURVE ( 'NONE', #39514, #4743, #43978, .T. ) ;
#7249=CYLINDRICAL_SURFACE ( 'NONE', #38426, 1.999999999999999112 ) ;
#7258=ORIENTED_EDGE ( 'NONE', *, *, #19448, .T. ) ;
#7282=DIRECTION ( 'NONE',  ( -3.071710424422018668E-17, 6.404604876783312462E-16, 1.000000000000000000 ) ) ;
#7286=CARTESIAN_POINT ( 'NONE',  ( -17.42409385541299471, -14.80920654474435771, 49.52966884056655772 ) ) ;
#7288=CARTESIAN_POINT ( 'NONE',  ( -17.42409385541299471, -14.80920654474434883, 62.02966884056656482 ) ) ;
#7317=CARTESIAN_POINT ( 'NONE',  ( -17.80887632446114921, -10.12652590253629903, 49.52966884056655772 ) ) ;
#7320=ORIENTED_EDGE ( 'NONE', *, *, #2131, .F. ) ;
#7328=EDGE_CURVE ( 'NONE', #19164, #20160, #29828, .T. ) ;
#7333=CARTESIAN_POINT ( 'NONE',  ( -18.40115675053315059, -19.96748611248585448, 49.52966884056656482 ) ) ;
#7338=LINE ( 'NONE', #45253, #21255 ) ;
#7346=VERTEX_POINT ( 'NONE', #41145 ) ;
#7354=LINE ( 'NONE', #40818, #2433 ) ;
#7366=ORIENTED_EDGE ( 'NONE', *, *, #38391, .F. ) ;
#7370=DIRECTION ( 'NONE',  ( 0.9956360040033425118, -0.09332174201254556101, 0.000000000000000000 ) ) ;
#7381=EDGE_CURVE ( 'NONE', #18890, #5301, #40897, .T. ) ;
#7383=CIRCLE ( 'NONE', #4215, 5.249999999999998224 ) ;
#7385=ORIENTED_EDGE ( 'NONE', *, *, #40033, .F. ) ;
#7387=DIRECTION ( 'NONE',  ( -0.8447509909909771686, 0.5351595679979589404, 0.000000000000000000 ) ) ;
#7395=ORIENTED_EDGE ( 'NONE', *, *, #30851, .T. ) ;
#7409=ADVANCED_FACE ( 'NONE', ( #46733 ), #46246, .T. ) ;
#7410=CIRCLE ( 'NONE', #27821, 1.999999999999999556 ) ;
#7436=CARTESIAN_POINT ( 'NONE',  ( -12.85799447202792045, -15.86467737382985632, 49.52966884056655772 ) ) ;
#7441=CARTESIAN_POINT ( 'NONE',  ( -17.42409385541299471, -14.80920654474435594, 52.02966884056656482 ) ) ;
#7460=EDGE_CURVE ( 'NONE', #3087, #36239, #42564, .T. ) ;
#7462=EDGE_CURVE ( 'NONE', #19053, #36634, #10953, .T. ) ;
#7471=VERTEX_POINT ( 'NONE', #28003 ) ;
#7475=DIRECTION ( 'NONE',  ( -3.071710424422018668E-17, 6.404604876783312462E-16, 1.000000000000000000 ) ) ;
#7497=DIRECTION ( 'NONE',  ( -3.071710424422018668E-17, 6.404604876783312462E-16, 1.000000000000000000 ) ) ;
#7501=EDGE_CURVE ( 'NONE', #8065, #7167, #27525, .T. ) ;
#7507=CYLINDRICAL_SURFACE ( 'NONE', #30574, 4.686499999999997002 ) ;
#7523=CIRCLE ( 'NONE', #35017, 4.686499999999999666 ) ;
#7529=DIRECTION ( 'NONE',  ( 0.9687793358424821033, -0.2479245821708680464, 0.000000000000000000 ) ) ;
#7530=CARTESIAN_POINT ( 'NONE',  ( -21.67230677980763431, -11.72453687863643701, 49.52966884056655772 ) ) ;
#7531=ORIENTED_EDGE ( 'NONE', *, *, #39587, .F. ) ;
#7532=DIRECTION ( 'NONE',  ( -0.9687793358424819923, 0.2479245821708680464, 0.000000000000000000 ) ) ;
#7536=CARTESIAN_POINT ( 'NONE',  ( -16.29155950929526497, -19.35680461458998636, 49.52966884056656482 ) ) ;
#7574=CARTESIAN_POINT ( 'NONE',  ( -14.82422806554511929, -10.90997840001177721, 49.52966884056655772 ) ) ;
#7575=CYLINDRICAL_SURFACE ( 'NONE', #8254, 1.999999999999999112 ) ;
#7596=ORIENTED_EDGE ( 'NONE', *, *, #36521, .F. ) ;
#7597=FACE_OUTER_BOUND ( 'NONE', #22535, .T. ) ;
#7605=CARTESIAN_POINT ( 'NONE',  ( -14.41069671968389265, -11.21995593321280360, 49.52966884056655772 ) ) ;
#7614=ORIENTED_EDGE ( 'NONE', *, *, #8323, .F. ) ;
#7639=CARTESIAN_POINT ( 'NONE',  ( -21.95370832667365235, -13.56094844357179774, 49.52966884056655772 ) ) ;
#7649=CARTESIAN_POINT ( 'NONE',  ( -22.67409364490373491, -14.81069326838761135, 49.52966884056655772 ) ) ;
#7690=ORIENTED_EDGE ( 'NONE', *, *, #36544, .T. ) ;
#7697=FACE_OUTER_BOUND ( 'NONE', #41283, .T. ) ;
#7716=ADVANCED_FACE ( 'NONE', ( #41517 ), #22562, .T. ) ;
#7720=AXIS2_PLACEMENT_3D ( 'NONE', #19329, #26969, #20065 ) ;
#7722=ORIENTED_EDGE ( 'NONE', *, *, #30365, .F. ) ;
#7724=DIRECTION ( 'NONE',  ( 0.9687793358424821033, -0.2479245821708679909, 0.000000000000000000 ) ) ;
#7725=VECTOR ( 'NONE', #12920, 1000.000000000000000 ) ;
#7736=AXIS2_PLACEMENT_3D ( 'NONE', #39941, #28853, #6213 ) ;
#7739=CARTESIAN_POINT ( 'NONE',  ( -17.61266704711333375, -10.12650194148654137, 49.52966884056655772 ) ) ;
#7743=AXIS2_PLACEMENT_3D ( 'NONE', #20881, #28517, #6096 ) ;
#7749=EDGE_CURVE ( 'NONE', #35637, #19053, #21941, .T. ) ;
#7761=ORIENTED_EDGE ( 'NONE', *, *, #36544, .F. ) ;
#7764=VECTOR ( 'NONE', #22510, 1000.000000000000000 ) ;
#7766=CARTESIAN_POINT ( 'NONE',  ( -17.42409385541299471, -14.80920654474435594, 52.02966884056656482 ) ) ;
#7801=CIRCLE ( 'NONE', #45552, 4.686499999999998778 ) ;
#7806=CARTESIAN_POINT ( 'NONE',  ( -17.42409385541299471, -14.80920654474435594, 52.02966884056656482 ) ) ;
#7813=CARTESIAN_POINT ( 'NONE',  ( -19.20714268997449281, -19.15619313305651161, 52.02966884056656482 ) ) ;
#7818=ORIENTED_EDGE ( 'NONE', *, *, #29388, .T. ) ;
#7839=EDGE_LOOP ( 'NONE', ( #27489, #23449, #2237, #42795 ) ) ;
#7847=DIRECTION ( 'NONE',  ( -3.071710424422018668E-17, 6.404604876783312462E-16, 1.000000000000000000 ) ) ;
#7848=EDGE_CURVE ( 'NONE', #45644, #39290, #1353, .T. ) ;
#7850=CYLINDRICAL_SURFACE ( 'NONE', #11615, 5.249999999999998224 ) ;
#7854=ORIENTED_EDGE ( 'NONE', *, *, #46240, .F. ) ;
#7857=CARTESIAN_POINT ( 'NONE',  ( -17.26599293058224305, -9.561587646847172550, 52.02966884056656482 ) ) ;
#7861=DIRECTION ( 'NONE',  ( -3.071710424422018668E-17, 6.404604876783312462E-16, 1.000000000000000000 ) ) ;
#7868=DIRECTION ( 'NONE',  ( 0.2189141945955470625, -0.9757441136919982050, 0.000000000000000000 ) ) ;
#7876=CARTESIAN_POINT ( 'NONE',  ( -21.01334446694451685, -11.79580940901521835, 49.52966884056655772 ) ) ;
#7897=DIRECTION ( 'NONE',  ( -3.071710424422018668E-17, 6.404604876783312462E-16, 1.000000000000000000 ) ) ;
#7898=AXIS2_PLACEMENT_3D ( 'NONE', #30135, #10676, #22002 ) ;
#7901=CIRCLE ( 'NONE', #11043, 2.000000000000001332 ) ;
#7904=DIRECTION ( 'NONE',  ( -0.6607190350374019250, -0.7506333037770469563, 0.000000000000000000 ) ) ;
#7908=AXIS2_PLACEMENT_3D ( 'NONE', #41080, #7113, #41315 ) ;
#7918=CARTESIAN_POINT ( 'NONE',  ( -17.42409385541299471, -14.80920654474435594, 52.02966884056656482 ) ) ;
#7922=EDGE_CURVE ( 'NONE', #23869, #30431, #3864, .T. ) ;
#7923=DIRECTION ( 'NONE',  ( -3.071710424422018668E-17, 6.404604876783312462E-16, 1.000000000000000000 ) ) ;
#7928=FACE_OUTER_BOUND ( 'NONE', #16263, .T. ) ;
#7944=DIRECTION ( 'NONE',  ( -3.071710424422018668E-17, 6.404604876783312462E-16, 1.000000000000000000 ) ) ;
#7945=AXIS2_PLACEMENT_3D ( 'NONE', #2836, #2609, #47435 ) ;
#7949=DIRECTION ( 'NONE',  ( -3.071710424422018668E-17, 6.404604876783312462E-16, 1.000000000000000000 ) ) ;
#7954=DIRECTION ( 'NONE',  ( 0.3964226963016397320, 0.9180681052388968144, 0.000000000000000000 ) ) ;
#7971=DIRECTION ( 'NONE',  ( -0.6607190350374019250, -0.7506333037770469563, 0.000000000000000000 ) ) ;
#7976=VERTEX_POINT ( 'NONE', #31892 ) ;
#7980=CARTESIAN_POINT ( 'NONE',  ( -14.82422806554511929, -10.90997840001177721, 49.52966884056655772 ) ) ;
#7990=CARTESIAN_POINT ( 'NONE',  ( -17.42409385541299471, -14.80920654474435771, 49.52966884056655772 ) ) ;
#7995=CIRCLE ( 'NONE', #4812, 1.999999999999999778 ) ;
#7996=ORIENTED_EDGE ( 'NONE', *, *, #32974, .F. ) ;
#7999=EDGE_LOOP ( 'NONE', ( #11041, #7366, #48156, #45765 ) ) ;
#8014=DIRECTION ( 'NONE',  ( 3.071710424422018668E-17, -6.404604876783312462E-16, -1.000000000000000000 ) ) ;
#8022=AXIS2_PLACEMENT_3D ( 'NONE', #35899, #40569, #43806 ) ;
#8036=ORIENTED_EDGE ( 'NONE', *, *, #43236, .T. ) ;
#8042=VECTOR ( 'NONE', #10955, 1000.000000000000000 ) ;
#8046=DIRECTION ( 'NONE',  ( -3.071710424422018668E-17, 6.404604876783312462E-16, 1.000000000000000000 ) ) ;
#8058=ORIENTED_EDGE ( 'NONE', *, *, #28708, .T. ) ;
#8059=CARTESIAN_POINT ( 'NONE',  ( -13.75179125342063458, -11.87837916245159953, 49.52966884056655772 ) ) ;
#8065=VERTEX_POINT ( 'NONE', #28454 ) ;
#8076=ORIENTED_EDGE ( 'NONE', *, *, #11038, .T. ) ;
#8087=CARTESIAN_POINT ( 'NONE',  ( -17.75227477277866939, -19.48420168222599713, 52.02966884056656482 ) ) ;
#8103=CARTESIAN_POINT ( 'NONE',  ( -19.86520892150080897, -18.82374422416847537, 49.52966884056656482 ) ) ;
#8113=DIRECTION ( 'NONE',  ( -3.071710424422018668E-17, 6.404604876783312462E-16, 1.000000000000000000 ) ) ;
#8114=EDGE_CURVE ( 'NONE', #40490, #241, #22766, .T. ) ;
#8116=ORIENTED_EDGE ( 'NONE', *, *, #5616, .T. ) ;
#8123=CARTESIAN_POINT ( 'NONE',  ( -15.66732230932660741, -10.46443543628982553, 49.52966884056655772 ) ) ;
#8135=ORIENTED_EDGE ( 'NONE', *, *, #21193, .T. ) ;
#8151=VERTEX_POINT ( 'NONE', #45410 ) ;
#8164=ORIENTED_EDGE ( 'NONE', *, *, #27077, .T. ) ;
#8167=CARTESIAN_POINT ( 'NONE',  ( -21.34628024798174550, -12.22231469401973847, 49.52966884056655772 ) ) ;
#8190=EDGE_CURVE ( 'NONE', #32458, #47056, #35029, .T. ) ;
#8208=EDGE_CURVE ( 'NONE', #1942, #1265, #47163, .T. ) ;
#8213=ADVANCED_FACE ( 'NONE', ( #23014 ), #4516, .T. ) ;
#8224=AXIS2_PLACEMENT_3D ( 'NONE', #21058, #46919, #20819 ) ;
#8250=CARTESIAN_POINT ( 'NONE',  ( -16.89979169948162863, -10.14008855580012458, 52.02966884056656482 ) ) ;
#8254=AXIS2_PLACEMENT_3D ( 'NONE', #22582, #19367, #38071 ) ;
#8261=EDGE_CURVE ( 'NONE', #38822, #8715, #30881, .T. ) ;
#8290=ORIENTED_EDGE ( 'NONE', *, *, #29668, .F. ) ;
#8299=LINE ( 'NONE', #11013, #35365 ) ;
#8323=EDGE_CURVE ( 'NONE', #33825, #31312, #24700, .T. ) ;
#8328=FACE_OUTER_BOUND ( 'NONE', #10494, .T. ) ;
#8337=DIRECTION ( 'NONE',  ( 0.9687793358424821033, -0.2479245821708677133, 0.000000000000000000 ) ) ;
#8338=ORIENTED_EDGE ( 'NONE', *, *, #29806, .F. ) ;
#8345=EDGE_CURVE ( 'NONE', #7976, #19337, #8641, .T. ) ;
#8356=ORIENTED_EDGE ( 'NONE', *, *, #35666, .T. ) ;
#8357=VERTEX_POINT ( 'NONE', #6466 ) ;
#8358=DIRECTION ( 'NONE',  ( -3.071710424422018668E-17, 6.404604876783312462E-16, 1.000000000000000000 ) ) ;
#8363=ORIENTED_EDGE ( 'NONE', *, *, #30565, .F. ) ;
#8369=CARTESIAN_POINT ( 'NONE',  ( -12.88390949798720619, -15.97110509908812936, 52.02966884056656482 ) ) ;
#8371=EDGE_CURVE ( 'NONE', #43656, #38294, #47921, .T. ) ;
#8377=CIRCLE ( 'NONE', #48440, 4.686499999999999666 ) ;
#8378=VECTOR ( 'NONE', #5403, 1000.000000000000000 ) ;
#8412=CARTESIAN_POINT ( 'NONE',  ( -13.44904343725875684, -12.32681728777199481, 49.52966884056655772 ) ) ;
#8426=CIRCLE ( 'NONE', #34383, 1.999999999999999556 ) ;
#8438=CARTESIAN_POINT ( 'NONE',  ( -17.42409385541299471, -14.80920654474435771, 49.52966884056655772 ) ) ;
#8439=CARTESIAN_POINT ( 'NONE',  ( -12.43150676794136089, -13.18545343111793855, 50.77966884056655772 ) ) ;
#8450=AXIS2_PLACEMENT_3D ( 'NONE', #47730, #21636, #39859 ) ;
#8460=CARTESIAN_POINT ( 'NONE',  ( -17.42409385541299471, -14.80920654474435594, 52.02966884056656482 ) ) ;
#8465=EDGE_CURVE ( 'NONE', #15068, #40396, #44816, .T. ) ;
#8476=CARTESIAN_POINT ( 'NONE',  ( -18.24390634433515856, -19.99480269976908176, 49.52966884056656482 ) ) ;
#8478=VERTEX_POINT ( 'NONE', #44380 ) ;
#8481=DIRECTION ( 'NONE',  ( -3.071710424422018668E-17, 6.404604876783312462E-16, 1.000000000000000000 ) ) ;
#8488=CARTESIAN_POINT ( 'NONE',  ( -17.42409385541299471, -14.80920654474435771, 49.52966884056655772 ) ) ;
#8496=CARTESIAN_POINT ( 'NONE',  ( -17.42409385541299471, -14.80920654474435771, 49.52966884056655772 ) ) ;
#8502=CARTESIAN_POINT ( 'NONE',  ( -14.95535764022100977, -18.80681796222810576, 49.52966884056656482 ) ) ;
#8504=CARTESIAN_POINT ( 'NONE',  ( -17.58219478024370730, -20.05682544264153933, 50.77966884056656482 ) ) ;
#8516=ORIENTED_EDGE ( 'NONE', *, *, #18582, .F. ) ;
#8529=VERTEX_POINT ( 'NONE', #15517 ) ;
#8546=DIRECTION ( 'NONE',  ( -0.9687793358424819923, 0.2479245821708680464, 0.000000000000000000 ) ) ;
#8554=VECTOR ( 'NONE', #16024, 1000.000000000000000 ) ;
#8556=ORIENTED_EDGE ( 'NONE', *, *, #46016, .T. ) ;
#8557=DIRECTION ( 'NONE',  ( -3.071710424422018668E-17, 6.404604876783312462E-16, 1.000000000000000000 ) ) ;
#8562=CARTESIAN_POINT ( 'NONE',  ( -20.60192465206874246, -18.25372010660273148, 52.02966884056656482 ) ) ;
#8568=CARTESIAN_POINT ( 'NONE',  ( -14.95535764022100977, -18.80681796222810576, 49.52966884056656482 ) ) ;
#8578=CARTESIAN_POINT ( 'NONE',  ( -22.10120296142702045, -17.19398125327358073, 50.77966884056655772 ) ) ;
#8580=ORIENTED_EDGE ( 'NONE', *, *, #23244, .F. ) ;
#8598=CARTESIAN_POINT ( 'NONE',  ( -17.42409385541299471, -14.80920654474435594, 52.02966884056656482 ) ) ;
#8617=EDGE_CURVE ( 'NONE', #15782, #43774, #1521, .T. ) ;
#8625=CARTESIAN_POINT ( 'NONE',  ( -12.74138925215518015, -14.62063335304397427, 49.52966884056655772 ) ) ;
#8626=EDGE_CURVE ( 'NONE', #11402, #28884, #32501, .T. ) ;
#8641=CIRCLE ( 'NONE', #19636, 1.999999999999999334 ) ;
#8642=DIRECTION ( 'NONE',  ( -0.9687793358424819923, 0.2479245821708680464, 0.000000000000000000 ) ) ;
#8662=DIRECTION ( 'NONE',  ( -3.071710424422018668E-17, 6.404604876783312462E-16, 1.000000000000000000 ) ) ;
#8672=ORIENTED_EDGE ( 'NONE', *, *, #217, .F. ) ;
#8673=ORIENTED_EDGE ( 'NONE', *, *, #15396, .F. ) ;
#8682=EDGE_CURVE ( 'NONE', #48460, #15180, #44092, .T. ) ;
#8697=DIRECTION ( 'NONE',  ( 0.7506333037770491767, -0.6607190350373993715, 0.000000000000000000 ) ) ;
#8700=DIRECTION ( 'NONE',  ( -3.071710424422018668E-17, 6.404604876783312462E-16, 1.000000000000000000 ) ) ;
#8715=VERTEX_POINT ( 'NONE', #17939 ) ;
#8728=ORIENTED_EDGE ( 'NONE', *, *, #1361, .F. ) ;
#8733=CARTESIAN_POINT ( 'NONE',  ( -17.42409385541299471, -14.80920654474435594, 52.02966884056656482 ) ) ;
#8742=CARTESIAN_POINT ( 'NONE',  ( -22.01964724813734620, -15.72799447708766607, 52.02966884056656482 ) ) ;
#8748=DIRECTION ( 'NONE',  ( -3.071710424422018668E-17, 6.404604876783312462E-16, 1.000000000000000000 ) ) ;
#8750=CIRCLE ( 'NONE', #29975, 4.686499999999998778 ) ;
#8758=CYLINDRICAL_SURFACE ( 'NONE', #12411, 5.249999999999998224 ) ;
#8771=VECTOR ( 'NONE', #42344, 1000.000000000000000 ) ;
#8775=EDGE_LOOP ( 'NONE', ( #26304, #9937, #24320, #18513 ) ) ;
#8783=DIRECTION ( 'NONE',  ( -0.7506333037770542838, 0.6607190350373937093, 0.000000000000000000 ) ) ;
#8796=VERTEX_POINT ( 'NONE', #45543 ) ;
#8805=ADVANCED_FACE ( 'NONE', ( #30768 ), #16191, .T. ) ;
#8806=VECTOR ( 'NONE', #25554, 1000.000000000000000 ) ;
#8810=EDGE_CURVE ( 'NONE', #43519, #9620, #15955, .T. ) ;
#8811=VERTEX_POINT ( 'NONE', #34425 ) ;
#8817=CIRCLE ( 'NONE', #36309, 4.686499999999998778 ) ;
#8818=DIRECTION ( 'NONE',  ( -0.5351595679979685993, -0.8447509909909710624, 0.000000000000000000 ) ) ;
#8830=CARTESIAN_POINT ( 'NONE',  ( -14.90085577400961014, -10.20532018813695707, 49.52966884056655772 ) ) ;
#8833=CARTESIAN_POINT ( 'NONE',  ( -17.42409385541299471, -14.80920654474435771, 49.52966884056655772 ) ) ;
#8834=ORIENTED_EDGE ( 'NONE', *, *, #10716, .T. ) ;
#8843=CIRCLE ( 'NONE', #4902, 0.3999999999999978018 ) ;
#8854=CARTESIAN_POINT ( 'NONE',  ( -13.27161037900033058, -18.02158587759403829, 50.77966884056655772 ) ) ;
#8859=VERTEX_POINT ( 'NONE', #37632 ) ;
#8862=CARTESIAN_POINT ( 'NONE',  ( -18.08884787034790875, -9.601462109806339740, 52.02966884056656482 ) ) ;
#8866=DIRECTION ( 'NONE',  ( 0.09332174201254196666, 0.9956360040033428449, 0.000000000000000000 ) ) ;
#8870=DIRECTION ( 'NONE',  ( -3.071710424422018668E-17, 6.404604876783312462E-16, 1.000000000000000000 ) ) ;
#8871=ORIENTED_EDGE ( 'NONE', *, *, #1506, .T. ) ;
#8880=EDGE_CURVE ( 'NONE', #20471, #18227, #3141, .T. ) ;
#8911=CYLINDRICAL_SURFACE ( 'NONE', #29537, 5.249999999999998224 ) ;
#8913=ORIENTED_EDGE ( 'NONE', *, *, #40227, .T. ) ;
#8925=CIRCLE ( 'NONE', #12840, 4.686499999999997890 ) ;
#8953=VERTEX_POINT ( 'NONE', #39098 ) ;
#8955=DIRECTION ( 'NONE',  ( -0.9979768094191907579, -0.06357898915123130767, 0.000000000000000000 ) ) ;
#8966=EDGE_CURVE ( 'NONE', #12002, #36239, #6280, .T. ) ;
#8996=AXIS2_PLACEMENT_3D ( 'NONE', #16436, #43036, #9315 ) ;
#9002=CARTESIAN_POINT ( 'NONE',  ( -15.66732230932660741, -10.46443543628982376, 52.02966884056656482 ) ) ;
#9016=DIRECTION ( 'NONE',  ( -3.071710424422018668E-17, 6.404604876783312462E-16, 1.000000000000000000 ) ) ;
#9036=VECTOR ( 'NONE', #39639, 1000.000000000000000 ) ;
#9062=ORIENTED_EDGE ( 'NONE', *, *, #26391, .F. ) ;
#9065=FACE_OUTER_BOUND ( 'NONE', #1608, .T. ) ;
#9070=UNCERTAINTY_MEASURE_WITH_UNIT (LENGTH_MEASURE( 1.000000000000000082E-05 ), #22723, 'distance_accuracy_value', 'NONE');
#9080=ORIENTED_EDGE ( 'NONE', *, *, #22857, .F. ) ;
#9097=VECTOR ( 'NONE', #7148, 1000.000000000000000 ) ;
#9100=CARTESIAN_POINT ( 'NONE',  ( -19.83890857264518104, -18.82566669410956806, 49.52966884056656482 ) ) ;
#9104=ORIENTED_EDGE ( 'NONE', *, *, #20383, .F. ) ;
#9106=FACE_OUTER_BOUND ( 'NONE', #22524, .T. ) ;
#9114=VERTEX_POINT ( 'NONE', #842 ) ;
#9115=CARTESIAN_POINT ( 'NONE',  ( -22.67171275331017810, -14.65110561991362381, 52.02966884056656482 ) ) ;
#9117=ORIENTED_EDGE ( 'NONE', *, *, #35700, .F. ) ;
#9125=CARTESIAN_POINT ( 'NONE',  ( -19.04501905262167227, -19.80271247795941392, 50.77966884056656482 ) ) ;
#9137=ORIENTED_EDGE ( 'NONE', *, *, #9324, .T. ) ;
#9139=CARTESIAN_POINT ( 'NONE',  ( -19.74436319619195501, -10.72363366794506234, 52.02966884056656482 ) ) ;
#9148=EDGE_CURVE ( 'NONE', #20159, #13083, #12164, .T. ) ;
#9154=EDGE_CURVE ( 'NONE', #14388, #42196, #39718, .T. ) ;
#9173=DIRECTION ( 'NONE',  ( -3.071710424422018668E-17, 6.404604876783312462E-16, 1.000000000000000000 ) ) ;
#9178=EDGE_CURVE ( 'NONE', #31757, #23869, #28404, .T. ) ;
#9204=DIRECTION ( 'NONE',  ( -3.071710424422018668E-17, 6.404604876783312462E-16, 1.000000000000000000 ) ) ;
#9212=CARTESIAN_POINT ( 'NONE',  ( -20.49775566701509177, -11.27142682889164327, 49.52966884056655772 ) ) ;
#9219=DIRECTION ( 'NONE',  ( -0.8603395911234869020, -0.5097212845717464802, 0.000000000000000000 ) ) ;
#9231=AXIS2_PLACEMENT_3D ( 'NONE', #17001, #12607, #35005 ) ;
#9235=ORIENTED_EDGE ( 'NONE', *, *, #33556, .F. ) ;
#9236=CARTESIAN_POINT ( 'NONE',  ( -12.38445583493520630, -13.33796604008351494, 50.77966884056655772 ) ) ;
#9240=DIRECTION ( 'NONE',  ( -3.071710424422018668E-17, 6.404604876783312462E-16, 1.000000000000000000 ) ) ;
#9248=LINE ( 'NONE', #5564, #31834 ) ;
#9253=CARTESIAN_POINT ( 'NONE',  ( -20.89331258220900978, -11.64059849529350643, 49.52966884056655772 ) ) ;
#9261=DIRECTION ( 'NONE',  ( 0.9687793358424821033, -0.2479245821708680464, 0.000000000000000000 ) ) ;
#9265=AXIS2_PLACEMENT_3D ( 'NONE', #31041, #42120, #34957 ) ;
#9266=ORIENTED_EDGE ( 'NONE', *, *, #46458, .F. ) ;
#9272=VECTOR ( 'NONE', #44429, 1000.000000000000000 ) ;
#9296=ORIENTED_EDGE ( 'NONE', *, *, #35401, .T. ) ;
#9304=CARTESIAN_POINT ( 'NONE',  ( -17.42409385541299471, -14.80920654474435771, 49.52966884056655772 ) ) ;
#9315=DIRECTION ( 'NONE',  ( 0.7700094066334510767, 0.6380325334150294125, 0.000000000000000000 ) ) ;
#9324=EDGE_CURVE ( 'NONE', #14637, #16885, #27542, .T. ) ;
#9328=CARTESIAN_POINT ( 'NONE',  ( -17.42409385541299471, -14.80920654474435771, 49.52966884056655772 ) ) ;
#9334=CIRCLE ( 'NONE', #24270, 2.000000000000001332 ) ;
#9337=DIRECTION ( 'NONE',  ( 0.9687793358424821033, -0.2479245821708677133, 0.000000000000000000 ) ) ;
#9341=LINE ( 'NONE', #9824, #8378 ) ;
#9346=CIRCLE ( 'NONE', #41567, 2.000000000000000444 ) ;
#9358=VERTEX_POINT ( 'NONE', #40672 ) ;
#9364=AXIS2_PLACEMENT_3D ( 'NONE', #1963, #28063, #13034 ) ;
#9380=ORIENTED_EDGE ( 'NONE', *, *, #21156, .F. ) ;
#9391=CYLINDRICAL_SURFACE ( 'NONE', #43432, 5.249999999999998224 ) ;
#9393=ORIENTED_EDGE ( 'NONE', *, *, #26062, .F. ) ;
#9399=VECTOR ( 'NONE', #16309, 1000.000000000000000 ) ;
#9407=ORIENTED_EDGE ( 'NONE', *, *, #40432, .F. ) ;
#9414=ORIENTED_EDGE ( 'NONE', *, *, #42422, .T. ) ;
#9417=CARTESIAN_POINT ( 'NONE',  ( -17.42409385541299471, -14.80920654474434883, 62.02966884056656482 ) ) ;
#9426=DIRECTION ( 'NONE',  ( -3.071710424422018668E-17, 6.404604876783312462E-16, 1.000000000000000000 ) ) ;
#9439=CARTESIAN_POINT ( 'NONE',  ( -22.02670722051955465, -15.75340237016373202, 52.02966884056656482 ) ) ;
#9450=CARTESIAN_POINT ( 'NONE',  ( -16.56761320685650318, -19.87745396966068157, 52.02966884056656482 ) ) ;
#9459=CARTESIAN_POINT ( 'NONE',  ( -21.82233664355339542, -16.46178511230714037, 49.52966884056655772 ) ) ;
#9473=CIRCLE ( 'NONE', #4756, 2.000000000000000888 ) ;
#9489=CYLINDRICAL_SURFACE ( 'NONE', #34492, 5.249999999999998224 ) ;
#9493=CYLINDRICAL_SURFACE ( 'NONE', #19510, 4.686499999999997002 ) ;
#9496=CARTESIAN_POINT ( 'NONE',  ( -18.55662820153069248, -10.26160847489872374, 49.52966884056655772 ) ) ;
#9498=EDGE_CURVE ( 'NONE', #15459, #8859, #25092, .T. ) ;
#9499=DIRECTION ( 'NONE',  ( 0.06357898915123501304, -0.9979768094191904249, 0.000000000000000000 ) ) ;
#9501=CLOSED_SHELL ( 'NONE', ( #4705, #45294, #39550, #40874, #47027, #1206, #22024, #6233, #21624, #3610, #20114, #25033, #5169, #31215, #30850, #38442, #48572, #44056, #40644, #35283, #19024, #24014, #38093, #11064, #39206, #11174, #23756, #5553, #6487, #2156, #20729, #489, #34395, #836, #23556, #38157, #2172, #48543, #4544, #23617, #36992, #26353, #6820, #24965, #30064, #11215, #17555, #8213, #2557, #17240, #25758, #27743, #15194, #41695, #5774, #45691, #38020, #26583, #39855, #41872, #19012, #23144, #3539, #46010, #26601, #360, #30014, #35373, #17328, #37130, #30969, #27214, #12344, #26261, #6493, #2363, #46162, #37110, #6087, #7716, #17578, #47055, #33457, #29511, #25537, #26242, #30909, #908, #33541, #46594, #46724, #12004, #45768, #19789, #6959, #21125, #10246, #31272, #409, #12044, #8805, #40164, #36421, #15931, #45764, #36145, #45723, #35958, #889, #42006, #25972, #43811, #38638, #758, #14289, #703, #33584, #1500, #33808, #41731, #29097, #28097, #11268, #1576, #48688, #31077, #46592, #13285, #21990, #37406, #14457, #24885, #29732, #16543, #24696, #29734, #48183, #36222, #24012, #12997, #12203, #14615, #15045, #7409, #43178, #21464, #30474, #46531, #22720, #17012, #36322, #358, #35302, #12204, #20103, #40507, #4841, #24959, #159, #6419, #42998, #16585, #30157, #16893, #31069, #9983, #29769, #27132, #40214 ) ) ;
#9504=DIRECTION ( 'NONE',  ( 0.9687793358424821033, -0.2479245821708679909, 0.000000000000000000 ) ) ;
#9514=CARTESIAN_POINT ( 'NONE',  ( -16.50530592306966682, -19.40475993746870387, 49.52966884056656482 ) ) ;
#9516=CYLINDRICAL_SURFACE ( 'NONE', #4773, 2.000000000000001332 ) ;
#9523=DIRECTION ( 'NONE',  ( 3.071710424422018668E-17, -6.404604876783312462E-16, -1.000000000000000000 ) ) ;
#9530=CIRCLE ( 'NONE', #46472, 2.000000000000000888 ) ;
#9546=VECTOR ( 'NONE', #3280, 1000.000000000000000 ) ;
#9549=DIRECTION ( 'NONE',  ( -3.071710424422018668E-17, 6.404604876783312462E-16, 1.000000000000000000 ) ) ;
#9559=CIRCLE ( 'NONE', #31548, 5.249999999999998224 ) ;
#9565=EDGE_CURVE ( 'NONE', #34714, #6531, #44051, .T. ) ;
#9567=CIRCLE ( 'NONE', #48074, 4.686499999999999666 ) ;
#9571=DIRECTION ( 'NONE',  ( -0.9956360040033418457, 0.09332174201255234725, 0.000000000000000000 ) ) ;
#9578=DIRECTION ( 'NONE',  ( -0.9294853595766571219, -0.3688590060343552857, 0.000000000000000000 ) ) ;
#9581=ORIENTED_EDGE ( 'NONE', *, *, #35320, .T. ) ;
#9587=CARTESIAN_POINT ( 'NONE',  ( -22.10255287824656989, -12.42708119714673742, 49.52966884056655772 ) ) ;
#9589=LINE ( 'NONE', #24605, #29561 ) ;
#9596=CIRCLE ( 'NONE', #37077, 5.249999999999998224 ) ;
#9600=CARTESIAN_POINT ( 'NONE',  ( -16.60428136649079534, -9.623610389719635450, 49.52966884056655772 ) ) ;
#9620=VERTEX_POINT ( 'NONE', #15198 ) ;
#9624=DIRECTION ( 'NONE',  ( -0.9687793358424821033, 0.2479245821708679631, -1.885439946533205044E-16 ) ) ;
#9625=DIRECTION ( 'NONE',  ( -3.071710424422018668E-17, 6.404604876783312462E-16, 1.000000000000000000 ) ) ;
#9628=EDGE_CURVE ( 'NONE', #40811, #20751, #36204, .T. ) ;
#9644=FACE_OUTER_BOUND ( 'NONE', #39418, .T. ) ;
#9645=EDGE_CURVE ( 'NONE', #33881, #13202, #15434, .T. ) ;
#9654=DIRECTION ( 'NONE',  ( -3.071710424422018668E-17, 6.404604876783312462E-16, 1.000000000000000000 ) ) ;
#9657=CARTESIAN_POINT ( 'NONE',  ( -17.42409385541299471, -14.80920654474435771, 49.52966884056655772 ) ) ;
#9670=CARTESIAN_POINT ( 'NONE',  ( -17.42409385541299471, -14.80920654474435771, 49.52966884056655772 ) ) ;
#9675=ORIENTED_EDGE ( 'NONE', *, *, #12666, .F. ) ;
#9676=DIRECTION ( 'NONE',  ( -3.071710424422018668E-17, 6.404604876783312462E-16, 1.000000000000000000 ) ) ;
#9683=EDGE_CURVE ( 'NONE', #1168, #8065, #31478, .T. ) ;
#9688=CYLINDRICAL_SURFACE ( 'NONE', #30641, 1.999999999999999112 ) ;
#9707=ORIENTED_EDGE ( 'NONE', *, *, #35231, .T. ) ;
#9711=CIRCLE ( 'NONE', #30126, 4.686499999999997890 ) ;
#9716=ORIENTED_EDGE ( 'NONE', *, *, #45811, .F. ) ;
#9726=CARTESIAN_POINT ( 'NONE',  ( -17.07160637253920044, -10.12398423200249731, 49.52966884056655772 ) ) ;
#9730=ORIENTED_EDGE ( 'NONE', *, *, #675, .T. ) ;
#9752=CARTESIAN_POINT ( 'NONE',  ( -21.93588290314558265, -13.54151500546508657, 49.52966884056655772 ) ) ;
#9779=EDGE_LOOP ( 'NONE', ( #11544, #3134, #18778, #36394 ) ) ;
#9798=ORIENTED_EDGE ( 'NONE', *, *, #217, .T. ) ;
#9802=CIRCLE ( 'NONE', #5860, 4.686499999999997002 ) ;
#9821=ORIENTED_EDGE ( 'NONE', *, *, #5491, .F. ) ;
#9822=EDGE_CURVE ( 'NONE', #45300, #32600, #18138, .T. ) ;
#9824=CARTESIAN_POINT ( 'NONE',  ( -21.10164091802717223, -17.71419016815049119, 49.52966884056655772 ) ) ;
#9866=ORIENTED_EDGE ( 'NONE', *, *, #10446, .T. ) ;
#9868=CIRCLE ( 'NONE', #20763, 2.000000000000001332 ) ;
#9869=CARTESIAN_POINT ( 'NONE',  ( -16.47989802999360265, -19.41181990985090877, 52.02966884056656482 ) ) ;
#9874=VERTEX_POINT ( 'NONE', #23315 ) ;
#9911=CARTESIAN_POINT ( 'NONE',  ( -17.42409385541299471, -14.80920654474435594, 52.02966884056656482 ) ) ;
#9914=DIRECTION ( 'NONE',  ( -3.071710424422018668E-17, 6.404604876783312462E-16, 1.000000000000000000 ) ) ;
#9919=FACE_OUTER_BOUND ( 'NONE', #6489, .T. ) ;
#9922=ORIENTED_EDGE ( 'NONE', *, *, #37266, .F. ) ;
#9931=DIRECTION ( 'NONE',  ( 0.9757441136919974278, 0.2189141945955503377, 0.000000000000000000 ) ) ;
#9937=ORIENTED_EDGE ( 'NONE', *, *, #45297, .F. ) ;
#9942=CARTESIAN_POINT ( 'NONE',  ( -17.42409385541299471, -14.80920654474435594, 52.02966884056656482 ) ) ;
#9955=CARTESIAN_POINT ( 'NONE',  ( -12.23896285002386719, -13.98645721660588315, 49.52966884056655772 ) ) ;
#9966=FACE_OUTER_BOUND ( 'NONE', #41028, .T. ) ;
#9967=CARTESIAN_POINT ( 'NONE',  ( -20.38066051823377478, -10.47086428435309102, 52.02966884056656482 ) ) ;
#9982=DIRECTION ( 'NONE',  ( -3.071710424422018668E-17, 6.404604876783312462E-16, 1.000000000000000000 ) ) ;
#9983=ADVANCED_FACE ( 'NONE', ( #6042 ), #9516, .T. ) ;
#9996=CARTESIAN_POINT ( 'NONE',  ( -13.50190746284422794, -17.39609839546894321, 52.02966884056656482 ) ) ;
#9998=CIRCLE ( 'NONE', #44588, 1.999999999999999112 ) ;
#10000=DIRECTION ( 'NONE',  ( -3.071710424422018668E-17, 6.404604876783312462E-16, 1.000000000000000000 ) ) ;
#10040=CARTESIAN_POINT ( 'NONE',  ( -17.42409385541299471, -14.80920654474435771, 49.52966884056655772 ) ) ;
#10051=DIRECTION ( 'NONE',  ( 0.9687793358424822143, -0.2479245821708672415, 0.000000000000000000 ) ) ;
#10084=CARTESIAN_POINT ( 'NONE',  ( -20.35492123770571382, -11.13690394275196560, 49.52966884056655772 ) ) ;
#10105=CIRCLE ( 'NONE', #44733, 2.000000000000000000 ) ;
#10107=VERTEX_POINT ( 'NONE', #10238 ) ;
#10108=EDGE_CURVE ( 'NONE', #48382, #19712, #25253, .T. ) ;
#10110=AXIS2_PLACEMENT_3D ( 'NONE', #37859, #37598, #19640 ) ;
#10116=FACE_OUTER_BOUND ( 'NONE', #38031, .T. ) ;
#10126=AXIS2_PLACEMENT_3D ( 'NONE', #14416, #32682, #44038 ) ;
#10138=DIRECTION ( 'NONE',  ( 0.9687793358424821033, -0.2479245821708680464, 0.000000000000000000 ) ) ;
#10149=CARTESIAN_POINT ( 'NONE',  ( -17.42409385541299471, -14.80920654474435594, 52.02966884056656482 ) ) ;
#10153=ORIENTED_EDGE ( 'NONE', *, *, #3073, .F. ) ;
#10156=FACE_OUTER_BOUND ( 'NONE', #28841, .T. ) ;
#10159=DIRECTION ( 'NONE',  ( -3.071710424422018668E-17, 6.404604876783312462E-16, 1.000000000000000000 ) ) ;
#10185=AXIS2_PLACEMENT_3D ( 'NONE', #18239, #6932, #2742 ) ;
#10192=AXIS2_PLACEMENT_3D ( 'NONE', #46377, #31598, #31346 ) ;
#10199=ORIENTED_EDGE ( 'NONE', *, *, #44149, .T. ) ;
#10205=FACE_OUTER_BOUND ( 'NONE', #40440, .T. ) ;
#10208=DIRECTION ( 'NONE',  ( 3.071710424422018668E-17, -6.404604876783312462E-16, -1.000000000000000000 ) ) ;
#10212=DIRECTION ( 'NONE',  ( -3.071710424422018668E-17, 6.404604876783312462E-16, 1.000000000000000000 ) ) ;
#10232=ORIENTED_EDGE ( 'NONE', *, *, #3275, .F. ) ;
#10234=EDGE_CURVE ( 'NONE', #29199, #30767, #43299, .T. ) ;
#10238=CARTESIAN_POINT ( 'NONE',  ( -18.47956468449850931, -19.37530592812942842, 49.52966884056656482 ) ) ;
#10245=CIRCLE ( 'NONE', #4757, 5.249999999999998224 ) ;
#10246=ADVANCED_FACE ( 'NONE', ( #12653 ), #42463, .T. ) ;
#10248=VECTOR ( 'NONE', #27303, 1000.000000000000000 ) ;
#10253=ORIENTED_EDGE ( 'NONE', *, *, #12071, .F. ) ;
#10256=DIRECTION ( 'NONE',  ( 0.9687793358424819923, -0.2479245821708680464, 0.000000000000000000 ) ) ;
#10265=DIRECTION ( 'NONE',  ( 0.9687793358424817702, -0.2479245821708688791, 0.000000000000000000 ) ) ;
#10267=DIRECTION ( 'NONE',  ( -3.071710424422018668E-17, 6.404604876783312462E-16, 1.000000000000000000 ) ) ;
#10273=ORIENTED_EDGE ( 'NONE', *, *, #32771, .F. ) ;
#10278=DIRECTION ( 'NONE',  ( -0.3688590060343657218, 0.9294853595766530141, 0.000000000000000000 ) ) ;
#10279=DIRECTION ( 'NONE',  ( -3.071710424422018668E-17, 6.404604876783312462E-16, 1.000000000000000000 ) ) ;
#10281=AXIS2_PLACEMENT_3D ( 'NONE', #45406, #23241, #41949 ) ;
#10287=DIRECTION ( 'NONE',  ( 0.9687793358424804380, -0.2479245821708739583, 0.000000000000000000 ) ) ;
#10311=CARTESIAN_POINT ( 'NONE',  ( -19.04501905262167227, -19.80271247795941392, 49.52966884056656482 ) ) ;
#10315=VECTOR ( 'NONE', #20784, 1000.000000000000000 ) ;
#10320=DIRECTION ( 'NONE',  ( -3.071710424422018668E-17, 6.404604876783312462E-16, 1.000000000000000000 ) ) ;
#10330=DIRECTION ( 'NONE',  ( -3.071710424422018668E-17, 6.404604876783312462E-16, 1.000000000000000000 ) ) ;
#10333=VERTEX_POINT ( 'NONE', #16326 ) ;
#10340=CARTESIAN_POINT ( 'NONE',  ( -17.97037870217379307, -19.46375863019785513, 49.52966884056656482 ) ) ;
#10351=DIRECTION ( 'NONE',  ( -0.3688590060343657773, 0.9294853595766529031, 0.000000000000000000 ) ) ;
#10364=VERTEX_POINT ( 'NONE', #9212 ) ;
#10374=CARTESIAN_POINT ( 'NONE',  ( -19.05047292022263505, -10.41396213884962840, 49.52966884056655772 ) ) ;
#10406=CARTESIAN_POINT ( 'NONE',  ( -22.67409364490373491, -14.81069326838761135, 52.02966884056656482 ) ) ;
#10407=VERTEX_POINT ( 'NONE', #47837 ) ;
#10418=CARTESIAN_POINT ( 'NONE',  ( -12.23896285002386719, -13.98645721660588137, 50.77966884056655772 ) ) ;
#10419=VERTEX_POINT ( 'NONE', #29368 ) ;
#10446=EDGE_CURVE ( 'NONE', #13430, #42667, #33850, .T. ) ;
#10465=CYLINDRICAL_SURFACE ( 'NONE', #18982, 4.686499999999997002 ) ;
#10469=ORIENTED_EDGE ( 'NONE', *, *, #8345, .F. ) ;
#10494=EDGE_LOOP ( 'NONE', ( #35247, #18373, #44585, #24044 ) ) ;
#10506=DIRECTION ( 'NONE',  ( 0.9687793358424822143, -0.2479245821708672415, 0.000000000000000000 ) ) ;
#10536=VECTOR ( 'NONE', #46671, 1000.000000000000000 ) ;
#10537=LINE ( 'NONE', #21853, #16548 ) ;
#10545=DIRECTION ( 'NONE',  ( -0.9687793358424817702, 0.2479245821708684905, 0.000000000000000000 ) ) ;
#10548=LINE ( 'NONE', #40105, #18125 ) ;
#10561=CARTESIAN_POINT ( 'NONE',  ( -21.67055903134415473, -17.89628178023893668, 52.02966884056656482 ) ) ;
#10565=AXIS2_PLACEMENT_3D ( 'NONE', #46739, #12511, #12983 ) ;
#10573=DIRECTION ( 'NONE',  ( -3.071710424422018668E-17, 6.404604876783312462E-16, 1.000000000000000000 ) ) ;
#10586=FACE_OUTER_BOUND ( 'NONE', #29128, .T. ) ;
#10611=ORIENTED_EDGE ( 'NONE', *, *, #22229, .T. ) ;
#10615=ORIENTED_EDGE ( 'NONE', *, *, #37342, .F. ) ;
#10624=LINE ( 'NONE', #14042, #40806 ) ;
#10629=AXIS2_PLACEMENT_3D ( 'NONE', #37952, #34011, #37705 ) ;
#10630=DIRECTION ( 'NONE',  ( 0.9687793358424821033, -0.2479245821708677133, 0.000000000000000000 ) ) ;
#10633=AXIS2_PLACEMENT_3D ( 'NONE', #48728, #22633, #14467 ) ;
#10639=CARTESIAN_POINT ( 'NONE',  ( -17.42409385541299471, -14.80920654474434883, 62.02966884056656482 ) ) ;
#10653=CARTESIAN_POINT ( 'NONE',  ( -13.95487512861695834, -17.97781459419518058, 49.52966884056656482 ) ) ;
#10676=DIRECTION ( 'NONE',  ( -3.071710424422018052E-17, 6.404604876783311476E-16, 1.000000000000000000 ) ) ;
#10681=DIRECTION ( 'NONE',  ( 0.9687793358424822143, -0.2479245821708672415, 0.000000000000000000 ) ) ;
#10683=VERTEX_POINT ( 'NONE', #29736 ) ;
#10684=FACE_OUTER_BOUND ( 'NONE', #31747, .T. ) ;
#10689=CARTESIAN_POINT ( 'NONE',  ( -19.18086540149941399, -19.15397765319887569, 49.52966884056656482 ) ) ;
#10708=ORIENTED_EDGE ( 'NONE', *, *, #46458, .T. ) ;
#10709=EDGE_CURVE ( 'NONE', #19712, #31360, #18962, .T. ) ;
#10716=EDGE_CURVE ( 'NONE', #28899, #15973, #25224, .T. ) ;
#10722=VECTOR ( 'NONE', #19933, 1000.000000000000000 ) ;
#10783=EDGE_LOOP ( 'NONE', ( #47186, #2513, #25542, #47138 ) ) ;
#10797=VERTEX_POINT ( 'NONE', #34872 ) ;
#10800=ORIENTED_EDGE ( 'NONE', *, *, #34879, .T. ) ;
#10812=ORIENTED_EDGE ( 'NONE', *, *, #35252, .F. ) ;
#10826=DIRECTION ( 'NONE',  ( 0.9687793358424821033, -0.2479245821708679909, 0.000000000000000000 ) ) ;
#10835=LINE ( 'NONE', #45319, #20560 ) ;
#10836=AXIS2_PLACEMENT_3D ( 'NONE', #32942, #37369, #18663 ) ;
#10848=ORIENTED_EDGE ( 'NONE', *, *, #4240, .T. ) ;
#10856=DIRECTION ( 'NONE',  ( -3.071710424422018668E-17, 6.404604876783312462E-16, 1.000000000000000000 ) ) ;
#10862=VERTEX_POINT ( 'NONE', #38569 ) ;
#10872=ORIENTED_EDGE ( 'NONE', *, *, #15998, .T. ) ;
#10886=DIRECTION ( 'NONE',  ( -3.071710424422018668E-17, 6.404604876783312462E-16, 1.000000000000000000 ) ) ;
#10905=CARTESIAN_POINT ( 'NONE',  ( -18.24684318355141599, -9.624075539355217757, 52.02966884056656482 ) ) ;
#10906=EDGE_CURVE ( 'NONE', #1509, #18890, #11088, .T. ) ;
#10918=CARTESIAN_POINT ( 'NONE',  ( -17.42409385541299471, -14.80920654474435771, 49.52966884056655772 ) ) ;
#10928=DIRECTION ( 'NONE',  ( -3.071710424422018668E-17, 6.404604876783312462E-16, 1.000000000000000000 ) ) ;
#10931=DIRECTION ( 'NONE',  ( -3.071710424422018668E-17, 6.404604876783312462E-16, 1.000000000000000000 ) ) ;
#10937=AXIS2_PLACEMENT_3D ( 'NONE', #23608, #47218, #28507 ) ;
#10943=CARTESIAN_POINT ( 'NONE',  ( -17.42409385541299471, -14.80920654474435771, 49.52966884056655772 ) ) ;
#10945=VERTEX_POINT ( 'NONE', #31427 ) ;
#10947=AXIS2_PLACEMENT_3D ( 'NONE', #29582, #25890, #40903 ) ;
#10951=ORIENTED_EDGE ( 'NONE', *, *, #34392, .F. ) ;
#10953=CIRCLE ( 'NONE', #38460, 5.249999999999998224 ) ;
#10955=DIRECTION ( 'NONE',  ( -3.071710424422018668E-17, 6.404604876783312462E-16, 1.000000000000000000 ) ) ;
#10962=FACE_OUTER_BOUND ( 'NONE', #34263, .T. ) ;
#10967=CIRCLE ( 'NONE', #38483, 2.000000000000002665 ) ;
#10973=EDGE_CURVE ( 'NONE', #45300, #10364, #8750, .T. ) ;
#10974=VERTEX_POINT ( 'NONE', #12718 ) ;
#10978=DIRECTION ( 'NONE',  ( -3.071710424422018668E-17, 6.404604876783312462E-16, 1.000000000000000000 ) ) ;
#10982=AXIS2_PLACEMENT_3D ( 'NONE', #24151, #5444, #28572 ) ;
#11005=EDGE_CURVE ( 'NONE', #35282, #19390, #12945, .T. ) ;
#11006=ORIENTED_EDGE ( 'NONE', *, *, #22044, .F. ) ;
#11013=CARTESIAN_POINT ( 'NONE',  ( -13.74654679279883851, -11.90422292133819582, 49.52966884056655772 ) ) ;
#11016=AXIS2_PLACEMENT_3D ( 'NONE', #5087, #16634, #27964 ) ;
#11026=ORIENTED_EDGE ( 'NONE', *, *, #16294, .T. ) ;
#11029=EDGE_LOOP ( 'NONE', ( #2892, #37068, #35031, #28582 ) ) ;
#11036=CARTESIAN_POINT ( 'NONE',  ( -17.77658133828675702, -19.49442885748621990, 52.02966884056656482 ) ) ;
#11038=EDGE_CURVE ( 'NONE', #28383, #17957, #33897, .T. ) ;
#11041=ORIENTED_EDGE ( 'NONE', *, *, #42366, .F. ) ;
#11043=AXIS2_PLACEMENT_3D ( 'NONE', #31736, #40805, #21388 ) ;
#11057=AXIS2_PLACEMENT_3D ( 'NONE', #30415, #369, #4304 ) ;
#11058=EDGE_CURVE ( 'NONE', #19923, #20471, #29189, .T. ) ;
#11064=ADVANCED_FACE ( 'NONE', ( #10962 ), #21567, .T. ) ;
#11077=CARTESIAN_POINT ( 'NONE',  ( -12.75497586646876691, -15.33350870067573979, 49.52966884056655772 ) ) ;
#11082=ORIENTED_EDGE ( 'NONE', *, *, #8465, .F. ) ;
#11085=LINE ( 'NONE', #37154, #2459 ) ;
#11088=CIRCLE ( 'NONE', #38609, 1.999999999999999556 ) ;
#11090=VERTEX_POINT ( 'NONE', #48625 ) ;
#11104=ORIENTED_EDGE ( 'NONE', *, *, #26391, .T. ) ;
#11119=CYLINDRICAL_SURFACE ( 'NONE', #45586, 2.000000000000001776 ) ;
#11129=CYLINDRICAL_SURFACE ( 'NONE', #13704, 4.686499999999997002 ) ;
#11138=CIRCLE ( 'NONE', #24546, 2.000000000000000444 ) ;
#11147=VERTEX_POINT ( 'NONE', #25013 ) ;
#11154=AXIS2_PLACEMENT_3D ( 'NONE', #42197, #38978, #46380 ) ;
#11173=DIRECTION ( 'NONE',  ( -0.9979768094191906469, -0.06357898915123129380, 0.000000000000000000 ) ) ;
#11174=ADVANCED_FACE ( 'NONE', ( #18325 ), #32861, .T. ) ;
#11178=ORIENTED_EDGE ( 'NONE', *, *, #12102, .F. ) ;
#11195=ORIENTED_EDGE ( 'NONE', *, *, #24428, .T. ) ;
#11200=ORIENTED_EDGE ( 'NONE', *, *, #30851, .F. ) ;
#11215=ADVANCED_FACE ( 'NONE', ( #19316 ), #23035, .T. ) ;
#11219=CARTESIAN_POINT ( 'NONE',  ( -12.75497586646876691, -15.33350870067573979, 49.52966884056655772 ) ) ;
#11234=DIRECTION ( 'NONE',  ( -3.071710424422018668E-17, 6.404604876783312462E-16, 1.000000000000000000 ) ) ;
#11240=DIRECTION ( 'NONE',  ( 0.9687793358424821033, -0.2479245821708677133, 0.000000000000000000 ) ) ;
#11248=CARTESIAN_POINT ( 'NONE',  ( -16.17583575424048092, -10.27959207348368764, 49.52966884056655772 ) ) ;
#11260=EDGE_CURVE ( 'NONE', #36681, #14637, #5625, .T. ) ;
#11268=ADVANCED_FACE ( 'NONE', ( #15120 ), #30178, .T. ) ;
#11279=AXIS2_PLACEMENT_3D ( 'NONE', #32111, #32364, #24248 ) ;
#11280=DIRECTION ( 'NONE',  ( -3.071710424422018668E-17, 6.404604876783312462E-16, 1.000000000000000000 ) ) ;
#11286=ORIENTED_EDGE ( 'NONE', *, *, #28789, .T. ) ;
#11290=ORIENTED_EDGE ( 'NONE', *, *, #34879, .F. ) ;
#11300=ORIENTED_EDGE ( 'NONE', *, *, #13897, .F. ) ;
#11311=ORIENTED_EDGE ( 'NONE', *, *, #7922, .F. ) ;
#11322=EDGE_CURVE ( 'NONE', #29174, #44867, #26066, .T. ) ;
#11342=ORIENTED_EDGE ( 'NONE', *, *, #11260, .T. ) ;
#11347=EDGE_LOOP ( 'NONE', ( #12364, #45299, #12674, #47214, #518, #47023, #32631, #17701, #30466, #47662, #23667, #39583, #7818, #39768, #19267, #41057, #27028, #17735, #12271, #40946, #38357, #16032, #11290, #5091, #26523, #43842, #18648, #1954, #31164, #22376, #19183, #20849, #43870, #44846, #18536, #36133, #46459, #6769, #8076, #28217, #39623, #38848, #6903, #38216, #4438, #18117, #13510, #20618, #22835, #33322, #22468, #47682, #21117, #14741, #32858, #37658, #42711, #13604, #28342, #48723, #31110, #7130, #35901, #24282, #43375, #41083, #13797, #36528, #39078, #14797, #11715, #19158, #41317, #33837, #39532, #29566, #22328, #22654, #11460, #43517, #18641, #25306, #26906, #5707, #18968, #38995, #35087, #19639, #32418, #18105, #37364, #43875, #23100, #18269, #21307, #13028, #14360, #31270, #44724, #12510, #23264, #40155, #35351, #4417, #792, #4288, #45852, #24121, #15379, #44267, #14051, #46134, #21419, #35076, #24764, #27018, #37253, #47770, #5046, #13338, #37194, #5515, #41044, #33870, #4053, #5442, #11736, #22799, #33057, #35998, #23423, #44239, #37323, #10273, #1832, #36601, #22595, #722, #6701, #41494, #18796, #15347, #42825, #13295, #26454, #37395, #9062, #24399, #547, #9581, #23598, #18759, #40705, #44778, #38571, #34877, #34040, #42443, #22827, #13579, #17526, #42207, #25667, #20363, #26098 ) ) ;
#11359=DIRECTION ( 'NONE',  ( 0.6380325334150260819, -0.7700094066334536302, 0.000000000000000000 ) ) ;
#11360=CARTESIAN_POINT ( 'NONE',  ( -14.98297878932515381, -10.79466886532025605, 49.52966884056655772 ) ) ;
#11361=VERTEX_POINT ( 'NONE', #8742 ) ;
#11371=DIRECTION ( 'NONE',  ( 0.6607190350373968180, 0.7506333037770515082, 0.000000000000000000 ) ) ;
#11372=VECTOR ( 'NONE', #18762, 1000.000000000000000 ) ;
#11378=CARTESIAN_POINT ( 'NONE',  ( -18.89533436007378597, -9.769568524266553311, 49.52966884056655772 ) ) ;
#11382=ORIENTED_EDGE ( 'NONE', *, *, #11511, .F. ) ;
#11401=CARTESIAN_POINT ( 'NONE',  ( -21.51080377022508472, -17.10312989180209087, 49.52966884056655772 ) ) ;
#11402=VERTEX_POINT ( 'NONE', #33046 ) ;
#11404=CIRCLE ( 'NONE', #28700, 5.249999999999998224 ) ;
#11416=ORIENTED_EDGE ( 'NONE', *, *, #32121, .F. ) ;
#11419=VERTEX_POINT ( 'NONE', #10905 ) ;
#11427=EDGE_LOOP ( 'NONE', ( #47016, #14907, #13913, #12891 ) ) ;
#11436=CIRCLE ( 'NONE', #6729, 2.000000000000003109 ) ;
#11439=DIRECTION ( 'NONE',  ( -3.071710424422018668E-17, 6.404604876783312462E-16, 1.000000000000000000 ) ) ;
#11448=CYLINDRICAL_SURFACE ( 'NONE', #26802, 5.249999999999998224 ) ;
#11450=EDGE_CURVE ( 'NONE', #24111, #18890, #39422, .T. ) ;
#11460=ORIENTED_EDGE ( 'NONE', *, *, #27395, .T. ) ;
#11475=CARTESIAN_POINT ( 'NONE',  ( -20.49775566701509177, -11.27142682889164327, 49.52966884056655772 ) ) ;
#11478=ORIENTED_EDGE ( 'NONE', *, *, #21006, .T. ) ;
#11481=CARTESIAN_POINT ( 'NONE',  ( -22.10679845867080928, -14.99777973644470919, 49.52966884056655772 ) ) ;
#11497=EDGE_CURVE ( 'NONE', #36884, #21817, #48570, .T. ) ;
#11511=EDGE_CURVE ( 'NONE', #4743, #33825, #9559, .T. ) ;
#11515=EDGE_CURVE ( 'NONE', #22937, #1590, #37467, .T. ) ;
#11517=EDGE_LOOP ( 'NONE', ( #23031, #31405, #43274, #27289 ) ) ;
#11522=EDGE_CURVE ( 'NONE', #17919, #38294, #29869, .T. ) ;
#11531=ORIENTED_EDGE ( 'NONE', *, *, #48522, .T. ) ;
#11534=DIRECTION ( 'NONE',  ( 0.2189141945955470070, -0.9757441136919980940, 0.000000000000000000 ) ) ;
#11544=ORIENTED_EDGE ( 'NONE', *, *, #11522, .T. ) ;
#11561=DIRECTION ( 'NONE',  ( 0.9687793358424819923, -0.2479245821708680464, 0.000000000000000000 ) ) ;
#11563=EDGE_LOOP ( 'NONE', ( #43050, #28849, #21285, #26323 ) ) ;
#11565=DIRECTION ( 'NONE',  ( -3.071710424422018668E-17, 6.404604876783312462E-16, 1.000000000000000000 ) ) ;
#11567=DIRECTION ( 'NONE',  ( 3.071710424422018668E-17, -6.404604876783312462E-16, -1.000000000000000000 ) ) ;
#11571=AXIS2_PLACEMENT_3D ( 'NONE', #16631, #46688, #42987 ) ;
#11576=CIRCLE ( 'NONE', #3705, 2.000000000000001332 ) ;
#11605=CARTESIAN_POINT ( 'NONE',  ( -13.42648243792925378, -12.34047032955235679, 49.52966884056655772 ) ) ;
#11613=AXIS2_PLACEMENT_3D ( 'NONE', #18171, #21875, #13977 ) ;
#11615=AXIS2_PLACEMENT_3D ( 'NONE', #14685, #33177, #22870 ) ;
#11618=DIRECTION ( 'NONE',  ( -3.071710424422018668E-17, 6.404604876783312462E-16, 1.000000000000000000 ) ) ;
#11627=FILL_AREA_STYLE_COLOUR ( '', #36740 ) ;
#11630=CARTESIAN_POINT ( 'NONE',  ( -12.85799447202792045, -15.86467737382985632, 49.52966884056655772 ) ) ;
#11641=CIRCLE ( 'NONE', #17910, 2.000000000000001332 ) ;
#11653=DIRECTION ( 'NONE',  ( -0.9757441136919988711, -0.2189141945955433433, 0.000000000000000000 ) ) ;
#11667=CARTESIAN_POINT ( 'NONE',  ( -20.38066051823377478, -10.47086428435309280, 49.52966884056655772 ) ) ;
#11670=EDGE_CURVE ( 'NONE', #13690, #28383, #6415, .T. ) ;
#11681=AXIS2_PLACEMENT_3D ( 'NONE', #45740, #22578, #37834 ) ;
#11695=CARTESIAN_POINT ( 'NONE',  ( -17.42409385541299471, -14.80920654474435771, 49.52966884056655772 ) ) ;
#11715=ORIENTED_EDGE ( 'NONE', *, *, #43313, .T. ) ;
#11730=VECTOR ( 'NONE', #1414, 1000.000000000000000 ) ;
#11736=ORIENTED_EDGE ( 'NONE', *, *, #452, .T. ) ;
#11745=DIRECTION ( 'NONE',  ( -3.071710424422018668E-17, 6.404604876783312462E-16, 1.000000000000000000 ) ) ;
#11771=DIRECTION ( 'NONE',  ( -3.071710424422018668E-17, 6.404604876783312462E-16, 1.000000000000000000 ) ) ;
#11777=CARTESIAN_POINT ( 'NONE',  ( -18.36828968083242231, -10.20659317963780843, 52.02966884056656482 ) ) ;
#11778=DIRECTION ( 'NONE',  ( -0.8603395911234869020, -0.5097212845717467022, 0.000000000000000000 ) ) ;
#11795=ORIENTED_EDGE ( 'NONE', *, *, #34420, .T. ) ;
#11805=EDGE_CURVE ( 'NONE', #20388, #40396, #15820, .T. ) ;
#11807=DIRECTION ( 'NONE',  ( 3.071710424422018668E-17, -6.404604876783312462E-16, -1.000000000000000000 ) ) ;
#11822=AXIS2_PLACEMENT_3D ( 'NONE', #20378, #10267, #6320 ) ;
#11827=AXIS2_PLACEMENT_3D ( 'NONE', #8733, #15850, #23261 ) ;
#11839=VERTEX_POINT ( 'NONE', #3948 ) ;
#11852=EDGE_CURVE ( 'NONE', #8811, #1752, #10835, .T. ) ;
#11855=ORIENTED_EDGE ( 'NONE', *, *, #18721, .T. ) ;
#11868=DIRECTION ( 'NONE',  ( -3.071710424422018668E-17, 6.404604876783312462E-16, 1.000000000000000000 ) ) ;
#11870=CYLINDRICAL_SURFACE ( 'NONE', #1474, 5.249999999999998224 ) ;
#11873=FACE_OUTER_BOUND ( 'NONE', #29538, .T. ) ;
#11878=ORIENTED_EDGE ( 'NONE', *, *, #16958, .T. ) ;
#11904=DIRECTION ( 'NONE',  ( -3.071710424422018668E-17, 6.404604876783312462E-16, 1.000000000000000000 ) ) ;
#11917=VECTOR ( 'NONE', #8046, 1000.000000000000000 ) ;
#11936=DIRECTION ( 'NONE',  ( 0.9687793358424821033, -0.2479245821708677133, 0.000000000000000000 ) ) ;
#11945=AXIS2_PLACEMENT_3D ( 'NONE', #8488, #8748, #15360 ) ;
#11951=AXIS2_PLACEMENT_3D ( 'NONE', #46843, #20507, #43407 ) ;
#11963=AXIS2_PLACEMENT_3D ( 'NONE', #37650, #40866, #11561 ) ;
#11967=LINE ( 'NONE', #4563, #48626 ) ;
#11970=DIRECTION ( 'NONE',  ( -0.9294853595766568999, -0.3688590060343556187, 0.000000000000000000 ) ) ;
#11995=ORIENTED_EDGE ( 'NONE', *, *, #4299, .T. ) ;
#12000=DIRECTION ( 'NONE',  ( 3.071710424422018668E-17, -6.404604876783312462E-16, -1.000000000000000000 ) ) ;
#12002=VERTEX_POINT ( 'NONE', #2178 ) ;
#12004=ADVANCED_FACE ( 'NONE', ( #17182 ), #36384, .T. ) ;
#12019=LINE ( 'NONE', #27513, #18175 ) ;
#12028=CARTESIAN_POINT ( 'NONE',  ( -17.42409385541299471, -14.80920654474434883, 62.02966884056656482 ) ) ;
#12038=ORIENTED_EDGE ( 'NONE', *, *, #21938, .T. ) ;
#12044=ADVANCED_FACE ( 'NONE', ( #21149 ), #13495, .T. ) ;
#12071=EDGE_CURVE ( 'NONE', #45570, #36726, #43404, .T. ) ;
#12077=DIRECTION ( 'NONE',  ( 3.071710424422018668E-17, -6.404604876783312462E-16, -1.000000000000000000 ) ) ;
#12079=ORIENTED_EDGE ( 'NONE', *, *, #18443, .F. ) ;
#12080=DIRECTION ( 'NONE',  ( -3.071710424422018668E-17, 6.404604876783312462E-16, 1.000000000000000000 ) ) ;
#12081=DIRECTION ( 'NONE',  ( 0.9687793358424821033, -0.2479245821708680464, 0.000000000000000000 ) ) ;
#12082=AXIS2_PLACEMENT_3D ( 'NONE', #7918, #281, #34725 ) ;
#12093=ORIENTED_EDGE ( 'NONE', *, *, #8114, .T. ) ;
#12102=EDGE_CURVE ( 'NONE', #14963, #28111, #48095, .T. ) ;
#12111=EDGE_CURVE ( 'NONE', #15459, #41134, #17443, .T. ) ;
#12114=AXIS2_PLACEMENT_3D ( 'NONE', #5441, #1740, #34482 ) ;
#12120=ORIENTED_EDGE ( 'NONE', *, *, #5999, .F. ) ;
#12127=DIRECTION ( 'NONE',  ( -3.071710424422018668E-17, 6.404604876783312462E-16, 1.000000000000000000 ) ) ;
#12134=DIRECTION ( 'NONE',  ( 0.9687793358424819923, -0.2479245821708680464, 0.000000000000000000 ) ) ;
#12152=AXIS2_PLACEMENT_3D ( 'NONE', #38908, #19960, #5188 ) ;
#12161=ORIENTED_EDGE ( 'NONE', *, *, #25916, .F. ) ;
#12164=LINE ( 'NONE', #20533, #46393 ) ;
#12171=ORIENTED_EDGE ( 'NONE', *, *, #1893, .T. ) ;
#12179=AXIS2_PLACEMENT_3D ( 'NONE', #3746, #26164, #27123 ) ;
#12180=EDGE_CURVE ( 'NONE', #27273, #26781, #26887, .T. ) ;
#12194=ORIENTED_EDGE ( 'NONE', *, *, #23223, .T. ) ;
#12199=CARTESIAN_POINT ( 'NONE',  ( -19.80621920301059902, -19.48766556757794532, 49.52966884056656482 ) ) ;
#12200=DIRECTION ( 'NONE',  ( 0.9687793358424821033, -0.2479245821708679909, 0.000000000000000000 ) ) ;
#12203=ADVANCED_FACE ( 'NONE', ( #34325 ), #45441, .T. ) ;
#12204=ADVANCED_FACE ( 'NONE', ( #45920 ), #45690, .T. ) ;
#12206=DIRECTION ( 'NONE',  ( -3.071710424422018668E-17, 6.404604876783312462E-16, 1.000000000000000000 ) ) ;
#12207=DIRECTION ( 'NONE',  ( 0.5097212845717493668, -0.8603395911234852367, 0.000000000000000000 ) ) ;
#12211=DIRECTION ( 'NONE',  ( -3.071710424422018668E-17, 6.404604876783312462E-16, 1.000000000000000000 ) ) ;
#12213=CARTESIAN_POINT ( 'NONE',  ( -13.84085632603101956, -17.84827948783496865, 49.52966884056656482 ) ) ;
#12216=EDGE_CURVE ( 'NONE', #38535, #8357, #15070, .T. ) ;
#12219=AXIS2_PLACEMENT_3D ( 'NONE', #5913, #9625, #24640 ) ;
#12221=ORIENTED_EDGE ( 'NONE', *, *, #5782, .T. ) ;
#12225=DIRECTION ( 'NONE',  ( -3.071710424422018668E-17, 6.404604876783312462E-16, 1.000000000000000000 ) ) ;
#12235=ORIENTED_EDGE ( 'NONE', *, *, #48551, .F. ) ;
#12250=DIRECTION ( 'NONE',  ( -3.071710424422018668E-17, 6.404604876783312462E-16, 1.000000000000000000 ) ) ;
#12271=ORIENTED_EDGE ( 'NONE', *, *, #10716, .F. ) ;
#12283=VECTOR ( 'NONE', #8481, 1000.000000000000000 ) ;
#12296=CARTESIAN_POINT ( 'NONE',  ( -15.13017050835524913, -18.89591645955643884, 49.52966884056656482 ) ) ;
#12299=DIRECTION ( 'NONE',  ( 0.7506333037770492878, -0.6607190350373991494, 0.000000000000000000 ) ) ;
#12300=ORIENTED_EDGE ( 'NONE', *, *, #34675, .F. ) ;
#12304=EDGE_CURVE ( 'NONE', #2214, #2300, #9596, .T. ) ;
#12334=CARTESIAN_POINT ( 'NONE',  ( -20.46316679850361808, -18.39244407412632043, 49.52966884056656482 ) ) ;
#12344=ADVANCED_FACE ( 'NONE', ( #31628 ), #5775, .T. ) ;
#12347=CARTESIAN_POINT ( 'NONE',  ( -12.73044152958719977, -14.59664269629646505, 52.02966884056656482 ) ) ;
#12349=EDGE_CURVE ( 'NONE', #28760, #9874, #8817, .T. ) ;
#12361=ORIENTED_EDGE ( 'NONE', *, *, #20395, .F. ) ;
#12364=ORIENTED_EDGE ( 'NONE', *, *, #38846, .T. ) ;
#12371=LINE ( 'NONE', #7980, #22647 ) ;
#12382=DIRECTION ( 'NONE',  ( -3.071710424422018668E-17, 6.404604876783312462E-16, 1.000000000000000000 ) ) ;
#12386=EDGE_CURVE ( 'NONE', #32100, #11419, #7234, .T. ) ;
#12390=DIRECTION ( 'NONE',  ( 0.8447509909909731718, -0.5351595679979651576, 0.000000000000000000 ) ) ;
#12393=CARTESIAN_POINT ( 'NONE',  ( -12.26581428767149795, -15.78626943986449760, 49.52966884056655772 ) ) ;
#12401=CARTESIAN_POINT ( 'NONE',  ( -17.42409385541299471, -14.80920654474435771, 49.52966884056655772 ) ) ;
#12403=CARTESIAN_POINT ( 'NONE',  ( -21.67055903134415473, -17.89628178023893668, 50.77966884056655772 ) ) ;
#12411=AXIS2_PLACEMENT_3D ( 'NONE', #30919, #23528, #34098 ) ;
#12416=EDGE_CURVE ( 'NONE', #48505, #31312, #32399, .T. ) ;
#12417=CARTESIAN_POINT ( 'NONE',  ( -12.89447938415233175, -16.05746464591688749, 52.02966884056656482 ) ) ;
#12431=CARTESIAN_POINT ( 'NONE',  ( -13.71283467540607504, -11.09584481999758232, 49.52966884056655772 ) ) ;
#12443=DIRECTION ( 'NONE',  ( -3.071710424422018668E-17, 6.404604876783312462E-16, 1.000000000000000000 ) ) ;
#12444=ORIENTED_EDGE ( 'NONE', *, *, #29177, .F. ) ;
#12447=VECTOR ( 'NONE', #11807, 1000.000000000000000 ) ;
#12448=DIRECTION ( 'NONE',  ( -3.071710424422018668E-17, 6.404604876783312462E-16, 1.000000000000000000 ) ) ;
#12452=AXIS2_PLACEMENT_3D ( 'NONE', #2627, #28734, #39812 ) ;
#12455=VERTEX_POINT ( 'NONE', #17556 ) ;
#12479=AXIS2_PLACEMENT_3D ( 'NONE', #34230, #34730, #15758 ) ;
#12484=CIRCLE ( 'NONE', #35250, 1.999999999999999112 ) ;
#12508=FACE_OUTER_BOUND ( 'NONE', #25603, .T. ) ;
#12510=ORIENTED_EDGE ( 'NONE', *, *, #24641, .T. ) ;
#12511=DIRECTION ( 'NONE',  ( -3.071710424422018668E-17, 6.404604876783312462E-16, 1.000000000000000000 ) ) ;
#12528=DIRECTION ( 'NONE',  ( -3.071710424422018668E-17, 6.404604876783312462E-16, 1.000000000000000000 ) ) ;
#12544=ORIENTED_EDGE ( 'NONE', *, *, #30460, .F. ) ;
#12553=AXIS2_PLACEMENT_3D ( 'NONE', #16252, #28340, #16978 ) ;
#12568=CYLINDRICAL_SURFACE ( 'NONE', #22374, 4.686499999999997002 ) ;
#12569=DIRECTION ( 'NONE',  ( -3.071710424422018668E-17, 6.404604876783312462E-16, 1.000000000000000000 ) ) ;
#12580=DIRECTION ( 'NONE',  ( 0.9687793358424822143, -0.2479245821708672415, 0.000000000000000000 ) ) ;
#12586=DIRECTION ( 'NONE',  ( 0.9687793358424821033, -0.2479245821708677133, 0.000000000000000000 ) ) ;
#12591=CIRCLE ( 'NONE', #40118, 1.999999999999999112 ) ;
#12607=DIRECTION ( 'NONE',  ( -3.071710424422018668E-17, 6.404604876783312462E-16, 1.000000000000000000 ) ) ;
#12617=VERTEX_POINT ( 'NONE', #35963 ) ;
#12625=VECTOR ( 'NONE', #43186, 1000.000000000000000 ) ;
#12626=DIRECTION ( 'NONE',  ( -3.071710424422018668E-17, 6.404604876783312462E-16, 1.000000000000000000 ) ) ;
#12634=CYLINDRICAL_SURFACE ( 'NONE', #17889, 1.999999999999999556 ) ;
#12653=FACE_OUTER_BOUND ( 'NONE', #7225, .T. ) ;
#12666=EDGE_CURVE ( 'NONE', #14945, #30767, #28361, .T. ) ;
#12674=ORIENTED_EDGE ( 'NONE', *, *, #6406, .F. ) ;
#12690=AXIS2_PLACEMENT_3D ( 'NONE', #30398, #14352, #4289 ) ;
#12698=VERTEX_POINT ( 'NONE', #47783 ) ;
#12718=CARTESIAN_POINT ( 'NONE',  ( -13.27161037900033058, -18.02158587759403829, 49.52966884056656482 ) ) ;
#12723=AXIS2_PLACEMENT_3D ( 'NONE', #14614, #14375, #22289 ) ;
#12734=DIRECTION ( 'NONE',  ( 0.9687793358424821033, -0.2479245821708677133, 0.000000000000000000 ) ) ;
#12736=ORIENTED_EDGE ( 'NONE', *, *, #8966, .F. ) ;
#12739=CYLINDRICAL_SURFACE ( 'NONE', #44171, 1.999999999999999112 ) ;
#12742=VERTEX_POINT ( 'NONE', #29315 ) ;
#12744=LINE ( 'NONE', #17137, #35080 ) ;
#12745=ORIENTED_EDGE ( 'NONE', *, *, #48606, .T. ) ;
#12746=DIRECTION ( 'NONE',  ( -3.071710424422018668E-17, 6.404604876783312462E-16, 1.000000000000000000 ) ) ;
#12756=VERTEX_POINT ( 'NONE', #10374 ) ;
#12760=EDGE_CURVE ( 'NONE', #40280, #40811, #39837, .T. ) ;
#12761=EDGE_CURVE ( 'NONE', #34423, #6071, #26476, .T. ) ;
#12766=DIRECTION ( 'NONE',  ( -3.071710424422018668E-17, 6.404604876783312462E-16, 1.000000000000000000 ) ) ;
#12769=LINE ( 'NONE', #20154, #29070 ) ;
#12778=CARTESIAN_POINT ( 'NONE',  ( -17.42409385541299471, -14.80920654474435594, 52.02966884056656482 ) ) ;
#12783=CARTESIAN_POINT ( 'NONE',  ( -19.89283007060495123, -10.81159512726059191, 49.52966884056655772 ) ) ;
#12790=CARTESIAN_POINT ( 'NONE',  ( -13.60167271156757707, -11.21037387301822186, 50.77966884056655772 ) ) ;
#12802=ORIENTED_EDGE ( 'NONE', *, *, #37342, .T. ) ;
#12806=FACE_BOUND ( 'NONE', #31205, .T. ) ;
#12840=AXIS2_PLACEMENT_3D ( 'NONE', #21936, #18228, #25158 ) ;
#12848=ORIENTED_EDGE ( 'NONE', *, *, #8190, .T. ) ;
#12849=CARTESIAN_POINT ( 'NONE',  ( -15.77151528785019430, -19.20744933288474954, 52.02966884056656482 ) ) ;
#12854=DIRECTION ( 'NONE',  ( 0.9687793358424821033, -0.2479245821708680464, 0.000000000000000000 ) ) ;
#12891=ORIENTED_EDGE ( 'NONE', *, *, #42838, .T. ) ;
#12920=DIRECTION ( 'NONE',  ( 3.071710424422018668E-17, -6.404604876783312462E-16, -1.000000000000000000 ) ) ;
#12945=LINE ( 'NONE', #39050, #14182 ) ;
#12959=VERTEX_POINT ( 'NONE', #41399 ) ;
#12964=ORIENTED_EDGE ( 'NONE', *, *, #40745, .F. ) ;
#12973=CIRCLE ( 'NONE', #46811, 4.686499999999998778 ) ;
#12983=DIRECTION ( 'NONE',  ( 0.9687793358424821033, -0.2479245821708680464, 0.000000000000000000 ) ) ;
#12992=CARTESIAN_POINT ( 'NONE',  ( -18.69178539469224987, -19.32099559247695097, 49.52966884056656482 ) ) ;
#12997=ADVANCED_FACE ( 'NONE', ( #20464 ), #42867, .T. ) ;
#13016=LINE ( 'NONE', #8625, #18806 ) ;
#13028=ORIENTED_EDGE ( 'NONE', *, *, #40997, .T. ) ;
#13034=DIRECTION ( 'NONE',  ( -0.5097212845717550289, 0.8603395911234817950, 0.000000000000000000 ) ) ;
#13038=DIRECTION ( 'NONE',  ( 3.071710424422018052E-17, -6.404604876783311476E-16, -1.000000000000000000 ) ) ;
#13045=DIRECTION ( 'NONE',  ( -3.071710424422018668E-17, 6.404604876783312462E-16, 1.000000000000000000 ) ) ;
#13046=DIRECTION ( 'NONE',  ( -3.071710424422018668E-17, 6.404604876783312462E-16, 1.000000000000000000 ) ) ;
#13051=VERTEX_POINT ( 'NONE', #1491 ) ;
#13072=ORIENTED_EDGE ( 'NONE', *, *, #7848, .F. ) ;
#13083=VERTEX_POINT ( 'NONE', #17942 ) ;
#13093=CARTESIAN_POINT ( 'NONE',  ( -17.42409385541299471, -14.80920654474435594, 52.02966884056656482 ) ) ;
#13117=VERTEX_POINT ( 'NONE', #6405 ) ;
#13129=VERTEX_POINT ( 'NONE', #36650 ) ;
#13138=ORIENTED_EDGE ( 'NONE', *, *, #9628, .F. ) ;
#13139=EDGE_CURVE ( 'NONE', #46408, #42407, #32959, .T. ) ;
#13163=DIRECTION ( 'NONE',  ( -3.071710424422018668E-17, 6.404604876783312462E-16, 1.000000000000000000 ) ) ;
#13196=ORIENTED_EDGE ( 'NONE', *, *, #11005, .F. ) ;
#13202=VERTEX_POINT ( 'NONE', #34187 ) ;
#13206=DIRECTION ( 'NONE',  ( 0.9687793358424821033, -0.2479245821708679909, 0.000000000000000000 ) ) ;
#13211=DIRECTION ( 'NONE',  ( -0.8603395911234869020, -0.5097212845717467022, 0.000000000000000000 ) ) ;
#13231=DIRECTION ( 'NONE',  ( -3.071710424422018668E-17, 6.404604876783312462E-16, 1.000000000000000000 ) ) ;
#13237=EDGE_CURVE ( 'NONE', #40280, #19312, #19420, .T. ) ;
#13239=AXIS2_PLACEMENT_3D ( 'NONE', #13093, #32323, #28388 ) ;
#13255=ORIENTED_EDGE ( 'NONE', *, *, #12666, .T. ) ;
#13269=ORIENTED_EDGE ( 'NONE', *, *, #2736, .T. ) ;
#13270=FACE_OUTER_BOUND ( 'NONE', #7839, .T. ) ;
#13271=AXIS2_PLACEMENT_3D ( 'NONE', #25657, #33267, #37710 ) ;
#13282=VECTOR ( 'NONE', #22943, 1000.000000000000000 ) ;
#13285=ADVANCED_FACE ( 'NONE', ( #33685 ), #30282, .T. ) ;
#13294=ORIENTED_EDGE ( 'NONE', *, *, #41059, .F. ) ;
#13295=ORIENTED_EDGE ( 'NONE', *, *, #14834, .T. ) ;
#13309=CARTESIAN_POINT ( 'NONE',  ( -18.53667165497532920, -10.24437071140731170, 49.52966884056655772 ) ) ;
#13333=CARTESIAN_POINT ( 'NONE',  ( -14.96223302779666398, -10.63593772014186278, 49.52966884056655772 ) ) ;
#13338=ORIENTED_EDGE ( 'NONE', *, *, #12304, .T. ) ;
#13348=EDGE_CURVE ( 'NONE', #34852, #25804, #1186, .T. ) ;
#13354=EDGE_CURVE ( 'NONE', #23394, #34714, #31237, .T. ) ;
#13358=CARTESIAN_POINT ( 'NONE',  ( -19.04784696903935881, -9.816619457272706128, 49.52966884056655772 ) ) ;
#13376=CIRCLE ( 'NONE', #16515, 4.686499999999998778 ) ;
#13378=EDGE_LOOP ( 'NONE', ( #39786, #2352, #47443, #8834 ) ) ;
#13380=CIRCLE ( 'NONE', #11827, 4.686499999999999666 ) ;
#13401=ORIENTED_EDGE ( 'NONE', *, *, #47941, .F. ) ;
#13414=CIRCLE ( 'NONE', #46449, 1.999999999999999112 ) ;
#13430=VERTEX_POINT ( 'NONE', #36838 ) ;
#13442=CARTESIAN_POINT ( 'NONE',  ( -20.48780003469585154, -11.24700778661463829, 49.52966884056655772 ) ) ;
#13446=ORIENTED_EDGE ( 'NONE', *, *, #29445, .T. ) ;
#13448=AXIS2_PLACEMENT_3D ( 'NONE', #16041, #12127, #4491 ) ;
#13449=ORIENTED_EDGE ( 'NONE', *, *, #30160, .T. ) ;
#13452=ORIENTED_EDGE ( 'NONE', *, *, #8261, .F. ) ;
#13474=DIRECTION ( 'NONE',  ( 0.9687793358424822143, -0.2479245821708672415, 0.000000000000000000 ) ) ;
#13484=EDGE_CURVE ( 'NONE', #20349, #30644, #14662, .T. ) ;
#13486=CARTESIAN_POINT ( 'NONE',  ( -17.42409385541299471, -14.80920654474435594, 52.02966884056656482 ) ) ;
#13495=CYLINDRICAL_SURFACE ( 'NONE', #31581, 2.000000000000000000 ) ;
#13502=CARTESIAN_POINT ( 'NONE',  ( -21.82233664355339542, -16.46178511230714037, 52.02966884056656482 ) ) ;
#13510=ORIENTED_EDGE ( 'NONE', *, *, #36767, .T. ) ;
#13514=EDGE_LOOP ( 'NONE', ( #37887, #37625, #4423, #19913 ) ) ;
#13520=CARTESIAN_POINT ( 'NONE',  ( -17.42409385541299471, -14.80920654474435771, 49.52966884056655772 ) ) ;
#13543=EDGE_CURVE ( 'NONE', #10107, #3267, #39092, .T. ) ;
#13549=ORIENTED_EDGE ( 'NONE', *, *, #5782, .F. ) ;
#13556=ORIENTED_EDGE ( 'NONE', *, *, #5463, .F. ) ;
#13569=LINE ( 'NONE', #32066, #38647 ) ;
#13577=DIRECTION ( 'NONE',  ( 0.2479245821708712660, 0.9687793358424811041, 0.000000000000000000 ) ) ;
#13578=EDGE_LOOP ( 'NONE', ( #5932, #583, #11416, #17503 ) ) ;
#13579=ORIENTED_EDGE ( 'NONE', *, *, #46154, .T. ) ;
#13580=DIRECTION ( 'NONE',  ( -3.071710424422018668E-17, 6.404604876783312462E-16, 1.000000000000000000 ) ) ;
#13590=ORIENTED_EDGE ( 'NONE', *, *, #1774, .T. ) ;
#13595=ORIENTED_EDGE ( 'NONE', *, *, #26603, .F. ) ;
#13596=DIRECTION ( 'NONE',  ( -0.6607190350374009258, -0.7506333037770478445, 0.000000000000000000 ) ) ;
#13603=ORIENTED_EDGE ( 'NONE', *, *, #25441, .T. ) ;
#13604=ORIENTED_EDGE ( 'NONE', *, *, #18660, .T. ) ;
#13616=ORIENTED_EDGE ( 'NONE', *, *, #8345, .T. ) ;
#13634=ORIENTED_EDGE ( 'NONE', *, *, #5110, .F. ) ;
#13662=ORIENTED_EDGE ( 'NONE', *, *, #34563, .F. ) ;
#13672=CYLINDRICAL_SURFACE ( 'NONE', #17104, 5.249999999999998224 ) ;
#13673=EDGE_CURVE ( 'NONE', #30431, #14945, #35952, .T. ) ;
#13690=VERTEX_POINT ( 'NONE', #39041 ) ;
#13696=CARTESIAN_POINT ( 'NONE',  ( -12.82854046268865034, -13.89041861240101028, 52.02966884056656482 ) ) ;
#13701=CIRCLE ( 'NONE', #34166, 2.000000000000000888 ) ;
#13704=AXIS2_PLACEMENT_3D ( 'NONE', #17761, #26151, #45121 ) ;
#13733=VECTOR ( 'NONE', #12206, 1000.000000000000000 ) ;
#13737=DIRECTION ( 'NONE',  ( 0.9757441136919973168, 0.2189141945955502822, 0.000000000000000000 ) ) ;
#13742=EDGE_CURVE ( 'NONE', #29199, #31757, #5290, .T. ) ;
#13745=LINE ( 'NONE', #2680, #28131 ) ;
#13749=LINE ( 'NONE', #28792, #36225 ) ;
#13759=VERTEX_POINT ( 'NONE', #43977 ) ;
#13764=ORIENTED_EDGE ( 'NONE', *, *, #46869, .F. ) ;
#13783=CARTESIAN_POINT ( 'NONE',  ( -22.02670722051955465, -15.75340237016373202, 49.52966884056655772 ) ) ;
#13795=DIRECTION ( 'NONE',  ( 0.9687793358424821033, -0.2479245821708677133, 0.000000000000000000 ) ) ;
#13797=ORIENTED_EDGE ( 'NONE', *, *, #25302, .T. ) ;
#13800=EDGE_CURVE ( 'NONE', #19337, #44272, #35587, .T. ) ;
#13806=ORIENTED_EDGE ( 'NONE', *, *, #15123, .F. ) ;
#13844=EDGE_CURVE ( 'NONE', #39405, #44032, #46165, .T. ) ;
#13855=ORIENTED_EDGE ( 'NONE', *, *, #9324, .F. ) ;
#13858=ORIENTED_EDGE ( 'NONE', *, *, #13844, .T. ) ;
#13863=DIRECTION ( 'NONE',  ( -0.3688590060343653887, 0.9294853595766531251, 0.000000000000000000 ) ) ;
#13876=DIRECTION ( 'NONE',  ( -3.071710424422018668E-17, 6.404604876783312462E-16, 1.000000000000000000 ) ) ;
#13889=LINE ( 'NONE', #28933, #36155 ) ;
#13890=EDGE_CURVE ( 'NONE', #2810, #27599, #39863, .T. ) ;
#13897=EDGE_CURVE ( 'NONE', #43519, #43657, #18624, .T. ) ;
#13906=VECTOR ( 'NONE', #15374, 1000.000000000000000 ) ;
#13913=ORIENTED_EDGE ( 'NONE', *, *, #40227, .F. ) ;
#13916=FACE_OUTER_BOUND ( 'NONE', #20291, .T. ) ;
#13938=EDGE_LOOP ( 'NONE', ( #28721, #22146, #3070, #17445 ) ) ;
#13939=DIRECTION ( 'NONE',  ( -3.071710424422018668E-17, 6.404604876783312462E-16, 1.000000000000000000 ) ) ;
#13951=EDGE_CURVE ( 'NONE', #9874, #39514, #45362, .T. ) ;
#13954=CARTESIAN_POINT ( 'NONE',  ( -12.74141321320493958, -14.42442407569615170, 52.02966884056656482 ) ) ;
#13955=DIRECTION ( 'NONE',  ( -3.071710424422018668E-17, 6.404604876783312462E-16, 1.000000000000000000 ) ) ;
#13961=CARTESIAN_POINT ( 'NONE',  ( -17.42409385541299471, -14.80920654474435771, 49.52966884056655772 ) ) ;
#13962=AXIS2_PLACEMENT_3D ( 'NONE', #44721, #18343, #26000 ) ;
#13965=CIRCLE ( 'NONE', #44702, 1.999999999999999334 ) ;
#13975=VECTOR ( 'NONE', #47225, 1000.000000000000000 ) ;
#13976=EDGE_LOOP ( 'NONE', ( #696, #10848, #2266, #17316 ) ) ;
#13977=DIRECTION ( 'NONE',  ( -0.6607190350374017029, -0.7506333037770471783, 0.000000000000000000 ) ) ;
#13989=DIRECTION ( 'NONE',  ( -3.071710424422018668E-17, 6.404604876783312462E-16, 1.000000000000000000 ) ) ;
#13994=CARTESIAN_POINT ( 'NONE',  ( -16.89979169948162863, -10.14008855580012458, 52.02966884056656482 ) ) ;
#14000=AXIS2_PLACEMENT_3D ( 'NONE', #19601, #35342, #1858 ) ;
#14017=CARTESIAN_POINT ( 'NONE',  ( -14.23827708255551627, -10.77544123782542229, 49.52966884056655772 ) ) ;
#14018=VERTEX_POINT ( 'NONE', #42649 ) ;
#14027=CIRCLE ( 'NONE', #10126, 5.249999999999998224 ) ;
#14042=CARTESIAN_POINT ( 'NONE',  ( -13.08575159502176177, -11.85263988192353324, 50.77966884056655772 ) ) ;
#14051=ORIENTED_EDGE ( 'NONE', *, *, #46170, .T. ) ;
#14059=LINE ( 'NONE', #48298, #40736 ) ;
#14075=AXIS2_PLACEMENT_3D ( 'NONE', #6459, #28852, #22199 ) ;
#14076=VERTEX_POINT ( 'NONE', #5209 ) ;
#14077=ORIENTED_EDGE ( 'NONE', *, *, #25022, .T. ) ;
#14080=EDGE_LOOP ( 'NONE', ( #32552, #40754, #28210, #1723 ) ) ;
#14098=CARTESIAN_POINT ( 'NONE',  ( -16.47989802999360265, -19.41181990985090877, 49.52966884056656482 ) ) ;
#14099=ORIENTED_EDGE ( 'NONE', *, *, #2914, .F. ) ;
#14106=DIRECTION ( 'NONE',  ( -3.071710424422018668E-17, 6.404604876783312462E-16, 1.000000000000000000 ) ) ;
#14108=CARTESIAN_POINT ( 'NONE',  ( -19.19606018965890115, -19.75113282002397597, 49.52966884056656482 ) ) ;
#14109=CARTESIAN_POINT ( 'NONE',  ( -21.81933826130772047, -16.43558560955401049, 52.02966884056656482 ) ) ;
#14111=CARTESIAN_POINT ( 'NONE',  ( -17.42409385541299471, -14.80920654474435594, 52.02966884056656482 ) ) ;
#14126=ORIENTED_EDGE ( 'NONE', *, *, #27817, .T. ) ;
#14131=DIRECTION ( 'NONE',  ( 0.9687793358424821033, -0.2479245821708677133, 0.000000000000000000 ) ) ;
#14136=CIRCLE ( 'NONE', #56, 4.686499999999998778 ) ;
#14144=ORIENTED_EDGE ( 'NONE', *, *, #18721, .F. ) ;
#14157=CARTESIAN_POINT ( 'NONE',  ( -12.75497586646876691, -15.33350870067573801, 52.02966884056656482 ) ) ;
#14182=VECTOR ( 'NONE', #9523, 1000.000000000000000 ) ;
#14238=VERTEX_POINT ( 'NONE', #44824 ) ;
#14242=DIRECTION ( 'NONE',  ( 3.071710424422018668E-17, -6.404604876783312462E-16, -1.000000000000000000 ) ) ;
#14256=ORIENTED_EDGE ( 'NONE', *, *, #42541, .T. ) ;
#14258=CIRCLE ( 'NONE', #3291, 1.999999999999999112 ) ;
#14289=ADVANCED_FACE ( 'NONE', ( #18686 ), #30291, .T. ) ;
#14329=DIRECTION ( 'NONE',  ( -3.071710424422018668E-17, 6.404604876783312462E-16, 1.000000000000000000 ) ) ;
#14341=ORIENTED_EDGE ( 'NONE', *, *, #550, .F. ) ;
#14348=EDGE_CURVE ( 'NONE', #10974, #8357, #1196, .T. ) ;
#14352=DIRECTION ( 'NONE',  ( -3.071710424422018668E-17, 6.404604876783312462E-16, 1.000000000000000000 ) ) ;
#14358=ORIENTED_EDGE ( 'NONE', *, *, #38328, .T. ) ;
#14360=ORIENTED_EDGE ( 'NONE', *, *, #23381, .F. ) ;
#14371=CARTESIAN_POINT ( 'NONE',  ( -16.87780900865216438, -10.15465445929086208, 49.52966884056655772 ) ) ;
#14375=DIRECTION ( 'NONE',  ( -3.071710424422018668E-17, 6.404604876783312462E-16, 1.000000000000000000 ) ) ;
#14388=VERTEX_POINT ( 'NONE', #31969 ) ;
#14400=CYLINDRICAL_SURFACE ( 'NONE', #17146, 2.000000000000000000 ) ;
#14414=CARTESIAN_POINT ( 'NONE',  ( -14.21171452256333012, -10.65672306833168115, 49.52966884056655772 ) ) ;
#14416=CARTESIAN_POINT ( 'NONE',  ( -17.42409385541299471, -14.80920654474435594, 52.02966884056656482 ) ) ;
#14424=FACE_OUTER_BOUND ( 'NONE', #44926, .T. ) ;
#14427=CARTESIAN_POINT ( 'NONE',  ( -12.74141321320493958, -14.42442407569615348, 49.52966884056655772 ) ) ;
#14452=CARTESIAN_POINT ( 'NONE',  ( -18.89533436007378597, -9.769568524266551535, 52.02966884056656482 ) ) ;
#14455=AXIS2_PLACEMENT_3D ( 'NONE', #29035, #6636, #29286 ) ;
#14457=ADVANCED_FACE ( 'NONE', ( #14424 ), #47484, .T. ) ;
#14466=DIRECTION ( 'NONE',  ( -0.09332174201254901658, -0.9956360040033422898, 0.000000000000000000 ) ) ;
#14467=DIRECTION ( 'NONE',  ( 0.9687793358424821033, -0.2479245821708677133, 0.000000000000000000 ) ) ;
#14479=VERTEX_POINT ( 'NONE', #40327 ) ;
#14488=ORIENTED_EDGE ( 'NONE', *, *, #20934, .F. ) ;
#14499=CARTESIAN_POINT ( 'NONE',  ( -21.51080377022508472, -17.10312989180208731, 52.02966884056656482 ) ) ;
#14521=FACE_OUTER_BOUND ( 'NONE', #14080, .T. ) ;
#14523=AXIS2_PLACEMENT_3D ( 'NONE', #9911, #43654, #13577 ) ;
#14525=ORIENTED_EDGE ( 'NONE', *, *, #2181, .F. ) ;
#14582=CARTESIAN_POINT ( 'NONE',  ( -21.10164091802717223, -17.71419016815049119, 49.52966884056655772 ) ) ;
#14588=DIRECTION ( 'NONE',  ( -3.071710424422018668E-17, 6.404604876783312462E-16, 1.000000000000000000 ) ) ;
#14591=EDGE_LOOP ( 'NONE', ( #40204, #21928, #32220, #19763 ) ) ;
#14598=EDGE_LOOP ( 'NONE', ( #16598, #48083, #8516, #29399 ) ) ;
#14608=CARTESIAN_POINT ( 'NONE',  ( -16.60134452727454146, -19.99433755013348346, 52.02966884056656482 ) ) ;
#14614=CARTESIAN_POINT ( 'NONE',  ( -17.42409385541299471, -14.80920654474435594, 52.02966884056656482 ) ) ;
#14615=ADVANCED_FACE ( 'NONE', ( #23570 ), #1630, .T. ) ;
#14621=CIRCLE ( 'NONE', #23325, 4.686499999999999666 ) ;
#14633=ORIENTED_EDGE ( 'NONE', *, *, #46680, .F. ) ;
#14634=DIRECTION ( 'NONE',  ( 0.9979768094191903138, 0.06357898915123821881, 0.000000000000000000 ) ) ;
#14637=VERTEX_POINT ( 'NONE', #26172 ) ;
#14652=ORIENTED_EDGE ( 'NONE', *, *, #45455, .F. ) ;
#14655=MANIFOLD_SOLID_BREP ( 'Stock-MAS-175-1', #9501 ) ;
#14662=CIRCLE ( 'NONE', #42232, 1.999999999999999112 ) ;
#14665=ORIENTED_EDGE ( 'NONE', *, *, #29316, .T. ) ;
#14668=DIRECTION ( 'NONE',  ( -3.071710424422018668E-17, 6.404604876783312462E-16, 1.000000000000000000 ) ) ;
#14672=CIRCLE ( 'NONE', #17078, 2.000000000000000000 ) ;
#14677=LINE ( 'NONE', #29746, #8806 ) ;
#14679=CARTESIAN_POINT ( 'NONE',  ( -21.76886496386750736, -13.05243499865792067, 49.52966884056655772 ) ) ;
#14685=CARTESIAN_POINT ( 'NONE',  ( -17.42409385541299471, -14.80920654474434883, 62.02966884056656482 ) ) ;
#14686=EDGE_CURVE ( 'NONE', #28351, #38822, #20259, .T. ) ;
#14689=LINE ( 'NONE', #40829, #27524 ) ;
#14707=ORIENTED_EDGE ( 'NONE', *, *, #13951, .F. ) ;
#14715=EDGE_CURVE ( 'NONE', #44272, #43656, #17109, .T. ) ;
#14718=DIRECTION ( 'NONE',  ( -3.071710424422018668E-17, 6.404604876783312462E-16, 1.000000000000000000 ) ) ;
#14723=CYLINDRICAL_SURFACE ( 'NONE', #5600, 4.686499999999997002 ) ;
#14730=DIRECTION ( 'NONE',  ( 3.071710424422018668E-17, -6.404604876783312462E-16, -1.000000000000000000 ) ) ;
#14740=DIRECTION ( 'NONE',  ( -0.9687793358424819923, 0.2479245821708680464, 0.000000000000000000 ) ) ;
#14741=ORIENTED_EDGE ( 'NONE', *, *, #42366, .T. ) ;
#14762=ORIENTED_EDGE ( 'NONE', *, *, #15861, .F. ) ;
#14763=CIRCLE ( 'NONE', #25039, 2.000000000000000888 ) ;
#14765=CYLINDRICAL_SURFACE ( 'NONE', #25844, 1.999999999999999556 ) ;
#14768=DIRECTION ( 'NONE',  ( 0.9294853595766541243, 0.3688590060343629462, 0.000000000000000000 ) ) ;
#14786=ORIENTED_EDGE ( 'NONE', *, *, #40824, .T. ) ;
#14797=ORIENTED_EDGE ( 'NONE', *, *, #14895, .T. ) ;
#14800=DIRECTION ( 'NONE',  ( -3.071710424422018668E-17, 6.404604876783312462E-16, 1.000000000000000000 ) ) ;
#14802=AXIS2_PLACEMENT_3D ( 'NONE', #20084, #12448, #31167 ) ;
#14803=AXIS2_PLACEMENT_3D ( 'NONE', #17339, #32383, #39280 ) ;
#14804=EDGE_CURVE ( 'NONE', #14479, #28111, #16299, .T. ) ;
#14817=DIRECTION ( 'NONE',  ( -3.071710424422018668E-17, 6.404604876783312462E-16, 1.000000000000000000 ) ) ;
#14819=ORIENTED_EDGE ( 'NONE', *, *, #18402, .F. ) ;
#14828=DIRECTION ( 'NONE',  ( -3.071710424422018668E-17, 6.404604876783312462E-16, 1.000000000000000000 ) ) ;
#14834=EDGE_CURVE ( 'NONE', #32811, #17454, #42301, .T. ) ;
#14836=AXIS2_PLACEMENT_3D ( 'NONE', #34673, #30026, #41332 ) ;
#14841=CARTESIAN_POINT ( 'NONE',  ( -17.42409385541299471, -14.80920654474435771, 49.52966884056655772 ) ) ;
#14848=ORIENTED_EDGE ( 'NONE', *, *, #13890, .T. ) ;
#14853=LINE ( 'NONE', #48617, #22978 ) ;
#14854=DIRECTION ( 'NONE',  ( -3.071710424422018668E-17, 6.404604876783312462E-16, 1.000000000000000000 ) ) ;
#14857=ORIENTED_EDGE ( 'NONE', *, *, #4048, .F. ) ;
#14867=AXIS2_PLACEMENT_3D ( 'NONE', #8496, #23524, #4806 ) ;
#14870=ORIENTED_EDGE ( 'NONE', *, *, #28419, .F. ) ;
#14881=ORIENTED_EDGE ( 'NONE', *, *, #24428, .F. ) ;
#14894=EDGE_CURVE ( 'NONE', #30011, #42667, #2677, .T. ) ;
#14895=EDGE_CURVE ( 'NONE', #26989, #19312, #6124, .T. ) ;
#14905=DIRECTION ( 'NONE',  ( -3.071710424422018668E-17, 6.404604876783312462E-16, 1.000000000000000000 ) ) ;
#14907=ORIENTED_EDGE ( 'NONE', *, *, #23883, .F. ) ;
#14911=DIRECTION ( 'NONE',  ( -3.071710424422018668E-17, 6.404604876783312462E-16, 1.000000000000000000 ) ) ;
#14914=EDGE_LOOP ( 'NONE', ( #41194, #25932, #43235, #14126 ) ) ;
#14931=CARTESIAN_POINT ( 'NONE',  ( -15.59410181515468530, -19.12364873146922051, 49.52966884056656482 ) ) ;
#14934=ORIENTED_EDGE ( 'NONE', *, *, #36083, .T. ) ;
#14944=AXIS2_PLACEMENT_3D ( 'NONE', #14157, #40524, #47680 ) ;
#14945=VERTEX_POINT ( 'NONE', #47508 ) ;
#14963=VERTEX_POINT ( 'NONE', #14452 ) ;
#14973=DIRECTION ( 'NONE',  ( -0.9687793358424819923, 0.2479245821708680464, 0.000000000000000000 ) ) ;
#14984=VECTOR ( 'NONE', #33398, 1000.000000000000000 ) ;
#14986=CIRCLE ( 'NONE', #38630, 2.000000000000001332 ) ;
#14997=ORIENTED_EDGE ( 'NONE', *, *, #22427, .T. ) ;
#15006=EDGE_CURVE ( 'NONE', #9620, #11090, #28130, .T. ) ;
#15008=CARTESIAN_POINT ( 'NONE',  ( -12.74909871793134997, -15.13738746211001462, 49.52966884056655772 ) ) ;
#15014=CARTESIAN_POINT ( 'NONE',  ( -17.42409385541299471, -14.80920654474435771, 49.52966884056655772 ) ) ;
#15023=CIRCLE ( 'NONE', #15809, 5.249999999999998224 ) ;
#15029=ORIENTED_EDGE ( 'NONE', *, *, #30425, .F. ) ;
#15036=AXIS2_PLACEMENT_3D ( 'NONE', #45198, #11439, #20295 ) ;
#15045=ADVANCED_FACE ( 'NONE', ( #26804 ), #7119, .T. ) ;
#15058=ORIENTED_EDGE ( 'NONE', *, *, #6005, .T. ) ;
#15061=CIRCLE ( 'NONE', #30032, 5.249999999999998224 ) ;
#15068=VERTEX_POINT ( 'NONE', #7857 ) ;
#15070=CIRCLE ( 'NONE', #22165, 2.000000000000000888 ) ;
#15077=CARTESIAN_POINT ( 'NONE',  ( -17.42409385541299471, -14.80920654474435771, 49.52966884056655772 ) ) ;
#15086=DIRECTION ( 'NONE',  ( -3.071710424422018668E-17, 6.404604876783312462E-16, 1.000000000000000000 ) ) ;
#15089=FACE_OUTER_BOUND ( 'NONE', #33454, .T. ) ;
#15091=DIRECTION ( 'NONE',  ( -3.071710424422018668E-17, 6.404604876783312462E-16, 1.000000000000000000 ) ) ;
#15109=ORIENTED_EDGE ( 'NONE', *, *, #11058, .T. ) ;
#15114=DIRECTION ( 'NONE',  ( -3.071710424422018668E-17, 6.404604876783312462E-16, 1.000000000000000000 ) ) ;
#15120=FACE_OUTER_BOUND ( 'NONE', #20843, .T. ) ;
#15123=EDGE_CURVE ( 'NONE', #10945, #10797, #13965, .T. ) ;
#15135=CARTESIAN_POINT ( 'NONE',  ( -17.42409385541299471, -14.80920654474435771, 49.52966884056655772 ) ) ;
#15149=CARTESIAN_POINT ( 'NONE',  ( -17.42409385541299471, -14.80920654474435594, 52.02966884056656482 ) ) ;
#15155=CARTESIAN_POINT ( 'NONE',  ( -17.42409385541299471, -14.80920654474435594, 52.02966884056656482 ) ) ;
#15156=ORIENTED_EDGE ( 'NONE', *, *, #48131, .F. ) ;
#15164=ORIENTED_EDGE ( 'NONE', *, *, #38391, .T. ) ;
#15180=VERTEX_POINT ( 'NONE', #5363 ) ;
#15194=ADVANCED_FACE ( 'NONE', ( #36346 ), #40302, .T. ) ;
#15198=CARTESIAN_POINT ( 'NONE',  ( -21.73853604213786639, -16.63919858500264937, 52.02966884056656482 ) ) ;
#15218=VECTOR ( 'NONE', #16058, 1000.000000000000000 ) ;
#15226=LINE ( 'NONE', #31001, #12447 ) ;
#15233=CARTESIAN_POINT ( 'NONE',  ( -14.36038767613011302, -18.37140530287405227, 52.02966884056656482 ) ) ;
#15238=LINE ( 'NONE', #44831, #15843 ) ;
#15243=AXIS2_PLACEMENT_3D ( 'NONE', #6530, #40017, #36533 ) ;
#15257=DIRECTION ( 'NONE',  ( -3.071710424422018668E-17, 6.404604876783312462E-16, 1.000000000000000000 ) ) ;
#15270=DIRECTION ( 'NONE',  ( -3.071710424422018668E-17, 6.404604876783312462E-16, 1.000000000000000000 ) ) ;
#15286=CIRCLE ( 'NONE', #12179, 2.000000000000001332 ) ;
#15287=DIRECTION ( 'NONE',  ( -3.071710424422018668E-17, 6.404604876783312462E-16, 1.000000000000000000 ) ) ;
#15301=CARTESIAN_POINT ( 'NONE',  ( -17.42409385541299471, -14.80920654474435594, 52.02966884056656482 ) ) ;
#15306=CARTESIAN_POINT ( 'NONE',  ( -18.24684318355141599, -9.624075539355219533, 50.77966884056655772 ) ) ;
#15316=FACE_OUTER_BOUND ( 'NONE', #40023, .T. ) ;
#15323=EDGE_CURVE ( 'NONE', #3327, #44193, #46672, .T. ) ;
#15329=DIRECTION ( 'NONE',  ( -3.071710424422018668E-17, 6.404604876783312462E-16, 1.000000000000000000 ) ) ;
#15339=CYLINDRICAL_SURFACE ( 'NONE', #12690, 2.000000000000001776 ) ;
#15347=ORIENTED_EDGE ( 'NONE', *, *, #36521, .T. ) ;
#15350=CARTESIAN_POINT ( 'NONE',  ( -17.01690395770326347, -19.47798354061844961, 49.52966884056656482 ) ) ;
#15351=EDGE_CURVE ( 'NONE', #15973, #42844, #30690, .T. ) ;
#15356=AXIS2_PLACEMENT_3D ( 'NONE', #25850, #22166, #29058 ) ;
#15360=DIRECTION ( 'NONE',  ( 0.9687793358424821033, -0.2479245821708680464, 0.000000000000000000 ) ) ;
#15362=EDGE_CURVE ( 'NONE', #8151, #39153, #45477, .T. ) ;
#15367=ORIENTED_EDGE ( 'NONE', *, *, #46303, .F. ) ;
#15374=DIRECTION ( 'NONE',  ( 3.071710424422018668E-17, -6.404604876783312462E-16, -1.000000000000000000 ) ) ;
#15379=ORIENTED_EDGE ( 'NONE', *, *, #19282, .F. ) ;
#15396=EDGE_CURVE ( 'NONE', #19337, #26266, #33657, .T. ) ;
#15399=CARTESIAN_POINT ( 'NONE',  ( -22.46373187589079379, -16.28044704940516496, 50.77966884056655772 ) ) ;
#15424=DIRECTION ( 'NONE',  ( 3.071710424422018668E-17, -6.404604876783312462E-16, -1.000000000000000000 ) ) ;
#15426=VERTEX_POINT ( 'NONE', #40003 ) ;
#15427=FACE_OUTER_BOUND ( 'NONE', #43975, .T. ) ;
#15429=CARTESIAN_POINT ( 'NONE',  ( -13.97958029355460852, -17.98703734140009303, 49.52966884056656482 ) ) ;
#15434=LINE ( 'NONE', #7605, #18898 ) ;
#15438=ORIENTED_EDGE ( 'NONE', *, *, #38567, .T. ) ;
#15441=VERTEX_POINT ( 'NONE', #6272 ) ;
#15449=DIRECTION ( 'NONE',  ( -3.071710424422018668E-17, 6.404604876783312462E-16, 1.000000000000000000 ) ) ;
#15450=VERTEX_POINT ( 'NONE', #9496 ) ;
#15453=AXIS2_PLACEMENT_3D ( 'NONE', #12334, #13045, #28076 ) ;
#15459=VERTEX_POINT ( 'NONE', #47874 ) ;
#15460=ORIENTED_EDGE ( 'NONE', *, *, #19326, .F. ) ;
#15468=DIRECTION ( 'NONE',  ( -3.071710424422018668E-17, 6.404604876783312462E-16, 1.000000000000000000 ) ) ;
#15480=CARTESIAN_POINT ( 'NONE',  ( -21.32332200014554857, -12.20934075487643966, 49.52966884056655772 ) ) ;
#15483=VERTEX_POINT ( 'NONE', #14108 ) ;
#15485=AXIS2_PLACEMENT_3D ( 'NONE', #38433, #15287, #22459 ) ;
#15515=VERTEX_POINT ( 'NONE', #44931 ) ;
#15517=CARTESIAN_POINT ( 'NONE',  ( -13.60167271156757707, -11.21037387301822363, 49.52966884056655772 ) ) ;
#15528=DIRECTION ( 'NONE',  ( -3.071710424422018668E-17, 6.404604876783312462E-16, 1.000000000000000000 ) ) ;
#15535=CARTESIAN_POINT ( 'NONE',  ( -20.98629261354270170, -17.87291272402722342, 52.02966884056656482 ) ) ;
#15546=CARTESIAN_POINT ( 'NONE',  ( -17.42409385541299471, -14.80920654474435771, 49.52966884056655772 ) ) ;
#15558=CIRCLE ( 'NONE', #47848, 2.000000000000001332 ) ;
#15559=ORIENTED_EDGE ( 'NONE', *, *, #26105, .F. ) ;
#15572=DIRECTION ( 'NONE',  ( 0.9687793358424821033, -0.2479245821708680464, 0.000000000000000000 ) ) ;
#15573=CARTESIAN_POINT ( 'NONE',  ( -19.25408589567127038, -10.49476435801948071, 49.52966884056655772 ) ) ;
#15579=DIRECTION ( 'NONE',  ( -3.071710424422018668E-17, 6.404604876783312462E-16, 1.000000000000000000 ) ) ;
#15592=ORIENTED_EDGE ( 'NONE', *, *, #23072, .F. ) ;
#15597=CYLINDRICAL_SURFACE ( 'NONE', #19313, 0.3999999999999978018 ) ;
#15604=ORIENTED_EDGE ( 'NONE', *, *, #34953, .F. ) ;
#15608=DIRECTION ( 'NONE',  ( 0.6380325334150259708, -0.7700094066334539633, 0.000000000000000000 ) ) ;
#15609=AXIS2_PLACEMENT_3D ( 'NONE', #18350, #37297, #44983 ) ;
#15619=ORIENTED_EDGE ( 'NONE', *, *, #8682, .F. ) ;
#15625=CYLINDRICAL_SURFACE ( 'NONE', #35161, 0.3999999999999978018 ) ;
#15628=PRODUCT_DEFINITION_FORMATION_WITH_SPECIFIED_SOURCE ( 'ANY', '', #859, .NOT_KNOWN. ) ;
#15636=AXIS2_PLACEMENT_3D ( 'NONE', #46123, #27404, #42439 ) ;
#15637=LINE ( 'NONE', #20807, #10536 ) ;
#15638=DIRECTION ( 'NONE',  ( 3.071710424422018668E-17, -6.404604876783312462E-16, -1.000000000000000000 ) ) ;
#15644=ORIENTED_EDGE ( 'NONE', *, *, #13673, .T. ) ;
#15646=AXIS2_PLACEMENT_3D ( 'NONE', #7317, #22317, #22824 ) ;
#15656=EDGE_CURVE ( 'NONE', #25645, #41118, #19288, .T. ) ;
#15669=AXIS2_PLACEMENT_3D ( 'NONE', #951, #37373, #33676 ) ;
#15677=AXIS2_PLACEMENT_3D ( 'NONE', #33883, #17467, #41042 ) ;
#15679=CARTESIAN_POINT ( 'NONE',  ( -17.42409385541299471, -14.80920654474435594, 52.02966884056656482 ) ) ;
#15688=DIRECTION ( 'NONE',  ( 3.071710424422018668E-17, -6.404604876783312462E-16, -1.000000000000000000 ) ) ;
#15692=EDGE_LOOP ( 'NONE', ( #38565, #12964, #22530, #13858 ) ) ;
#15699=VECTOR ( 'NONE', #44418, 1000.000000000000000 ) ;
#15701=DIRECTION ( 'NONE',  ( -3.071710424422018668E-17, 6.404604876783312462E-16, 1.000000000000000000 ) ) ;
#15707=CIRCLE ( 'NONE', #22846, 5.249999999999998224 ) ;
#15713=DIRECTION ( 'NONE',  ( -3.071710424422018668E-17, 6.404604876783312462E-16, 1.000000000000000000 ) ) ;
#15718=LINE ( 'NONE', #5641, #45998 ) ;
#15721=EDGE_CURVE ( 'NONE', #26463, #20224, #15825, .T. ) ;
#15727=ORIENTED_EDGE ( 'NONE', *, *, #20472, .F. ) ;
#15729=LINE ( 'NONE', #26593, #43789 ) ;
#15757=LINE ( 'NONE', #23413, #31596 ) ;
#15758=DIRECTION ( 'NONE',  ( 0.9687793358424817702, -0.2479245821708686570, 0.000000000000000000 ) ) ;
#15764=CARTESIAN_POINT ( 'NONE',  ( -15.80316865820435446, -9.815700611529287301, 49.52966884056655772 ) ) ;
#15782=VERTEX_POINT ( 'NONE', #39697 ) ;
#15798=AXIS2_PLACEMENT_3D ( 'NONE', #16148, #34384, #8546 ) ;
#15802=DIRECTION ( 'NONE',  ( -3.071710424422018668E-17, 6.404604876783312462E-16, 1.000000000000000000 ) ) ;
#15809=AXIS2_PLACEMENT_3D ( 'NONE', #9657, #35492, #31808 ) ;
#15820=CIRCLE ( 'NONE', #140, 1.999999999999999556 ) ;
#15822=CARTESIAN_POINT ( 'NONE',  ( -21.50966673221228120, -17.12947588552333045, 52.02966884056656482 ) ) ;
#15825=LINE ( 'NONE', #34293, #1404 ) ;
#15843=VECTOR ( 'NONE', #14730, 1000.000000000000000 ) ;
#15846=DIRECTION ( 'NONE',  ( 0.9687793358424821033, -0.2479245821708680464, 0.000000000000000000 ) ) ;
#15850=DIRECTION ( 'NONE',  ( -3.071710424422018668E-17, 6.404604876783312462E-16, 1.000000000000000000 ) ) ;
#15857=AXIS2_PLACEMENT_3D ( 'NONE', #41741, #23038, #23766 ) ;
#15861=EDGE_CURVE ( 'NONE', #39071, #29156, #47092, .T. ) ;
#15867=DIRECTION ( 'NONE',  ( 3.071710424422018668E-17, -6.404604876783312462E-16, -1.000000000000000000 ) ) ;
#15869=EDGE_CURVE ( 'NONE', #13117, #15068, #30087, .T. ) ;
#15872=FACE_OUTER_BOUND ( 'NONE', #27751, .T. ) ;
#15893=ORIENTED_EDGE ( 'NONE', *, *, #45664, .T. ) ;
#15911=DIRECTION ( 'NONE',  ( -3.071710424422018668E-17, 6.404604876783312462E-16, 1.000000000000000000 ) ) ;
#15920=DIRECTION ( 'NONE',  ( -3.071710424422018668E-17, 6.404604876783312462E-16, 1.000000000000000000 ) ) ;
#15931=ADVANCED_FACE ( 'NONE', ( #21706 ), #14765, .T. ) ;
#15938=DIRECTION ( 'NONE',  ( 0.9687793358424819923, -0.2479245821708680464, 0.000000000000000000 ) ) ;
#15947=CARTESIAN_POINT ( 'NONE',  ( -21.34628024798174550, -12.22231469401973847, 52.02966884056656482 ) ) ;
#15950=ORIENTED_EDGE ( 'NONE', *, *, #26544, .F. ) ;
#15951=DIRECTION ( 'NONE',  ( -0.9180681052388980357, 0.3964226963016366789, 0.000000000000000000 ) ) ;
#15953=VERTEX_POINT ( 'NONE', #2983 ) ;
#15954=VERTEX_POINT ( 'NONE', #17992 ) ;
#15955=LINE ( 'NONE', #19914, #20448 ) ;
#15956=DIRECTION ( 'NONE',  ( -3.071710424422018668E-17, 6.404604876783312462E-16, 1.000000000000000000 ) ) ;
#15957=CARTESIAN_POINT ( 'NONE',  ( -21.44055400477819973, -12.39439182751215718, 49.52966884056655772 ) ) ;
#15973=VERTEX_POINT ( 'NONE', #16913 ) ;
#15984=FACE_OUTER_BOUND ( 'NONE', #35198, .T. ) ;
#15990=EDGE_CURVE ( 'NONE', #10407, #36695, #10105, .T. ) ;
#15993=CARTESIAN_POINT ( 'NONE',  ( -21.42170527289675164, -17.27794275993632667, 49.52966884056655772 ) ) ;
#15998=EDGE_CURVE ( 'NONE', #16885, #22869, #949, .T. ) ;
#16007=ORIENTED_EDGE ( 'NONE', *, *, #19760, .F. ) ;
#16013=CARTESIAN_POINT ( 'NONE',  ( -20.01098570613759975, -18.73139293731311383, 49.52966884056656482 ) ) ;
#16024=DIRECTION ( 'NONE',  ( -3.071710424422018668E-17, 6.404604876783312462E-16, 1.000000000000000000 ) ) ;
#16032=ORIENTED_EDGE ( 'NONE', *, *, #11511, .T. ) ;
#16038=DIRECTION ( 'NONE',  ( -3.071710424422018668E-17, 6.404604876783312462E-16, 1.000000000000000000 ) ) ;
#16040=VERTEX_POINT ( 'NONE', #16433 ) ;
#16041=CARTESIAN_POINT ( 'NONE',  ( -17.42409385541299471, -14.80920654474435771, 49.52966884056655772 ) ) ;
#16057=CARTESIAN_POINT ( 'NONE',  ( -18.67235195658554403, -19.33882101600501713, 49.52966884056656482 ) ) ;
#16058=DIRECTION ( 'NONE',  ( -3.071710424422018668E-17, 6.404604876783312462E-16, 1.000000000000000000 ) ) ;
#16073=VERTEX_POINT ( 'NONE', #34910 ) ;
#16132=ORIENTED_EDGE ( 'NONE', *, *, #13890, .F. ) ;
#16137=FACE_OUTER_BOUND ( 'NONE', #28248, .T. ) ;
#16148=CARTESIAN_POINT ( 'NONE',  ( -12.73887154267113253, -15.16169402761809870, 52.02966884056656482 ) ) ;
#16152=ORIENTED_EDGE ( 'NONE', *, *, #12760, .F. ) ;
#16171=DIRECTION ( 'NONE',  ( 0.9294853595766542353, 0.3688590060343623911, 0.000000000000000000 ) ) ;
#16173=ORIENTED_EDGE ( 'NONE', *, *, #13543, .F. ) ;
#16188=EDGE_CURVE ( 'NONE', #35450, #12002, #44749, .T. ) ;
#16191=CYLINDRICAL_SURFACE ( 'NONE', #2366, 1.999999999999999556 ) ;
#16196=DIRECTION ( 'NONE',  ( 3.071710424422018668E-17, -6.404604876783312462E-16, -1.000000000000000000 ) ) ;
#16214=ORIENTED_EDGE ( 'NONE', *, *, #550, .T. ) ;
#16215=DIRECTION ( 'NONE',  ( -3.071710424422018668E-17, 6.404604876783312462E-16, 1.000000000000000000 ) ) ;
#16221=ORIENTED_EDGE ( 'NONE', *, *, #34838, .F. ) ;
#16233=CIRCLE ( 'NONE', #39845, 2.000000000000001776 ) ;
#16235=CARTESIAN_POINT ( 'NONE',  ( -18.53667165497532920, -10.24437071140730993, 52.02966884056656482 ) ) ;
#16252=CARTESIAN_POINT ( 'NONE',  ( -17.07160637253920044, -10.12398423200249731, 49.52966884056655772 ) ) ;
#16253=CYLINDRICAL_SURFACE ( 'NONE', #24739, 5.249999999999998224 ) ;
#16255=ORIENTED_EDGE ( 'NONE', *, *, #7501, .F. ) ;
#16262=EDGE_CURVE ( 'NONE', #38614, #9358, #12484, .T. ) ;
#16263=EDGE_LOOP ( 'NONE', ( #8338, #30862, #43426, #37071 ) ) ;
#16266=AXIS2_PLACEMENT_3D ( 'NONE', #17294, #9204, #24224 ) ;
#16269=ORIENTED_EDGE ( 'NONE', *, *, #2131, .T. ) ;
#16294=EDGE_CURVE ( 'NONE', #31052, #34094, #37599, .T. ) ;
#16299=CIRCLE ( 'NONE', #19482, 1.999999999999999556 ) ;
#16309=DIRECTION ( 'NONE',  ( 3.071710424422018668E-17, -6.404604876783312462E-16, -1.000000000000000000 ) ) ;
#16321=CARTESIAN_POINT ( 'NONE',  ( -17.42409385541299471, -14.80920654474438614, 2.029618040566568027 ) ) ;
#16326=CARTESIAN_POINT ( 'NONE',  ( -14.51911023200684703, -18.48675360735851925, 52.02966884056656482 ) ) ;
#16333=EDGE_CURVE ( 'NONE', #10419, #22869, #34477, .T. ) ;
#16347=EDGE_CURVE ( 'NONE', #33723, #16869, #16380, .T. ) ;
#16358=EDGE_CURVE ( 'NONE', #16476, #45570, #28922, .T. ) ;
#16370=CIRCLE ( 'NONE', #17126, 5.249999999999998224 ) ;
#16375=AXIS2_PLACEMENT_3D ( 'NONE', #48481, #32962, #10351 ) ;
#16380=CIRCLE ( 'NONE', #14000, 4.686499999999998778 ) ;
#16385=ORIENTED_EDGE ( 'NONE', *, *, #8880, .F. ) ;
#16401=VERTEX_POINT ( 'NONE', #35814 ) ;
#16416=AXIS2_PLACEMENT_3D ( 'NONE', #47800, #2737, #40645 ) ;
#16427=CARTESIAN_POINT ( 'NONE',  ( -17.42409385541299471, -14.80920654474435594, 52.02966884056656482 ) ) ;
#16433=CARTESIAN_POINT ( 'NONE',  ( -20.50876352152089765, -19.05741946913900620, 49.52966884056656482 ) ) ;
#16435=ORIENTED_EDGE ( 'NONE', *, *, #12216, .F. ) ;
#16436=CARTESIAN_POINT ( 'NONE',  ( -17.42409385541299471, -14.80920654474435771, 49.52966884056655772 ) ) ;
#16443=AXIS2_PLACEMENT_3D ( 'NONE', #20274, #14905, #1553 ) ;
#16450=CIRCLE ( 'NONE', #21981, 2.000000000000001776 ) ;
#16464=CARTESIAN_POINT ( 'NONE',  ( -13.02585106727260822, -13.15662797718154309, 49.52966884056655772 ) ) ;
#16476=VERTEX_POINT ( 'NONE', #17347 ) ;
#16486=EDGE_LOOP ( 'NONE', ( #27549, #3612, #14707, #42929 ) ) ;
#16496=CARTESIAN_POINT ( 'NONE',  ( -13.17588093101833557, -17.89387621085224467, 52.02966884056656482 ) ) ;
#16503=ORIENTED_EDGE ( 'NONE', *, *, #8626, .T. ) ;
#16515=AXIS2_PLACEMENT_3D ( 'NONE', #48584, #14817, #8697 ) ;
#16535=CARTESIAN_POINT ( 'NONE',  ( -13.40763370604777371, -17.22402126197653160, 49.52966884056655772 ) ) ;
#16543=ADVANCED_FACE ( 'NONE', ( #22770 ), #25712, .T. ) ;
#16548=VECTOR ( 'NONE', #41063, 1000.000000000000000 ) ;
#16549=DIRECTION ( 'NONE',  ( -0.9687793358424819923, 0.2479245821708680464, 0.000000000000000000 ) ) ;
#16562=AXIS2_PLACEMENT_3D ( 'NONE', #13954, #36607, #44517 ) ;
#16571=CIRCLE ( 'NONE', #40166, 4.686499999999997890 ) ;
#16579=ORIENTED_EDGE ( 'NONE', *, *, #36329, .F. ) ;
#16583=AXIS2_PLACEMENT_3D ( 'NONE', #36354, #29225, #21113 ) ;
#16584=DIRECTION ( 'NONE',  ( -3.071710424422018668E-17, 6.404604876783312462E-16, 1.000000000000000000 ) ) ;
#16585=ADVANCED_FACE ( 'NONE', ( #48356 ), #7507, .T. ) ;
#16594=ORIENTED_EDGE ( 'NONE', *, *, #18084, .F. ) ;
#16598=ORIENTED_EDGE ( 'NONE', *, *, #15869, .T. ) ;
#16630=VERTEX_POINT ( 'NONE', #12393 ) ;
#16631=CARTESIAN_POINT ( 'NONE',  ( -12.85169559483840374, -15.89028456787280952, 52.02966884056656482 ) ) ;
#16634=DIRECTION ( 'NONE',  ( -3.071710424422018668E-17, 6.404604876783312462E-16, 1.000000000000000000 ) ) ;
#16640=EDGE_LOOP ( 'NONE', ( #20738, #8058, #26763, #13072 ) ) ;
#16644=CARTESIAN_POINT ( 'NONE',  ( -17.42409385541299471, -14.80920654474435594, 52.02966884056656482 ) ) ;
#16645=DIRECTION ( 'NONE',  ( -0.7700094066334558507, -0.6380325334150235284, 0.000000000000000000 ) ) ;
#16675=CARTESIAN_POINT ( 'NONE',  ( -21.24651499925844078, -18.40803921647045982, 50.77966884056655772 ) ) ;
#16677=VERTEX_POINT ( 'NONE', #38489 ) ;
#16679=CARTESIAN_POINT ( 'NONE',  ( -14.25548580596218429, -11.33998781794830712, 49.52966884056655772 ) ) ;
#16680=ORIENTED_EDGE ( 'NONE', *, *, #1716, .T. ) ;
#16728=DIRECTION ( 'NONE',  ( 0.9687793358424817702, -0.2479245821708688791, 0.000000000000000000 ) ) ;
#16742=DIRECTION ( 'NONE',  ( -0.9956360040033418457, 0.09332174201255234725, 0.000000000000000000 ) ) ;
#16749=DIRECTION ( 'NONE',  ( 0.9687793358424821033, -0.2479245821708677133, 0.000000000000000000 ) ) ;
#16768=AXIS2_PLACEMENT_3D ( 'NONE', #3589, #36817, #6804 ) ;
#16770=DIRECTION ( 'NONE',  ( -3.071710424422018668E-17, 6.404604876783312462E-16, 1.000000000000000000 ) ) ;
#16775=DIRECTION ( 'NONE',  ( -0.3964226963016464489, -0.9180681052388938168, 0.000000000000000000 ) ) ;
#16788=ORIENTED_EDGE ( 'NONE', *, *, #28481, .T. ) ;
#16794=CARTESIAN_POINT ( 'NONE',  ( -22.10677449762105340, -15.19398901379252820, 49.52966884056655772 ) ) ;
#16812=CARTESIAN_POINT ( 'NONE',  ( -17.42409385541299471, -14.80920654474435771, 49.52966884056655772 ) ) ;
#16850=DIRECTION ( 'NONE',  ( -3.071710424422018668E-17, 6.404604876783312462E-16, 1.000000000000000000 ) ) ;
#16859=EDGE_LOOP ( 'NONE', ( #9296, #23649, #48029, #36342 ) ) ;
#16860=CARTESIAN_POINT ( 'NONE',  ( -17.42409385541299471, -14.80920654474435771, 49.52966884056655772 ) ) ;
#16863=ORIENTED_EDGE ( 'NONE', *, *, #34258, .T. ) ;
#16869=VERTEX_POINT ( 'NONE', #45122 ) ;
#16885=VERTEX_POINT ( 'NONE', #42389 ) ;
#16893=ADVANCED_FACE ( 'NONE', ( #4715 ), #19736, .T. ) ;
#16897=FACE_OUTER_BOUND ( 'NONE', #27219, .T. ) ;
#16900=AXIS2_PLACEMENT_3D ( 'NONE', #30950, #11745, #42270 ) ;
#16911=DIRECTION ( 'NONE',  ( -3.071710424422018668E-17, 6.404604876783312462E-16, 1.000000000000000000 ) ) ;
#16913=CARTESIAN_POINT ( 'NONE',  ( -12.74698474939898318, -12.42443183621509917, 52.02966884056656482 ) ) ;
#16931=DIRECTION ( 'NONE',  ( -3.071710424422018668E-17, 6.404604876783312462E-16, 1.000000000000000000 ) ) ;
#16934=CARTESIAN_POINT ( 'NONE',  ( -17.42409385541299471, -14.80920654474434883, 62.02966884056656482 ) ) ;
#16951=EDGE_CURVE ( 'NONE', #13117, #1942, #35295, .T. ) ;
#16958=EDGE_CURVE ( 'NONE', #27154, #32100, #42704, .T. ) ;
#16968=AXIS2_PLACEMENT_3D ( 'NONE', #31011, #37649, #46032 ) ;
#16969=CYLINDRICAL_SURFACE ( 'NONE', #35331, 4.686499999999997002 ) ;
#16978=DIRECTION ( 'NONE',  ( -0.9294853595766571219, -0.3688590060343552857, 0.000000000000000000 ) ) ;
#16988=ORIENTED_EDGE ( 'NONE', *, *, #45968, .F. ) ;
#16995=FACE_OUTER_BOUND ( 'NONE', #48392, .T. ) ;
#17001=CARTESIAN_POINT ( 'NONE',  ( -19.07667242297576138, -10.41096375660395168, 49.52966884056655772 ) ) ;
#17012=ADVANCED_FACE ( 'NONE', ( #846 ), #38245, .T. ) ;
#17017=CARTESIAN_POINT ( 'NONE',  ( -13.84085632603101956, -17.84827948783496865, 52.02966884056656482 ) ) ;
#17018=DIRECTION ( 'NONE',  ( -0.7700094066334558507, -0.6380325334150236394, 0.000000000000000000 ) ) ;
#17024=EDGE_CURVE ( 'NONE', #28884, #35750, #28237, .T. ) ;
#17045=ORIENTED_EDGE ( 'NONE', *, *, #12180, .T. ) ;
#17068=DIRECTION ( 'NONE',  ( -3.071710424422018668E-17, 6.404604876783312462E-16, 1.000000000000000000 ) ) ;
#17070=AXIS2_PLACEMENT_3D ( 'NONE', #47701, #13939, #10287 ) ;
#17071=ORIENTED_EDGE ( 'NONE', *, *, #35262, .T. ) ;
#17078=AXIS2_PLACEMENT_3D ( 'NONE', #8502, #1842, #39018 ) ;
#17099=DIRECTION ( 'NONE',  ( 0.9687793358424821033, -0.2479245821708680464, 0.000000000000000000 ) ) ;
#17101=VERTEX_POINT ( 'NONE', #13358 ) ;
#17104=AXIS2_PLACEMENT_3D ( 'NONE', #24792, #17383, #46715 ) ;
#17105=CARTESIAN_POINT ( 'NONE',  ( -17.42409385541299471, -14.80920654474435594, 52.02966884056656482 ) ) ;
#17109=CIRCLE ( 'NONE', #35987, 4.686499999999998778 ) ;
#17126=AXIS2_PLACEMENT_3D ( 'NONE', #5796, #6269, #36045 ) ;
#17128=AXIS2_PLACEMENT_3D ( 'NONE', #29908, #44940, #44444 ) ;
#17129=CARTESIAN_POINT ( 'NONE',  ( -16.44703096029287437, -9.650926977002853846, 52.02966884056656482 ) ) ;
#17133=AXIS2_PLACEMENT_3D ( 'NONE', #41574, #41321, #33417 ) ;
#17134=CIRCLE ( 'NONE', #12452, 5.249999999999998224 ) ;
#17137=CARTESIAN_POINT ( 'NONE',  ( -15.65212752116712558, -9.867280269464723474, 50.77966884056655772 ) ) ;
#17146=AXIS2_PLACEMENT_3D ( 'NONE', #33876, #3860, #6576 ) ;
#17147=EDGE_CURVE ( 'NONE', #23374, #38177, #34516, .T. ) ;
#17149=CYLINDRICAL_SURFACE ( 'NONE', #10937, 4.686499999999997002 ) ;
#17155=ORIENTED_EDGE ( 'NONE', *, *, #17808, .T. ) ;
#17157=DIRECTION ( 'NONE',  ( -3.071710424422018668E-17, 6.404604876783312462E-16, 1.000000000000000000 ) ) ;
#17174=DIRECTION ( 'NONE',  ( 0.9687793358424821033, -0.2479245821708677133, 0.000000000000000000 ) ) ;
#17182=FACE_OUTER_BOUND ( 'NONE', #11563, .T. ) ;
#17198=DIRECTION ( 'NONE',  ( 3.071710424422018668E-17, -6.404604876783312462E-16, -1.000000000000000000 ) ) ;
#17203=ORIENTED_EDGE ( 'NONE', *, *, #44963, .T. ) ;
#17219=DIRECTION ( 'NONE',  ( -3.071710424422018668E-17, 6.404604876783312462E-16, 1.000000000000000000 ) ) ;
#17227=CARTESIAN_POINT ( 'NONE',  ( -17.42409385541299471, -14.80920654474435771, 49.52966884056655772 ) ) ;
#17228=VECTOR ( 'NONE', #19596, 1000.000000000000000 ) ;
#17240=ADVANCED_FACE ( 'NONE', ( #44392 ), #22220, .T. ) ;
#17244=EDGE_CURVE ( 'NONE', #14076, #1460, #42414, .T. ) ;
#17246=AXIS2_PLACEMENT_3D ( 'NONE', #11036, #15867, #3641 ) ;
#17253=CARTESIAN_POINT ( 'NONE',  ( -12.87649578556737318, -13.67667219862661021, 49.52966884056655772 ) ) ;
#17270=DIRECTION ( 'NONE',  ( -3.071710424422018668E-17, 6.404604876783312462E-16, 1.000000000000000000 ) ) ;
#17281=EDGE_LOOP ( 'NONE', ( #43349, #47082, #24845, #34453 ) ) ;
#17294=CARTESIAN_POINT ( 'NONE',  ( -17.42409385541299471, -14.80920654474435771, 49.52966884056655772 ) ) ;
#17297=DIRECTION ( 'NONE',  ( -0.9687793358424822143, 0.2479245821708672415, 0.000000000000000000 ) ) ;
#17316=ORIENTED_EDGE ( 'NONE', *, *, #32718, .F. ) ;
#17319=ORIENTED_EDGE ( 'NONE', *, *, #31986, .F. ) ;
#17327=LINE ( 'NONE', #9236, #17553 ) ;
#17328=ADVANCED_FACE ( 'NONE', ( #14521 ), #21709, .T. ) ;
#17339=CARTESIAN_POINT ( 'NONE',  ( -17.42409385541299471, -14.80920654474435771, 49.52966884056655772 ) ) ;
#17347=CARTESIAN_POINT ( 'NONE',  ( -22.63183829035100914, -15.47396055967929129, 49.52966884056655772 ) ) ;
#17348=FACE_OUTER_BOUND ( 'NONE', #803, .T. ) ;
#17349=VERTEX_POINT ( 'NONE', #4453 ) ;
#17351=DIRECTION ( 'NONE',  ( -3.071710424422018668E-17, 6.404604876783312462E-16, 1.000000000000000000 ) ) ;
#17381=ORIENTED_EDGE ( 'NONE', *, *, #5542, .F. ) ;
#17383=DIRECTION ( 'NONE',  ( -3.071710424422018668E-17, 6.404604876783312462E-16, 1.000000000000000000 ) ) ;
#17388=DIRECTION ( 'NONE',  ( -0.3964226963016471150, -0.9180681052388935948, 0.000000000000000000 ) ) ;
#17389=FACE_OUTER_BOUND ( 'NONE', #25770, .T. ) ;
#17397=CARTESIAN_POINT ( 'NONE',  ( -13.86189509728330904, -11.74550036546146004, 49.52966884056655772 ) ) ;
#17399=VERTEX_POINT ( 'NONE', #15764 ) ;
#17406=PRODUCT_DEFINITION_CONTEXT ( 'detailed design', #39771, 'design' ) ;
#17416=CARTESIAN_POINT ( 'NONE',  ( -19.94733193681641481, -19.41309290135173526, 52.02966884056656482 ) ) ;
#17431=CYLINDRICAL_SURFACE ( 'NONE', #29927, 2.000000000000000000 ) ;
#17443=CIRCLE ( 'NONE', #24538, 5.249999999999998224 ) ;
#17444=EDGE_CURVE ( 'NONE', #30955, #10419, #6244, .T. ) ;
#17445=ORIENTED_EDGE ( 'NONE', *, *, #12111, .T. ) ;
#17452=VERTEX_POINT ( 'NONE', #31530 ) ;
#17454=VERTEX_POINT ( 'NONE', #31049 ) ;
#17460=CIRCLE ( 'NONE', #37099, 4.686499999999999666 ) ;
#17467=DIRECTION ( 'NONE',  ( -3.071710424422018668E-17, 6.404604876783312462E-16, 1.000000000000000000 ) ) ;
#17475=DIRECTION ( 'NONE',  ( -3.071710424422018668E-17, 6.404604876783312462E-16, 1.000000000000000000 ) ) ;
#17484=DIRECTION ( 'NONE',  ( -3.071710424422018668E-17, 6.404604876783312462E-16, 1.000000000000000000 ) ) ;
#17487=ORIENTED_EDGE ( 'NONE', *, *, #20258, .T. ) ;
#17496=ORIENTED_EDGE ( 'NONE', *, *, #6406, .T. ) ;
#17503=ORIENTED_EDGE ( 'NONE', *, *, #1268, .T. ) ;
#17514=DIRECTION ( 'NONE',  ( 3.071710424422018668E-17, -6.404604876783312462E-16, -1.000000000000000000 ) ) ;
#17526=ORIENTED_EDGE ( 'NONE', *, *, #40542, .T. ) ;
#17542=ORIENTED_EDGE ( 'NONE', *, *, #3955, .T. ) ;
#17553=VECTOR ( 'NONE', #20312, 1000.000000000000000 ) ;
#17555=ADVANCED_FACE ( 'NONE', ( #12806, #35685 ), #24147, .F. ) ;
#17556=CARTESIAN_POINT ( 'NONE',  ( -13.88631413956031579, -11.73554473314221980, 52.02966884056656482 ) ) ;
#17561=VERTEX_POINT ( 'NONE', #28068 ) ;
#17563=DIRECTION ( 'NONE',  ( -3.071710424422018668E-17, 6.404604876783312462E-16, 1.000000000000000000 ) ) ;
#17572=CYLINDRICAL_SURFACE ( 'NONE', #26043, 1.999999999999999112 ) ;
#17578=ADVANCED_FACE ( 'NONE', ( #24639 ), #16969, .T. ) ;
#17580=DIRECTION ( 'NONE',  ( -3.071710424422018668E-17, 6.404604876783312462E-16, 1.000000000000000000 ) ) ;
#17593=ORIENTED_EDGE ( 'NONE', *, *, #35262, .F. ) ;
#17596=DIRECTION ( 'NONE',  ( -3.071710424422018668E-17, 6.404604876783312462E-16, 1.000000000000000000 ) ) ;
#17605=VECTOR ( 'NONE', #22214, 1000.000000000000000 ) ;
#17614=LINE ( 'NONE', #28715, #36672 ) ;
#17619=DIRECTION ( 'NONE',  ( -3.071710424422018668E-17, 6.404604876783312462E-16, 1.000000000000000000 ) ) ;
#17622=CARTESIAN_POINT ( 'NONE',  ( -17.94839601134439633, -19.47832453368858552, 49.52966884056656482 ) ) ;
#17623=EDGE_LOOP ( 'NONE', ( #33089, #39926, #9080, #27133 ) ) ;
#17632=EDGE_CURVE ( 'NONE', #9114, #22244, #29287, .T. ) ;
#17634=CARTESIAN_POINT ( 'NONE',  ( -12.91230480768039790, -16.07689808402359333, 52.02966884056656482 ) ) ;
#17651=EDGE_CURVE ( 'NONE', #45860, #42513, #18845, .T. ) ;
#17669=ORIENTED_EDGE ( 'NONE', *, *, #25101, .F. ) ;
#17674=EDGE_LOOP ( 'NONE', ( #46743, #10199, #6630, #35741 ) ) ;
#17678=AXIS2_PLACEMENT_3D ( 'NONE', #7806, #22821, #34116 ) ;
#17679=CYLINDRICAL_SURFACE ( 'NONE', #8450, 2.000000000000001332 ) ;
#17683=CARTESIAN_POINT ( 'NONE',  ( -17.42409385541299471, -14.80920654474435594, 52.02966884056656482 ) ) ;
#17700=EDGE_LOOP ( 'NONE', ( #23645, #13269, #42321, #31472 ) ) ;
#17701=ORIENTED_EDGE ( 'NONE', *, *, #34000, .T. ) ;
#17702=EDGE_CURVE ( 'NONE', #2342, #6917, #21205, .T. ) ;
#17711=CIRCLE ( 'NONE', #36569, 2.000000000000001776 ) ;
#17716=DIRECTION ( 'NONE',  ( -3.071710424422018668E-17, 6.404604876783312462E-16, 1.000000000000000000 ) ) ;
#17734=CIRCLE ( 'NONE', #16968, 4.686499999999998778 ) ;
#17735=ORIENTED_EDGE ( 'NONE', *, *, #18378, .T. ) ;
#17759=DIRECTION ( 'NONE',  ( 3.071710424422018668E-17, -6.404604876783312462E-16, -1.000000000000000000 ) ) ;
#17761=CARTESIAN_POINT ( 'NONE',  ( -17.42409385541299471, -14.80920654474435771, 49.52966884056655772 ) ) ;
#17775=CARTESIAN_POINT ( 'NONE',  ( -16.89979169948162863, -10.14008855580012636, 49.52966884056655772 ) ) ;
#17782=AXIS2_PLACEMENT_3D ( 'NONE', #940, #45528, #15938 ) ;
#17797=FACE_OUTER_BOUND ( 'NONE', #43376, .T. ) ;
#17808=EDGE_CURVE ( 'NONE', #24396, #47392, #5471, .T. ) ;
#17811=AXIS2_PLACEMENT_3D ( 'NONE', #26473, #34329, #19572 ) ;
#17815=DIRECTION ( 'NONE',  ( -3.071710424422018668E-17, 6.404604876783312462E-16, 1.000000000000000000 ) ) ;
#17820=DIRECTION ( 'NONE',  ( -3.071710424422018668E-17, 6.404604876783312462E-16, 1.000000000000000000 ) ) ;
#17833=EDGE_LOOP ( 'NONE', ( #17319, #27472, #25798, #5159 ) ) ;
#17836=DIRECTION ( 'NONE',  ( 0.7506333037770493988, -0.6607190350373991494, 0.000000000000000000 ) ) ;
#17845=DIRECTION ( 'NONE',  ( -3.071710424422018668E-17, 6.404604876783312462E-16, 1.000000000000000000 ) ) ;
#17861=DIRECTION ( 'NONE',  ( 0.9956360040033426229, -0.09332174201254497814, 0.000000000000000000 ) ) ;
#17880=ORIENTED_EDGE ( 'NONE', *, *, #45811, .T. ) ;
#17881=DIRECTION ( 'NONE',  ( -3.071710424422018668E-17, 6.404604876783312462E-16, 1.000000000000000000 ) ) ;
#17883=VECTOR ( 'NONE', #41833, 1000.000000000000000 ) ;
#17884=CYLINDRICAL_SURFACE ( 'NONE', #41598, 1.999999999999999112 ) ;
#17887=CARTESIAN_POINT ( 'NONE',  ( -17.42409385541299471, -14.80920654474434883, 62.02966884056656482 ) ) ;
#17888=DIRECTION ( 'NONE',  ( -3.071710424422018668E-17, 6.404604876783312462E-16, 1.000000000000000000 ) ) ;
#17889=AXIS2_PLACEMENT_3D ( 'NONE', #20271, #30643, #35275 ) ;
#17890=ORIENTED_EDGE ( 'NONE', *, *, #31715, .F. ) ;
#17905=DIRECTION ( 'NONE',  ( 0.9687793358424822143, -0.2479245821708672415, 0.000000000000000000 ) ) ;
#17910=AXIS2_PLACEMENT_3D ( 'NONE', #3167, #10330, #32941 ) ;
#17919=VERTEX_POINT ( 'NONE', #2638 ) ;
#17931=CARTESIAN_POINT ( 'NONE',  ( -20.89331258220900978, -11.64059849529350643, 49.52966884056655772 ) ) ;
#17939=CARTESIAN_POINT ( 'NONE',  ( -19.38197731428664028, -19.06713733463150007, 52.02966884056656482 ) ) ;
#17942=CARTESIAN_POINT ( 'NONE',  ( -13.82526118368687484, -18.63162768858978779, 52.02966884056656482 ) ) ;
#17949=CIRCLE ( 'NONE', #41563, 5.249999999999998224 ) ;
#17957=VERTEX_POINT ( 'NONE', #47468 ) ;
#17970=CIRCLE ( 'NONE', #40008, 5.249999999999998224 ) ;
#17989=DIRECTION ( 'NONE',  ( 0.9687793358424821033, -0.2479245821708680464, 0.000000000000000000 ) ) ;
#17992=CARTESIAN_POINT ( 'NONE',  ( -22.46373187589079379, -16.28044704940516496, 52.02966884056656482 ) ) ;
#18020=CIRCLE ( 'NONE', #41628, 4.686499999999998778 ) ;
#18021=CIRCLE ( 'NONE', #15677, 5.249999999999998224 ) ;
#18025=ORIENTED_EDGE ( 'NONE', *, *, #34392, .T. ) ;
#18029=DIRECTION ( 'NONE',  ( -3.071710424422018668E-17, 6.404604876783312462E-16, 1.000000000000000000 ) ) ;
#18040=CARTESIAN_POINT ( 'NONE',  ( -18.08884787034790875, -9.601462109806339740, 49.52966884056655772 ) ) ;
#18074=EDGE_CURVE ( 'NONE', #44032, #15954, #41530, .T. ) ;
#18079=AXIS2_PLACEMENT_3D ( 'NONE', #43275, #2134, #10506 ) ;
#18084=EDGE_CURVE ( 'NONE', #18613, #35420, #18020, .T. ) ;
#18105=ORIENTED_EDGE ( 'NONE', *, *, #8966, .T. ) ;
#18115=VECTOR ( 'NONE', #4948, 1000.000000000000000 ) ;
#18117=ORIENTED_EDGE ( 'NONE', *, *, #8880, .T. ) ;
#18125=VECTOR ( 'NONE', #6122, 1000.000000000000000 ) ;
#18138=LINE ( 'NONE', #29727, #37759 ) ;
#18143=CIRCLE ( 'NONE', #45704, 2.000000000000000000 ) ;
#18165=VECTOR ( 'NONE', #7475, 1000.000000000000000 ) ;
#18171=CARTESIAN_POINT ( 'NONE',  ( -17.42409385541299471, -14.80920654474435594, 52.02966884056656482 ) ) ;
#18173=ORIENTED_EDGE ( 'NONE', *, *, #3275, .T. ) ;
#18175=VECTOR ( 'NONE', #12250, 1000.000000000000000 ) ;
#18217=ORIENTED_EDGE ( 'NONE', *, *, #23758, .F. ) ;
#18227=VERTEX_POINT ( 'NONE', #42392 ) ;
#18228=DIRECTION ( 'NONE',  ( -3.071710424422018668E-17, 6.404604876783312462E-16, 1.000000000000000000 ) ) ;
#18232=LINE ( 'NONE', #36941, #1621 ) ;
#18239=CARTESIAN_POINT ( 'NONE',  ( -17.42409385541299471, -14.80920654474435771, 49.52966884056655772 ) ) ;
#18269=ORIENTED_EDGE ( 'NONE', *, *, #26130, .T. ) ;
#18302=DIRECTION ( 'NONE',  ( 0.9687793358424821033, -0.2479245821708677133, 0.000000000000000000 ) ) ;
#18304=DIRECTION ( 'NONE',  ( -0.5351595679979681552, -0.8447509909909712844, 0.000000000000000000 ) ) ;
#18325=FACE_OUTER_BOUND ( 'NONE', #2599, .T. ) ;
#18326=DIRECTION ( 'NONE',  ( -3.071710424422018668E-17, 6.404604876783312462E-16, 1.000000000000000000 ) ) ;
#18343=DIRECTION ( 'NONE',  ( -3.071710424422018668E-17, 6.404604876783312462E-16, 1.000000000000000000 ) ) ;
#18347=ORIENTED_EDGE ( 'NONE', *, *, #20722, .T. ) ;
#18350=CARTESIAN_POINT ( 'NONE',  ( -14.49326647312025074, -18.48150914673672673, 52.02966884056656482 ) ) ;
#18373=ORIENTED_EDGE ( 'NONE', *, *, #7164, .F. ) ;
#18374=CARTESIAN_POINT ( 'NONE',  ( -12.17647495751581133, -14.96730746957505076, 50.77966884056655772 ) ) ;
#18378=EDGE_CURVE ( 'NONE', #27894, #15973, #24344, .T. ) ;
#18386=EDGE_CURVE ( 'NONE', #17101, #12756, #3085, .T. ) ;
#18388=AXIS2_PLACEMENT_3D ( 'NONE', #21231, #32069, #16549 ) ;
#18390=DIRECTION ( 'NONE',  ( -0.06357898915124172989, 0.9979768094191899808, 0.000000000000000000 ) ) ;
#18394=ORIENTED_EDGE ( 'NONE', *, *, #20722, .F. ) ;
#18402=EDGE_CURVE ( 'NONE', #19923, #4090, #2329, .T. ) ;
#18414=ORIENTED_EDGE ( 'NONE', *, *, #44587, .F. ) ;
#18429=DIRECTION ( 'NONE',  ( -3.071710424422018668E-17, 6.404604876783312462E-16, 1.000000000000000000 ) ) ;
#18438=EDGE_LOOP ( 'NONE', ( #48191, #22874, #39576, #14997 ) ) ;
#18443=EDGE_CURVE ( 'NONE', #35820, #22785, #21980, .T. ) ;
#18446=ORIENTED_EDGE ( 'NONE', *, *, #42111, .F. ) ;
#18462=ORIENTED_EDGE ( 'NONE', *, *, #19280, .F. ) ;
#18490=DIRECTION ( 'NONE',  ( -3.071710424422018668E-17, 6.404604876783312462E-16, 1.000000000000000000 ) ) ;
#18493=FACE_OUTER_BOUND ( 'NONE', #42799, .T. ) ;
#18513=ORIENTED_EDGE ( 'NONE', *, *, #34751, .T. ) ;
#18524=VERTEX_POINT ( 'NONE', #45307 ) ;
#18527=VERTEX_POINT ( 'NONE', #8123 ) ;
#18536=ORIENTED_EDGE ( 'NONE', *, *, #2914, .T. ) ;
#18582=EDGE_CURVE ( 'NONE', #4090, #18227, #34431, .T. ) ;
#18587=ORIENTED_EDGE ( 'NONE', *, *, #15351, .F. ) ;
#18588=CARTESIAN_POINT ( 'NONE',  ( -13.71073213066623531, -18.52046572475128983, 50.77966884056655772 ) ) ;
#18600=CARTESIAN_POINT ( 'NONE',  ( -18.24684318355141599, -9.624075539355221309, 49.52966884056655772 ) ) ;
#18613=VERTEX_POINT ( 'NONE', #35642 ) ;
#18621=DIRECTION ( 'NONE',  ( -3.071710424422018668E-17, 6.404604876783312462E-16, 1.000000000000000000 ) ) ;
#18624=CIRCLE ( 'NONE', #43037, 2.000000000000000444 ) ;
#18625=ORIENTED_EDGE ( 'NONE', *, *, #9822, .T. ) ;
#18641=ORIENTED_EDGE ( 'NONE', *, *, #28789, .F. ) ;
#18643=DIRECTION ( 'NONE',  ( 3.071710424422018668E-17, -6.404604876783312462E-16, -1.000000000000000000 ) ) ;
#18646=DIRECTION ( 'NONE',  ( 0.9294853595766542353, 0.3688590060343623911, 0.000000000000000000 ) ) ;
#18647=EDGE_CURVE ( 'NONE', #24138, #8953, #12769, .T. ) ;
#18648=ORIENTED_EDGE ( 'NONE', *, *, #22229, .F. ) ;
#18660=EDGE_CURVE ( 'NONE', #14479, #41118, #3953, .T. ) ;
#18663=DIRECTION ( 'NONE',  ( 0.5351595679979623821, 0.8447509909909748371, 0.000000000000000000 ) ) ;
#18666=AXIS2_PLACEMENT_3D ( 'NONE', #43641, #20979, #39691 ) ;
#18679=CARTESIAN_POINT ( 'NONE',  ( -13.71073213066623531, -18.52046572475128983, 52.02966884056656482 ) ) ;
#18686=FACE_OUTER_BOUND ( 'NONE', #46808, .T. ) ;
#18711=ORIENTED_EDGE ( 'NONE', *, *, #46041, .F. ) ;
#18718=DIRECTION ( 'NONE',  ( 0.9687793358424821033, -0.2479245821708680464, 0.000000000000000000 ) ) ;
#18721=EDGE_CURVE ( 'NONE', #30644, #46754, #31728, .T. ) ;
#18732=VECTOR ( 'NONE', #39, 1000.000000000000000 ) ;
#18733=VECTOR ( 'NONE', #28970, 1000.000000000000000 ) ;
#18741=DIRECTION ( 'NONE',  ( 0.9687793358424821033, -0.2479245821708677133, 0.000000000000000000 ) ) ;
#18752=CYLINDRICAL_SURFACE ( 'NONE', #23156, 4.686499999999997002 ) ;
#18753=EDGE_CURVE ( 'NONE', #37481, #35750, #15707, .T. ) ;
#18759=ORIENTED_EDGE ( 'NONE', *, *, #44878, .T. ) ;
#18762=DIRECTION ( 'NONE',  ( 3.071710424422018668E-17, -6.404604876783312462E-16, -1.000000000000000000 ) ) ;
#18768=ORIENTED_EDGE ( 'NONE', *, *, #45101, .F. ) ;
#18769=SURFACE_SIDE_STYLE ('',( #37464 ) ) ;
#18778=ORIENTED_EDGE ( 'NONE', *, *, #5549, .F. ) ;
#18788=CYLINDRICAL_SURFACE ( 'NONE', #40114, 4.686499999999997002 ) ;
#18796=ORIENTED_EDGE ( 'NONE', *, *, #15362, .T. ) ;
#18806=VECTOR ( 'NONE', #20430, 1000.000000000000000 ) ;
#18815=LINE ( 'NONE', #839, #46740 ) ;
#18824=AXIS2_PLACEMENT_3D ( 'NONE', #19536, #4286, #8955 ) ;
#18829=ORIENTED_EDGE ( 'NONE', *, *, #12180, .F. ) ;
#18845=CIRCLE ( 'NONE', #31430, 1.999999999999999778 ) ;
#18847=FACE_OUTER_BOUND ( 'NONE', #13938, .T. ) ;
#18859=CARTESIAN_POINT ( 'NONE',  ( -20.38066051823377478, -10.47086428435309280, 50.77966884056655772 ) ) ;
#18865=DIRECTION ( 'NONE',  ( -3.071710424422018668E-17, 6.404604876783312462E-16, 1.000000000000000000 ) ) ;
#18871=DIRECTION ( 'NONE',  ( 3.071710424422018668E-17, -6.404604876783312462E-16, -1.000000000000000000 ) ) ;
#18889=VECTOR ( 'NONE', #41599, 1000.000000000000000 ) ;
#18890=VERTEX_POINT ( 'NONE', #30228 ) ;
#18898=VECTOR ( 'NONE', #30502, 1000.000000000000000 ) ;
#18903=VERTEX_POINT ( 'NONE', #26770 ) ;
#18905=EDGE_CURVE ( 'NONE', #45281, #19709, #7338, .T. ) ;
#18907=LINE ( 'NONE', #4146, #25254 ) ;
#18916=EDGE_LOOP ( 'NONE', ( #26678, #20568, #27249, #27730 ) ) ;
#18949=EDGE_CURVE ( 'NONE', #29256, #13129, #8299, .T. ) ;
#18952=FACE_OUTER_BOUND ( 'NONE', #30796, .T. ) ;
#18962=CIRCLE ( 'NONE', #26034, 1.999999999999999778 ) ;
#18968=ORIENTED_EDGE ( 'NONE', *, *, #22427, .F. ) ;
#18974=VERTEX_POINT ( 'NONE', #7574 ) ;
#18978=ORIENTED_EDGE ( 'NONE', *, *, #25778, .T. ) ;
#18982=AXIS2_PLACEMENT_3D ( 'NONE', #6279, #13876, #9504 ) ;
#18983=DIRECTION ( 'NONE',  ( -3.071710424422018668E-17, 6.404604876783312462E-16, 1.000000000000000000 ) ) ;
#19001=AXIS2_PLACEMENT_3D ( 'NONE', #44707, #3565, #14131 ) ;
#19011=DIRECTION ( 'NONE',  ( -0.9687793358424822143, 0.2479245821708672415, 0.000000000000000000 ) ) ;
#19012=ADVANCED_FACE ( 'NONE', ( #1867 ), #27726, .T. ) ;
#19024=ADVANCED_FACE ( 'NONE', ( #16137 ), #5580, .T. ) ;
#19030=VERTEX_POINT ( 'NONE', #9514 ) ;
#19047=DIRECTION ( 'NONE',  ( 0.7506333037770493988, -0.6607190350373991494, 0.000000000000000000 ) ) ;
#19053=VERTEX_POINT ( 'NONE', #46925 ) ;
#19073=EDGE_CURVE ( 'NONE', #23878, #15180, #26729, .T. ) ;
#19075=DIRECTION ( 'NONE',  ( -3.071710424422018668E-17, 6.404604876783312462E-16, 1.000000000000000000 ) ) ;
#19096=FACE_OUTER_BOUND ( 'NONE', #31768, .T. ) ;
#19103=DIRECTION ( 'NONE',  ( 0.9687793358424821033, -0.2479245821708677133, 0.000000000000000000 ) ) ;
#19110=AXIS2_PLACEMENT_3D ( 'NONE', #9726, #24744, #21037 ) ;
#19114=DIRECTION ( 'NONE',  ( -0.2189141945955536961, 0.9757441136919967617, 0.000000000000000000 ) ) ;
#19117=CARTESIAN_POINT ( 'NONE',  ( -17.42409385541299471, -14.80920654474435771, 49.52966884056655772 ) ) ;
#19122=EDGE_CURVE ( 'NONE', #14238, #8811, #44072, .T. ) ;
#19139=VERTEX_POINT ( 'NONE', #40494 ) ;
#19143=CARTESIAN_POINT ( 'NONE',  ( -14.38502091232239621, -11.22596901536237013, 52.02966884056656482 ) ) ;
#19144=CIRCLE ( 'NONE', #12082, 5.249999999999998224 ) ;
#19158=ORIENTED_EDGE ( 'NONE', *, *, #36525, .T. ) ;
#19161=EDGE_CURVE ( 'NONE', #36429, #33207, #13889, .T. ) ;
#19164=VERTEX_POINT ( 'NONE', #39775 ) ;
#19180=DIRECTION ( 'NONE',  ( -3.071710424422018668E-17, 6.404604876783312462E-16, 1.000000000000000000 ) ) ;
#19181=CARTESIAN_POINT ( 'NONE',  ( -19.19606018965890115, -19.75113282002397597, 50.77966884056656482 ) ) ;
#19182=CARTESIAN_POINT ( 'NONE',  ( -18.50517187854146783, -19.38160480531894692, 49.52966884056656482 ) ) ;
#19183=ORIENTED_EDGE ( 'NONE', *, *, #11450, .T. ) ;
#19189=CYLINDRICAL_SURFACE ( 'NONE', #21345, 2.000000000000001332 ) ;
#19207=CIRCLE ( 'NONE', #24745, 5.249999999999998224 ) ;
#19223=EDGE_CURVE ( 'NONE', #28760, #28899, #29664, .T. ) ;
#19250=AXIS2_PLACEMENT_3D ( 'NONE', #15535, #45621, #19489 ) ;
#19252=CIRCLE ( 'NONE', #379, 4.686499999999998778 ) ;
#19253=CARTESIAN_POINT ( 'NONE',  ( -14.95535764022100977, -18.80681796222810576, 52.02966884056656482 ) ) ;
#19262=DIRECTION ( 'NONE',  ( 0.9687793358424821033, -0.2479245821708679909, 0.000000000000000000 ) ) ;
#19267=ORIENTED_EDGE ( 'NONE', *, *, #31459, .F. ) ;
#19274=DIRECTION ( 'NONE',  ( -3.071710424422018668E-17, 6.404604876783312462E-16, 1.000000000000000000 ) ) ;
#19280=EDGE_CURVE ( 'NONE', #36826, #9358, #6303, .T. ) ;
#19282=EDGE_CURVE ( 'NONE', #36314, #42245, #12591, .T. ) ;
#19284=DIRECTION ( 'NONE',  ( 0.06357898915123476324, -0.9979768094191905359, 0.000000000000000000 ) ) ;
#19285=VERTEX_POINT ( 'NONE', #22782 ) ;
#19288=LINE ( 'NONE', #15573, #34441 ) ;
#19312=VERTEX_POINT ( 'NONE', #29917 ) ;
#19313=AXIS2_PLACEMENT_3D ( 'NONE', #16321, #30412, #31364 ) ;
#19316=FACE_OUTER_BOUND ( 'NONE', #5657, .T. ) ;
#19317=DIRECTION ( 'NONE',  ( -3.071710424422018668E-17, 6.404604876783312462E-16, 1.000000000000000000 ) ) ;
#19325=CARTESIAN_POINT ( 'NONE',  ( -17.80887632446114921, -10.12652590253629725, 52.02966884056656482 ) ) ;
#19326=EDGE_CURVE ( 'NONE', #40825, #13202, #13380, .T. ) ;
#19329=CARTESIAN_POINT ( 'NONE',  ( -17.42409385541299471, -14.80920654474435594, 52.02966884056656482 ) ) ;
#19337=VERTEX_POINT ( 'NONE', #39240 ) ;
#19340=CYLINDRICAL_SURFACE ( 'NONE', #26282, 5.249999999999998224 ) ;
#19344=ORIENTED_EDGE ( 'NONE', *, *, #3137, .F. ) ;
#19354=DIRECTION ( 'NONE',  ( -3.071710424422018668E-17, 6.404604876783312462E-16, 1.000000000000000000 ) ) ;
#19367=DIRECTION ( 'NONE',  ( -3.071710424422018668E-17, 6.404604876783312462E-16, 1.000000000000000000 ) ) ;
#19390=VERTEX_POINT ( 'NONE', #8476 ) ;
#19395=ORIENTED_EDGE ( 'NONE', *, *, #19714, .T. ) ;
#19405=LINE ( 'NONE', #42310, #38349 ) ;
#19420=LINE ( 'NONE', #7876, #20182 ) ;
#19431=EDGE_CURVE ( 'NONE', #25847, #47981, #21264, .T. ) ;
#19448=EDGE_CURVE ( 'NONE', #10107, #13759, #24951, .T. ) ;
#19471=ORIENTED_EDGE ( 'NONE', *, *, #3199, .F. ) ;
#19482=AXIS2_PLACEMENT_3D ( 'NONE', #44160, #47985, #47737 ) ;
#19489=DIRECTION ( 'NONE',  ( -0.9687793358424822143, 0.2479245821708672415, 0.000000000000000000 ) ) ;
#19498=ORIENTED_EDGE ( 'NONE', *, *, #4971, .T. ) ;
#19510=AXIS2_PLACEMENT_3D ( 'NONE', #24752, #42968, #32609 ) ;
#19517=CIRCLE ( 'NONE', #47046, 4.686499999999997890 ) ;
#19536=CARTESIAN_POINT ( 'NONE',  ( -15.64104502085146642, -10.46221995643221270, 49.52966884056655772 ) ) ;
#19551=CIRCLE ( 'NONE', #31362, 2.000000000000001332 ) ;
#19553=CIRCLE ( 'NONE', #35291, 1.999999999999999112 ) ;
#19557=AXIS2_PLACEMENT_3D ( 'NONE', #35580, #12211, #20333 ) ;
#19565=CIRCLE ( 'NONE', #6173, 2.000000000000001776 ) ;
#19572=DIRECTION ( 'NONE',  ( 0.9687793358424822143, -0.2479245821708672415, 0.000000000000000000 ) ) ;
#19584=AXIS2_PLACEMENT_3D ( 'NONE', #39709, #10159, #5506 ) ;
#19596=DIRECTION ( 'NONE',  ( -3.071710424422018668E-17, 6.404604876783312462E-16, 1.000000000000000000 ) ) ;
#19600=EDGE_LOOP ( 'NONE', ( #43400, #29550, #5819, #33050 ) ) ;
#19601=CARTESIAN_POINT ( 'NONE',  ( -17.42409385541299471, -14.80920654474435594, 52.02966884056656482 ) ) ;
#19605=DIRECTION ( 'NONE',  ( 0.2479245821708712938, 0.9687793358424811041, 0.000000000000000000 ) ) ;
#19630=ORIENTED_EDGE ( 'NONE', *, *, #24665, .F. ) ;
#19631=EDGE_CURVE ( 'NONE', #14637, #10419, #24353, .T. ) ;
#19636=AXIS2_PLACEMENT_3D ( 'NONE', #43418, #13580, #43658 ) ;
#19639=ORIENTED_EDGE ( 'NONE', *, *, #33783, .T. ) ;
#19640=DIRECTION ( 'NONE',  ( 0.9687793358424819923, -0.2479245821708678243, 0.000000000000000000 ) ) ;
#19642=CARTESIAN_POINT ( 'NONE',  ( -16.17583575424048092, -10.27959207348368764, 49.52966884056655772 ) ) ;
#19645=DIRECTION ( 'NONE',  ( -3.071710424422018668E-17, 6.404604876783312462E-16, 1.000000000000000000 ) ) ;
#19658=EDGE_CURVE ( 'NONE', #17957, #41560, #29112, .T. ) ;
#19664=DIRECTION ( 'NONE',  ( 0.9687793358424817702, -0.2479245821708686570, 0.000000000000000000 ) ) ;
#19676=DIRECTION ( 'NONE',  ( -3.071710424422018668E-17, 6.404604876783312462E-16, 1.000000000000000000 ) ) ;
#19689=VERTEX_POINT ( 'NONE', #9587 ) ;
#19708=EDGE_CURVE ( 'NONE', #36678, #9620, #1627, .T. ) ;
#19709=VERTEX_POINT ( 'NONE', #34932 ) ;
#19710=DIRECTION ( 'NONE',  ( -3.071710424422018668E-17, 6.404604876783312462E-16, 1.000000000000000000 ) ) ;
#19712=VERTEX_POINT ( 'NONE', #28285 ) ;
#19714=EDGE_CURVE ( 'NONE', #39071, #45281, #39341, .T. ) ;
#19733=VERTEX_POINT ( 'NONE', #20893 ) ;
#19736=CYLINDRICAL_SURFACE ( 'NONE', #725, 1.999999999999999112 ) ;
#19753=ORIENTED_EDGE ( 'NONE', *, *, #14348, .T. ) ;
#19760=EDGE_CURVE ( 'NONE', #10364, #18524, #7901, .T. ) ;
#19763=ORIENTED_EDGE ( 'NONE', *, *, #4860, .T. ) ;
#19767=ORIENTED_EDGE ( 'NONE', *, *, #13951, .T. ) ;
#19773=VERTEX_POINT ( 'NONE', #3380 ) ;
#19776=DIRECTION ( 'NONE',  ( -3.071710424422018668E-17, 6.404604876783312462E-16, 1.000000000000000000 ) ) ;
#19779=EDGE_CURVE ( 'NONE', #467, #38954, #10537, .T. ) ;
#19781=AXIS2_PLACEMENT_3D ( 'NONE', #30420, #19075, #373 ) ;
#19784=CARTESIAN_POINT ( 'NONE',  ( -17.94839601134439633, -19.47832453368858197, 52.02966884056656482 ) ) ;
#19789=ADVANCED_FACE ( 'NONE', ( #36847 ), #17431, .T. ) ;
#19805=CIRCLE ( 'NONE', #38657, 1.999999999999999556 ) ;
#19811=FACE_OUTER_BOUND ( 'NONE', #32900, .T. ) ;
#19816=ORIENTED_EDGE ( 'NONE', *, *, #6785, .F. ) ;
#19850=DIRECTION ( 'NONE',  ( -0.2189141945955538626, 0.9757441136919966507, 0.000000000000000000 ) ) ;
#19852=CARTESIAN_POINT ( 'NONE',  ( -13.75179125342063458, -11.87837916245159775, 52.02966884056656482 ) ) ;
#19884=DIRECTION ( 'NONE',  ( -3.071710424422018668E-17, 6.404604876783312462E-16, 1.000000000000000000 ) ) ;
#19885=CARTESIAN_POINT ( 'NONE',  ( -21.13745558015973103, -11.09794736473739896, 49.52966884056655772 ) ) ;
#19906=DIRECTION ( 'NONE',  ( -3.071710424422018668E-17, 6.404604876783312462E-16, 1.000000000000000000 ) ) ;
#19913=ORIENTED_EDGE ( 'NONE', *, *, #4529, .F. ) ;
#19914=CARTESIAN_POINT ( 'NONE',  ( -21.73853604213786639, -16.63919858500264937, 49.52966884056655772 ) ) ;
#19922=FACE_OUTER_BOUND ( 'NONE', #11427, .T. ) ;
#19923=VERTEX_POINT ( 'NONE', #37846 ) ;
#19924=ORIENTED_EDGE ( 'NONE', *, *, #28360, .T. ) ;
#19933=DIRECTION ( 'NONE',  ( -3.071710424422018668E-17, 6.404604876783312462E-16, 1.000000000000000000 ) ) ;
#19936=DIRECTION ( 'NONE',  ( -3.071710424422018668E-17, 6.404604876783312462E-16, 1.000000000000000000 ) ) ;
#19939=EDGE_LOOP ( 'NONE', ( #31924, #25816, #7614, #11382 ) ) ;
#19941=CARTESIAN_POINT ( 'NONE',  ( -22.11774618123879677, -15.02177039319221308, 49.52966884056655772 ) ) ;
#19948=DIRECTION ( 'NONE',  ( -3.071710424422018668E-17, 6.404604876783312462E-16, 1.000000000000000000 ) ) ;
#19955=AXIS2_PLACEMENT_3D ( 'NONE', #45824, #12080, #29824 ) ;
#19958=FACE_OUTER_BOUND ( 'NONE', #30836, .T. ) ;
#19960=DIRECTION ( 'NONE',  ( -3.071710424422018668E-17, 6.404604876783312462E-16, 1.000000000000000000 ) ) ;
#19963=CYLINDRICAL_SURFACE ( 'NONE', #20302, 5.249999999999998224 ) ;
#19981=CYLINDRICAL_SURFACE ( 'NONE', #5399, 5.249999999999998224 ) ;
#19985=EDGE_CURVE ( 'NONE', #20224, #6783, #14136, .T. ) ;
#19989=CIRCLE ( 'NONE', #15243, 4.686499999999999666 ) ;
#19997=CIRCLE ( 'NONE', #28642, 2.000000000000000444 ) ;
#20011=CARTESIAN_POINT ( 'NONE',  ( -14.21171452256333012, -10.65672306833167760, 52.02966884056656482 ) ) ;
#20029=DIRECTION ( 'NONE',  ( 0.9687793358424822143, -0.2479245821708672415, 0.000000000000000000 ) ) ;
#20057=CIRCLE ( 'NONE', #17678, 5.249999999999998224 ) ;
#20065=DIRECTION ( 'NONE',  ( 0.9687793358424821033, -0.2479245821708677133, 0.000000000000000000 ) ) ;
#20066=VERTEX_POINT ( 'NONE', #46124 ) ;
#20084=CARTESIAN_POINT ( 'NONE',  ( -17.03931138636480824, -19.49188718695241462, 49.52966884056656482 ) ) ;
#20089=VECTOR ( 'NONE', #48365, 1000.000000000000000 ) ;
#20103=ADVANCED_FACE ( 'NONE', ( #34541 ), #26933, .T. ) ;
#20105=DIRECTION ( 'NONE',  ( -3.071710424422018668E-17, 6.404604876783312462E-16, 1.000000000000000000 ) ) ;
#20114=ADVANCED_FACE ( 'NONE', ( #348 ), #38480, .T. ) ;
#20119=CIRCLE ( 'NONE', #5158, 2.000000000000000888 ) ;
#20121=CARTESIAN_POINT ( 'NONE',  ( -22.10931616815485512, -14.45671906187057765, 52.02966884056656482 ) ) ;
#20135=CARTESIAN_POINT ( 'NONE',  ( -17.42409385541299471, -14.80920654474434883, 62.02966884056656482 ) ) ;
#20141=FACE_OUTER_BOUND ( 'NONE', #32679, .T. ) ;
#20154=CARTESIAN_POINT ( 'NONE',  ( -20.43749099114212342, -18.39845715627588874, 49.52966884056656482 ) ) ;
#20158=AXIS2_PLACEMENT_3D ( 'NONE', #41351, #42092, #3941 ) ;
#20159=VERTEX_POINT ( 'NONE', #37995 ) ;
#20160=VERTEX_POINT ( 'NONE', #4281 ) ;
#20171=EDGE_CURVE ( 'NONE', #35776, #7471, #29144, .T. ) ;
#20182=VECTOR ( 'NONE', #22155, 1000.000000000000000 ) ;
#20192=AXIS2_PLACEMENT_3D ( 'NONE', #10040, #44034, #37089 ) ;
#20198=CARTESIAN_POINT ( 'NONE',  ( -12.74563483257940177, -17.19133189234193893, 52.02966884056656482 ) ) ;
#20201=ORIENTED_EDGE ( 'NONE', *, *, #17651, .F. ) ;
#20216=CARTESIAN_POINT ( 'NONE',  ( -14.51911023200684703, -18.48675360735852280, 49.52966884056656482 ) ) ;
#20224=VERTEX_POINT ( 'NONE', #24207 ) ;
#20241=CARTESIAN_POINT ( 'NONE',  ( -17.42409385541299471, -14.80920654474435771, 49.52966884056655772 ) ) ;
#20258=EDGE_CURVE ( 'NONE', #12617, #11419, #43326, .T. ) ;
#20259=CIRCLE ( 'NONE', #43066, 2.000000000000000000 ) ;
#20260=CIRCLE ( 'NONE', #35954, 1.999999999999999778 ) ;
#20271=CARTESIAN_POINT ( 'NONE',  ( -20.35492123770571382, -11.13690394275196560, 49.52966884056655772 ) ) ;
#20274=CARTESIAN_POINT ( 'NONE',  ( -17.42409385541299471, -14.80920654474435594, 52.02966884056656482 ) ) ;
#20276=CIRCLE ( 'NONE', #5339, 1.999999999999999778 ) ;
#20280=CIRCLE ( 'NONE', #33638, 2.000000000000000000 ) ;
#20284=ORIENTED_EDGE ( 'NONE', *, *, #45089, .F. ) ;
#20291=EDGE_LOOP ( 'NONE', ( #16680, #48525, #26427, #40576 ) ) ;
#20295=DIRECTION ( 'NONE',  ( 0.9687793358424821033, -0.2479245821708679909, 0.000000000000000000 ) ) ;
#20302=AXIS2_PLACEMENT_3D ( 'NONE', #35210, #42130, #1482 ) ;
#20312=DIRECTION ( 'NONE',  ( -3.071710424422018668E-17, 6.404604876783312462E-16, 1.000000000000000000 ) ) ;
#20313=CARTESIAN_POINT ( 'NONE',  ( -14.25548580596218429, -11.33998781794830712, 49.52966884056655772 ) ) ;
#20322=CARTESIAN_POINT ( 'NONE',  ( -17.42409385541299471, -14.80920654474435771, 49.52966884056655772 ) ) ;
#20324=EDGE_CURVE ( 'NONE', #6587, #38614, #10548, .T. ) ;
#20327=VECTOR ( 'NONE', #32884, 1000.000000000000000 ) ;
#20332=ORIENTED_EDGE ( 'NONE', *, *, #28547, .F. ) ;
#20333=DIRECTION ( 'NONE',  ( 0.6380325334150255268, -0.7700094066334542964, 0.000000000000000000 ) ) ;
#20345=CARTESIAN_POINT ( 'NONE',  ( -17.42409385541299471, -14.80920654474434883, 62.02966884056656482 ) ) ;
#20349=VERTEX_POINT ( 'NONE', #10311 ) ;
#20361=CIRCLE ( 'NONE', #3844, 5.249999999999998224 ) ;
#20363=ORIENTED_EDGE ( 'NONE', *, *, #33848, .T. ) ;
#20376=DIRECTION ( 'NONE',  ( -3.071710424422018668E-17, 6.404604876783312462E-16, 1.000000000000000000 ) ) ;
#20378=CARTESIAN_POINT ( 'NONE',  ( -13.08950423898529891, -12.99622877252704001, 49.52966884056655772 ) ) ;
#20383=EDGE_CURVE ( 'NONE', #23878, #36333, #7354, .T. ) ;
#20384=DIRECTION ( 'NONE',  ( 0.9687793358424821033, -0.2479245821708679909, 0.000000000000000000 ) ) ;
#20387=DIRECTION ( 'NONE',  ( -3.071710424422018668E-17, 6.404604876783312462E-16, 1.000000000000000000 ) ) ;
#20388=VERTEX_POINT ( 'NONE', #3391 ) ;
#20395=EDGE_CURVE ( 'NONE', #25765, #11361, #18907, .T. ) ;
#20412=AXIS2_PLACEMENT_3D ( 'NONE', #29094, #44148, #25407 ) ;
#20427=CYLINDRICAL_SURFACE ( 'NONE', #1267, 1.999999999999999556 ) ;
#20429=CARTESIAN_POINT ( 'NONE',  ( -12.74698474939898496, -12.42443183621510094, 49.52966884056655772 ) ) ;
#20430=DIRECTION ( 'NONE',  ( -3.071710424422018668E-17, 6.404604876783312462E-16, 1.000000000000000000 ) ) ;
#20441=CARTESIAN_POINT ( 'NONE',  ( -15.18259368501833784, -19.55664553709809894, 50.77966884056656482 ) ) ;
#20445=DIRECTION ( 'NONE',  ( 0.7700094066334511878, 0.6380325334150293015, 0.000000000000000000 ) ) ;
#20448=VECTOR ( 'NONE', #19180, 1000.000000000000000 ) ;
#20451=DIRECTION ( 'NONE',  ( -3.071710424422018668E-17, 6.404604876783312462E-16, 1.000000000000000000 ) ) ;
#20464=FACE_OUTER_BOUND ( 'NONE', #44497, .T. ) ;
#20471=VERTEX_POINT ( 'NONE', #26057 ) ;
#20472=EDGE_CURVE ( 'NONE', #15515, #25922, #48697, .T. ) ;
#20474=CARTESIAN_POINT ( 'NONE',  ( -15.61111608319569477, -19.14379616117205885, 49.52966884056656482 ) ) ;
#20499=DIRECTION ( 'NONE',  ( 0.9956360040033426229, -0.09332174201254549162, 0.000000000000000000 ) ) ;
#20504=FACE_OUTER_BOUND ( 'NONE', #8775, .T. ) ;
#20505=CIRCLE ( 'NONE', #24448, 5.249999999999998224 ) ;
#20507=DIRECTION ( 'NONE',  ( -3.071710424422018668E-17, 6.404604876783312462E-16, 1.000000000000000000 ) ) ;
#20521=VERTEX_POINT ( 'NONE', #39060 ) ;
#20533=CARTESIAN_POINT ( 'NONE',  ( -13.82526118368687484, -18.63162768858978779, 50.77966884056655772 ) ) ;
#20534=ORIENTED_EDGE ( 'NONE', *, *, #48683, .F. ) ;
#20536=DIRECTION ( 'NONE',  ( -3.071710424422018668E-17, 6.404604876783312462E-16, 1.000000000000000000 ) ) ;
#20539=CARTESIAN_POINT ( 'NONE',  ( -13.83484324388145303, -17.82260368047347399, 49.52966884056656482 ) ) ;
#20560=VECTOR ( 'NONE', #11567, 1000.000000000000000 ) ;
#20565=EDGE_LOOP ( 'NONE', ( #14762, #19395, #28471, #14099 ) ) ;
#20568=ORIENTED_EDGE ( 'NONE', *, *, #32277, .F. ) ;
#20569=FACE_OUTER_BOUND ( 'NONE', #6468, .T. ) ;
#20572=DIRECTION ( 'NONE',  ( 0.9687793358424822143, -0.2479245821708672415, 0.000000000000000000 ) ) ;
#20575=FACE_OUTER_BOUND ( 'NONE', #25475, .T. ) ;
#20580=DIRECTION ( 'NONE',  ( -3.071710424422018668E-17, 6.404604876783312462E-16, 1.000000000000000000 ) ) ;
#20584=CARTESIAN_POINT ( 'NONE',  ( -15.79771479060332240, -19.20445095063907104, 52.02966884056656482 ) ) ;
#20592=DIRECTION ( 'NONE',  ( -3.071710424422018668E-17, 6.404604876783312462E-16, 1.000000000000000000 ) ) ;
#20594=DIRECTION ( 'NONE',  ( 0.9687793358424821033, -0.2479245821708677133, 0.000000000000000000 ) ) ;
#20605=ORIENTED_EDGE ( 'NONE', *, *, #6005, .F. ) ;
#20618=ORIENTED_EDGE ( 'NONE', *, *, #8465, .T. ) ;
#20622=CYLINDRICAL_SURFACE ( 'NONE', #40211, 5.249999999999998224 ) ;
#20645=EDGE_CURVE ( 'NONE', #16885, #44810, #33888, .T. ) ;
#20672=DIRECTION ( 'NONE',  ( -3.071710424422018668E-17, 6.404604876783312462E-16, 1.000000000000000000 ) ) ;
#20684=ORIENTED_EDGE ( 'NONE', *, *, #19431, .F. ) ;
#20712=DIRECTION ( 'NONE',  ( -3.071710424422018668E-17, 6.404604876783312462E-16, 1.000000000000000000 ) ) ;
#20713=EDGE_LOOP ( 'NONE', ( #9821, #6555, #16863, #44016 ) ) ;
#20722=EDGE_CURVE ( 'NONE', #467, #35820, #36230, .T. ) ;
#20729=ADVANCED_FACE ( 'NONE', ( #380 ), #11448, .T. ) ;
#20736=DIRECTION ( 'NONE',  ( -0.9687793358424819923, 0.2479245821708680464, 0.000000000000000000 ) ) ;
#20738=ORIENTED_EDGE ( 'NONE', *, *, #1271, .T. ) ;
#20751=VERTEX_POINT ( 'NONE', #7530 ) ;
#20763=AXIS2_PLACEMENT_3D ( 'NONE', #12213, #4835, #19605 ) ;
#20774=DIRECTION ( 'NONE',  ( -3.071710424422018668E-17, 6.404604876783312462E-16, 1.000000000000000000 ) ) ;
#20780=CARTESIAN_POINT ( 'NONE',  ( -19.74436319619195501, -10.72363366794506412, 49.52966884056655772 ) ) ;
#20784=DIRECTION ( 'NONE',  ( 3.071710424422018668E-17, -6.404604876783312462E-16, -1.000000000000000000 ) ) ;
#20807=CARTESIAN_POINT ( 'NONE',  ( -12.75531685953890282, -14.40201664703461049, 49.52966884056655772 ) ) ;
#20815=DIRECTION ( 'NONE',  ( 0.9687793358424819923, -0.2479245821708676023, 0.000000000000000000 ) ) ;
#20819=DIRECTION ( 'NONE',  ( 0.9687793358424817702, -0.2479245821708686570, 0.000000000000000000 ) ) ;
#20843=EDGE_LOOP ( 'NONE', ( #46089, #24264, #8556, #7395 ) ) ;
#20849=ORIENTED_EDGE ( 'NONE', *, *, #10906, .F. ) ;
#20860=EDGE_LOOP ( 'NONE', ( #37979, #3133, #35707, #35010 ) ) ;
#20863=AXIS2_PLACEMENT_3D ( 'NONE', #11360, #40904, #29583 ) ;
#20881=CARTESIAN_POINT ( 'NONE',  ( -17.42409385541299471, -14.80920654474435594, 52.02966884056656482 ) ) ;
#20893=CARTESIAN_POINT ( 'NONE',  ( -17.83128375312269753, -10.14042954887025871, 52.02966884056656482 ) ) ;
#20898=AXIS2_PLACEMENT_3D ( 'NONE', #38190, #31067, #46086 ) ;
#20926=CARTESIAN_POINT ( 'NONE',  ( -19.25408589567127038, -10.49476435801948071, 49.52966884056655772 ) ) ;
#20933=FACE_OUTER_BOUND ( 'NONE', #14598, .T. ) ;
#20934=EDGE_CURVE ( 'NONE', #9358, #26370, #47853, .T. ) ;
#20972=VERTEX_POINT ( 'NONE', #1829 ) ;
#20974=CARTESIAN_POINT ( 'NONE',  ( -17.42409385541299471, -14.80920654474435594, 52.02966884056656482 ) ) ;
#20977=DIRECTION ( 'NONE',  ( -3.071710424422018668E-17, 6.404604876783312462E-16, 1.000000000000000000 ) ) ;
#20979=DIRECTION ( 'NONE',  ( 3.071710424422018668E-17, -6.404604876783312462E-16, -1.000000000000000000 ) ) ;
#20981=FACE_OUTER_BOUND ( 'NONE', #27795, .T. ) ;
#21002=AXIS2_PLACEMENT_3D ( 'NONE', #742, #26349, #7904 ) ;
#21006=EDGE_CURVE ( 'NONE', #11419, #45533, #40948, .T. ) ;
#21012=CIRCLE ( 'NONE', #37506, 2.000000000000001332 ) ;
#21023=DIRECTION ( 'NONE',  ( -3.071710424422018668E-17, 6.404604876783312462E-16, 1.000000000000000000 ) ) ;
#21037=DIRECTION ( 'NONE',  ( 0.9687793358424819923, -0.2479245821708680464, 0.000000000000000000 ) ) ;
#21039=CIRCLE ( 'NONE', #33590, 2.000000000000001332 ) ;
#21048=DIRECTION ( 'NONE',  ( 0.9687793358424821033, -0.2479245821708679909, 0.000000000000000000 ) ) ;
#21052=CARTESIAN_POINT ( 'NONE',  ( -19.19606018965890115, -19.75113282002397597, 52.02966884056656482 ) ) ;
#21058=CARTESIAN_POINT ( 'NONE',  ( -13.95487512861695834, -17.97781459419518058, 49.52966884056656482 ) ) ;
#21060=VERTEX_POINT ( 'NONE', #26417 ) ;
#21082=AXIS2_PLACEMENT_3D ( 'NONE', #45411, #25708, #18302 ) ;
#21088=FACE_OUTER_BOUND ( 'NONE', #31468, .T. ) ;
#21094=AXIS2_PLACEMENT_3D ( 'NONE', #48649, #11234, #40525 ) ;
#21107=ORIENTED_EDGE ( 'NONE', *, *, #26894, .F. ) ;
#21113=DIRECTION ( 'NONE',  ( -0.7700094066334557397, -0.6380325334150237504, 0.000000000000000000 ) ) ;
#21114=CIRCLE ( 'NONE', #22707, 1.999999999999999112 ) ;
#21117=ORIENTED_EDGE ( 'NONE', *, *, #20258, .F. ) ;
#21124=LINE ( 'NONE', #36121, #22549 ) ;
#21125=ADVANCED_FACE ( 'NONE', ( #41926 ), #27145, .T. ) ;
#21138=AXIS2_PLACEMENT_3D ( 'NONE', #16057, #576, #19047 ) ;
#21144=VECTOR ( 'NONE', #31710, 1000.000000000000000 ) ;
#21149=FACE_OUTER_BOUND ( 'NONE', #46994, .T. ) ;
#21156=EDGE_CURVE ( 'NONE', #6917, #45300, #32361, .T. ) ;
#21158=DIRECTION ( 'NONE',  ( -0.09332174201254901658, -0.9956360040033422898, 0.000000000000000000 ) ) ;
#21160=EDGE_LOOP ( 'NONE', ( #24931, #12544 ) ) ;
#21169=ORIENTED_EDGE ( 'NONE', *, *, #26603, .T. ) ;
#21170=DIRECTION ( 'NONE',  ( -0.9687793358424819923, 0.2479245821708680464, 0.000000000000000000 ) ) ;
#21175=CARTESIAN_POINT ( 'NONE',  ( -17.01690395770326347, -19.47798354061844961, 52.02966884056656482 ) ) ;
#21177=AXIS2_PLACEMENT_3D ( 'NONE', #48051, #44373, #44611 ) ;
#21187=AXIS2_PLACEMENT_3D ( 'NONE', #31163, #12443, #12207 ) ;
#21192=ORIENTED_EDGE ( 'NONE', *, *, #18905, .F. ) ;
#21193=EDGE_CURVE ( 'NONE', #15483, #20349, #15023, .T. ) ;
#21205=CIRCLE ( 'NONE', #32951, 5.249999999999998224 ) ;
#21231=CARTESIAN_POINT ( 'NONE',  ( -12.85925802207596114, -13.69662874518196993, 52.02966884056656482 ) ) ;
#21240=AXIS2_PLACEMENT_3D ( 'NONE', #35913, #48217, #6380 ) ;
#21248=VECTOR ( 'NONE', #23954, 1000.000000000000000 ) ;
#21255=VECTOR ( 'NONE', #18621, 1000.000000000000000 ) ;
#21264=LINE ( 'NONE', #32806, #12625 ) ;
#21265=CARTESIAN_POINT ( 'NONE',  ( -18.50517187854146783, -19.38160480531894336, 52.02966884056656482 ) ) ;
#21273=DIRECTION ( 'NONE',  ( 0.9687793358424821033, -0.2479245821708677133, 0.000000000000000000 ) ) ;
#21285=ORIENTED_EDGE ( 'NONE', *, *, #42111, .T. ) ;
#21294=EDGE_CURVE ( 'NONE', #18524, #23374, #37034, .T. ) ;
#21304=AXIS2_PLACEMENT_3D ( 'NONE', #30623, #22745, #12134 ) ;
#21306=DIRECTION ( 'NONE',  ( 0.9687793358424821033, -0.2479245821708677133, 0.000000000000000000 ) ) ;
#21307=ORIENTED_EDGE ( 'NONE', *, *, #40745, .T. ) ;
#21312=ORIENTED_EDGE ( 'NONE', *, *, #8682, .T. ) ;
#21316=CIRCLE ( 'NONE', #34648, 4.686499999999997890 ) ;
#21323=CARTESIAN_POINT ( 'NONE',  ( -17.42409385541299471, -14.80920654474435594, 52.02966884056656482 ) ) ;
#21332=ORIENTED_EDGE ( 'NONE', *, *, #34070, .F. ) ;
#21338=CYLINDRICAL_SURFACE ( 'NONE', #31199, 5.249999999999998224 ) ;
#21345=AXIS2_PLACEMENT_3D ( 'NONE', #30289, #27061, #4661 ) ;
#21350=CYLINDRICAL_SURFACE ( 'NONE', #36255, 2.000000000000000000 ) ;
#21351=EDGE_LOOP ( 'NONE', ( #19753, #16435, #46427, #13449 ) ) ;
#21370=CARTESIAN_POINT ( 'NONE',  ( -22.10120296142702045, -17.19398125327358073, 49.52966884056655772 ) ) ;
#21376=DIRECTION ( 'NONE',  ( 0.7700094066334515208, 0.6380325334150288574, 0.000000000000000000 ) ) ;
#21388=DIRECTION ( 'NONE',  ( -0.7700094066334558507, -0.6380325334150236394, 0.000000000000000000 ) ) ;
#21403=CARTESIAN_POINT ( 'NONE',  ( -22.07864594086649390, -14.26292169798353981, 49.52966884056655772 ) ) ;
#21408=VERTEX_POINT ( 'NONE', #14499 ) ;
#21416=DIRECTION ( 'NONE',  ( 3.071710424422018668E-17, -6.404604876783312462E-16, -1.000000000000000000 ) ) ;
#21419=ORIENTED_EDGE ( 'NONE', *, *, #17024, .F. ) ;
#21424=CARTESIAN_POINT ( 'NONE',  ( -17.42409385541299471, -14.80920654474435771, 49.52966884056655772 ) ) ;
#21425=ORIENTED_EDGE ( 'NONE', *, *, #43452, .F. ) ;
#21439=DIRECTION ( 'NONE',  ( 0.9687793358424821033, -0.2479245821708677133, 0.000000000000000000 ) ) ;
#21464=ADVANCED_FACE ( 'NONE', ( #39557 ), #40288, .T. ) ;
#21518=DIRECTION ( 'NONE',  ( -3.071710424422018668E-17, 6.404604876783312462E-16, 1.000000000000000000 ) ) ;
#21531=CARTESIAN_POINT ( 'NONE',  ( -17.42409385541299471, -14.80920654474434883, 62.02966884056656482 ) ) ;
#21533=FACE_OUTER_BOUND ( 'NONE', #20713, .T. ) ;
#21545=EDGE_LOOP ( 'NONE', ( #21192, #34841, #22552, #22614 ) ) ;
#21547=DIRECTION ( 'NONE',  ( 0.9687793358424821033, -0.2479245821708680464, 0.000000000000000000 ) ) ;
#21567=CYLINDRICAL_SURFACE ( 'NONE', #5588, 5.249999999999998224 ) ;
#21582=EDGE_LOOP ( 'NONE', ( #37260, #12038, #14358, #38074 ) ) ;
#21583=DIRECTION ( 'NONE',  ( -3.071710424422018668E-17, 6.404604876783312462E-16, 1.000000000000000000 ) ) ;
#21610=FACE_OUTER_BOUND ( 'NONE', #34742, .T. ) ;
#21624=ADVANCED_FACE ( 'NONE', ( #18847 ), #44720, .T. ) ;
#21631=ORIENTED_EDGE ( 'NONE', *, *, #6646, .F. ) ;
#21636=DIRECTION ( 'NONE',  ( -3.071710424422018668E-17, 6.404604876783312462E-16, 1.000000000000000000 ) ) ;
#21652=LINE ( 'NONE', #33431, #44391 ) ;
#21704=VERTEX_POINT ( 'NONE', #4556 ) ;
#21706=FACE_OUTER_BOUND ( 'NONE', #4732, .T. ) ;
#21709=CYLINDRICAL_SURFACE ( 'NONE', #10947, 4.686499999999997002 ) ;
#21711=ORIENTED_EDGE ( 'NONE', *, *, #1031, .F. ) ;
#21758=DIRECTION ( 'NONE',  ( -0.9687793358424819923, 0.2479245821708680464, 0.000000000000000000 ) ) ;
#21767=CYLINDRICAL_SURFACE ( 'NONE', #43182, 5.249999999999998224 ) ;
#21770=VECTOR ( 'NONE', #26700, 1000.000000000000000 ) ;
#21780=ORIENTED_EDGE ( 'NONE', *, *, #29388, .F. ) ;
#21817=VERTEX_POINT ( 'NONE', #47143 ) ;
#21828=CARTESIAN_POINT ( 'NONE',  ( -21.98892968875003717, -15.92178434430670642, 52.02966884056656482 ) ) ;
#21834=DIRECTION ( 'NONE',  ( -0.9294853595766571219, -0.3688590060343552857, 0.000000000000000000 ) ) ;
#21853=CARTESIAN_POINT ( 'NONE',  ( -13.40763370604777371, -17.22402126197653160, 49.52966884056655772 ) ) ;
#21862=DIRECTION ( 'NONE',  ( 0.9687793358424821033, -0.2479245821708677133, 0.000000000000000000 ) ) ;
#21863=CIRCLE ( 'NONE', #7720, 5.249999999999998224 ) ;
#21865=AXIS2_PLACEMENT_3D ( 'NONE', #14841, #17820, #21547 ) ;
#21875=DIRECTION ( 'NONE',  ( -3.071710424422018668E-17, 6.404604876783312462E-16, 1.000000000000000000 ) ) ;
#21904=CIRCLE ( 'NONE', #13239, 5.249999999999998224 ) ;
#21914=LINE ( 'NONE', #36916, #10722 ) ;
#21920=DIRECTION ( 'NONE',  ( 0.9687793358424821033, -0.2479245821708680464, 0.000000000000000000 ) ) ;
#21925=CIRCLE ( 'NONE', #9364, 4.686499999999997890 ) ;
#21928=ORIENTED_EDGE ( 'NONE', *, *, #10709, .T. ) ;
#21930=AXIS2_PLACEMENT_3D ( 'NONE', #16812, #1564, #15846 ) ;
#21936=CARTESIAN_POINT ( 'NONE',  ( -17.42409385541299471, -14.80920654474435594, 52.02966884056656482 ) ) ;
#21938=EDGE_CURVE ( 'NONE', #17399, #10862, #30784, .T. ) ;
#21941=CIRCLE ( 'NONE', #21187, 1.999999999999999778 ) ;
#21954=DIRECTION ( 'NONE',  ( -3.071710424422018668E-17, 6.404604876783312462E-16, 1.000000000000000000 ) ) ;
#21980=CIRCLE ( 'NONE', #36892, 5.249999999999998224 ) ;
#21981=AXIS2_PLACEMENT_3D ( 'NONE', #45001, #13989, #48663 ) ;
#21989=AXIS2_PLACEMENT_3D ( 'NONE', #9439, #9914, #36473 ) ;
#21990=ADVANCED_FACE ( 'NONE', ( #33795 ), #18788, .T. ) ;
#21991=CARTESIAN_POINT ( 'NONE',  ( -17.42409385541299471, -14.80920654474435594, 52.02966884056656482 ) ) ;
#21992=DIRECTION ( 'NONE',  ( 0.6380325334150263039, -0.7700094066334535192, 0.000000000000000000 ) ) ;
#22002=DIRECTION ( 'NONE',  ( 0.9687793358424821033, -0.2479245821708679631, 1.885439946533205044E-16 ) ) ;
#22024=ADVANCED_FACE ( 'NONE', ( #22487, #37485 ), #29629, .F. ) ;
#22032=CIRCLE ( 'NONE', #30695, 1.999999999999999556 ) ;
#22044=EDGE_CURVE ( 'NONE', #7471, #21408, #33537, .T. ) ;
#22052=DIRECTION ( 'NONE',  ( -3.071710424422018668E-17, 6.404604876783312462E-16, 1.000000000000000000 ) ) ;
#22055=DIRECTION ( 'NONE',  ( 0.9687793358424821033, -0.2479245821708677133, 0.000000000000000000 ) ) ;
#22061=ORIENTED_EDGE ( 'NONE', *, *, #33653, .T. ) ;
#22069=CARTESIAN_POINT ( 'NONE',  ( -17.21153000696512336, -19.50285887057015088, 52.02966884056656482 ) ) ;
#22073=EDGE_CURVE ( 'NONE', #36314, #8953, #13376, .T. ) ;
#22090=ORIENTED_EDGE ( 'NONE', *, *, #19161, .F. ) ;
#22106=EDGE_CURVE ( 'NONE', #45116, #33352, #1052, .T. ) ;
#22120=CIRCLE ( 'NONE', #23715, 5.249999999999998224 ) ;
#22146=ORIENTED_EDGE ( 'NONE', *, *, #24826, .F. ) ;
#22155=DIRECTION ( 'NONE',  ( -3.071710424422018668E-17, 6.404604876783312462E-16, 1.000000000000000000 ) ) ;
#22165=AXIS2_PLACEMENT_3D ( 'NONE', #12417, #21023, #1323 ) ;
#22166=DIRECTION ( 'NONE',  ( -3.071710424422018668E-17, 6.404604876783312462E-16, 1.000000000000000000 ) ) ;
#22167=DIRECTION ( 'NONE',  ( 3.071710424422018668E-17, -6.404604876783312462E-16, -1.000000000000000000 ) ) ;
#22188=CARTESIAN_POINT ( 'NONE',  ( -19.94733193681641481, -19.41309290135173526, 49.52966884056656482 ) ) ;
#22195=CARTESIAN_POINT ( 'NONE',  ( -12.89447938415233175, -16.05746464591689104, 49.52966884056655772 ) ) ;
#22199=DIRECTION ( 'NONE',  ( 0.3964226963016398431, 0.9180681052388965924, 0.000000000000000000 ) ) ;
#22209=DIRECTION ( 'NONE',  ( -3.071710424422018668E-17, 6.404604876783312462E-16, 1.000000000000000000 ) ) ;
#22214=DIRECTION ( 'NONE',  ( -3.071710424422018668E-17, 6.404604876783312462E-16, 1.000000000000000000 ) ) ;
#22220=CYLINDRICAL_SURFACE ( 'NONE', #13271, 1.999999999999999556 ) ;
#22223=CARTESIAN_POINT ( 'NONE',  ( -17.42558057905623059, -9.559206755253617516, 52.02966884056656482 ) ) ;
#22226=EDGE_LOOP ( 'NONE', ( #6285, #48012, #42560, #8356 ) ) ;
#22229=EDGE_CURVE ( 'NONE', #40825, #36429, #12, .T. ) ;
#22237=ORIENTED_EDGE ( 'NONE', *, *, #48263, .T. ) ;
#22244=VERTEX_POINT ( 'NONE', #39684 ) ;
#22247=FACE_OUTER_BOUND ( 'NONE', #24378, .T. ) ;
#22288=EDGE_CURVE ( 'NONE', #44188, #21060, #40914, .T. ) ;
#22289=DIRECTION ( 'NONE',  ( 0.9687793358424821033, -0.2479245821708677133, 0.000000000000000000 ) ) ;
#22295=EDGE_CURVE ( 'NONE', #10862, #23394, #3158, .T. ) ;
#22297=ORIENTED_EDGE ( 'NONE', *, *, #27763, .F. ) ;
#22302=CIRCLE ( 'NONE', #27052, 2.000000000000001776 ) ;
#22304=DIRECTION ( 'NONE',  ( 0.9687793358424817702, -0.2479245821708684905, 0.000000000000000000 ) ) ;
#22314=DIRECTION ( 'NONE',  ( 0.9180681052388952601, -0.3964226963016432292, 0.000000000000000000 ) ) ;
#22316=FACE_OUTER_BOUND ( 'NONE', #9779, .T. ) ;
#22317=DIRECTION ( 'NONE',  ( -3.071710424422018668E-17, 6.404604876783312462E-16, 1.000000000000000000 ) ) ;
#22328=ORIENTED_EDGE ( 'NONE', *, *, #38370, .F. ) ;
#22351=EDGE_CURVE ( 'NONE', #40523, #17101, #10245, .T. ) ;
#22355=DIRECTION ( 'NONE',  ( -0.9687793358424822143, 0.2479245821708672415, 0.000000000000000000 ) ) ;
#22371=EDGE_CURVE ( 'NONE', #3267, #19390, #816, .T. ) ;
#22374=AXIS2_PLACEMENT_3D ( 'NONE', #13520, #28065, #24144 ) ;
#22376=ORIENTED_EDGE ( 'NONE', *, *, #4529, .T. ) ;
#22395=CYLINDRICAL_SURFACE ( 'NONE', #29207, 5.249999999999998224 ) ;
#22407=VECTOR ( 'NONE', #48539, 1000.000000000000000 ) ;
#22413=CARTESIAN_POINT ( 'NONE',  ( -17.42409385541299471, -14.80920654474435594, 52.02966884056656482 ) ) ;
#22414=EDGE_LOOP ( 'NONE', ( #8164, #8290, #3698, #2001 ) ) ;
#22423=DIRECTION ( 'NONE',  ( -3.071710424422018668E-17, 6.404604876783312462E-16, 1.000000000000000000 ) ) ;
#22427=EDGE_CURVE ( 'NONE', #20224, #3327, #1583, .T. ) ;
#22437=CIRCLE ( 'NONE', #10629, 4.686499999999998778 ) ;
#22458=CARTESIAN_POINT ( 'NONE',  ( -19.36557164464469594, -19.08778335711046026, 49.52966884056656482 ) ) ;
#22459=DIRECTION ( 'NONE',  ( 0.09332174201254166135, 0.9956360040033429559, 0.000000000000000000 ) ) ;
#22468=ORIENTED_EDGE ( 'NONE', *, *, #36200, .T. ) ;
#22470=FILL_AREA_STYLE ('',( #11627 ) ) ;
#22474=DIRECTION ( 'NONE',  ( 0.9687793358424821033, -0.2479245821708677133, 0.000000000000000000 ) ) ;
#22487=FACE_BOUND ( 'NONE', #21160, .T. ) ;
#22510=DIRECTION ( 'NONE',  ( 3.071710424422018668E-17, -6.404604876783312462E-16, -1.000000000000000000 ) ) ;
#22523=ORIENTED_EDGE ( 'NONE', *, *, #39407, .F. ) ;
#22524=EDGE_LOOP ( 'NONE', ( #23250, #30754, #15727, #36687 ) ) ;
#22530=ORIENTED_EDGE ( 'NONE', *, *, #24474, .F. ) ;
#22535=EDGE_LOOP ( 'NONE', ( #222, #31664, #44503, #6678 ) ) ;
#22538=VECTOR ( 'NONE', #24668, 1000.000000000000000 ) ;
#22549=VECTOR ( 'NONE', #39099, 1000.000000000000000 ) ;
#22552=ORIENTED_EDGE ( 'NONE', *, *, #28294, .F. ) ;
#22553=CARTESIAN_POINT ( 'NONE',  ( -15.04196850781542771, -10.13074752191075234, 50.77966884056655772 ) ) ;
#22562=CYLINDRICAL_SURFACE ( 'NONE', #15646, 1.999999999999999556 ) ;
#22563=VERTEX_POINT ( 'NONE', #9115 ) ;
#22574=VERTEX_POINT ( 'NONE', #10561 ) ;
#22578=DIRECTION ( 'NONE',  ( -3.071710424422018668E-17, 6.404604876783312462E-16, 1.000000000000000000 ) ) ;
#22582=CARTESIAN_POINT ( 'NONE',  ( -14.36038767613011302, -18.37140530287405582, 49.52966884056656482 ) ) ;
#22591=CIRCLE ( 'NONE', #33560, 2.000000000000000888 ) ;
#22595=ORIENTED_EDGE ( 'NONE', *, *, #6646, .T. ) ;
#22611=CARTESIAN_POINT ( 'NONE',  ( -13.86189509728330904, -11.74550036546146004, 49.52966884056655772 ) ) ;
#22614=ORIENTED_EDGE ( 'NONE', *, *, #37210, .F. ) ;
#22619=CARTESIAN_POINT ( 'NONE',  ( -17.42409385541299471, -14.80920654474435771, 49.52966884056655772 ) ) ;
#22633=DIRECTION ( 'NONE',  ( -3.071710424422018668E-17, 6.404604876783312462E-16, 1.000000000000000000 ) ) ;
#22647=VECTOR ( 'NONE', #19776, 1000.000000000000000 ) ;
#22654=ORIENTED_EDGE ( 'NONE', *, *, #33042, .T. ) ;
#22656=DIRECTION ( 'NONE',  ( -3.071710424422018668E-17, 6.404604876783312462E-16, 1.000000000000000000 ) ) ;
#22670=ORIENTED_EDGE ( 'NONE', *, *, #25170, .F. ) ;
#22690=AXIS2_PLACEMENT_3D ( 'NONE', #8103, #30514, #7370 ) ;
#22692=CYLINDRICAL_SURFACE ( 'NONE', #25112, 4.686499999999997002 ) ;
#22704=ORIENTED_EDGE ( 'NONE', *, *, #25101, .T. ) ;
#22706=DIRECTION ( 'NONE',  ( -3.071710424422018668E-17, 6.404604876783312462E-16, 1.000000000000000000 ) ) ;
#22707=AXIS2_PLACEMENT_3D ( 'NONE', #27025, #18643, #22355 ) ;
#22711=DIRECTION ( 'NONE',  ( 0.9687793358424819923, -0.2479245821708678243, 0.000000000000000000 ) ) ;
#22716=LINE ( 'NONE', #23696, #8554 ) ;
#22720=ADVANCED_FACE ( 'NONE', ( #26552 ), #30263, .T. ) ;
#22723=( LENGTH_UNIT ( ) NAMED_UNIT ( * ) SI_UNIT ( .MILLI., .METRE. ) );
#22726=EDGE_CURVE ( 'NONE', #47056, #8151, #14621, .T. ) ;
#22730=AXIS2_PLACEMENT_3D ( 'NONE', #26875, #33990, #517 ) ;
#22734=CIRCLE ( 'NONE', #43973, 2.000000000000000888 ) ;
#22745=DIRECTION ( 'NONE',  ( -3.071710424422018668E-17, 6.404604876783312462E-16, 1.000000000000000000 ) ) ;
#22751=DIRECTION ( 'NONE',  ( -3.071710424422018668E-17, 6.404604876783312462E-16, 1.000000000000000000 ) ) ;
#22753=DIRECTION ( 'NONE',  ( 0.2479245821708711550, 0.9687793358424812151, 0.000000000000000000 ) ) ;
#22766=LINE ( 'NONE', #10689, #33736 ) ;
#22770=FACE_OUTER_BOUND ( 'NONE', #26730, .T. ) ;
#22776=DIRECTION ( 'NONE',  ( 0.06357898915123498529, -0.9979768094191904249, 0.000000000000000000 ) ) ;
#22782=CARTESIAN_POINT ( 'NONE',  ( -22.41759978862804914, -13.18828134753566239, 52.02966884056656482 ) ) ;
#22785=VERTEX_POINT ( 'NONE', #35139 ) ;
#22792=EDGE_CURVE ( 'NONE', #25029, #17957, #12744, .T. ) ;
#22799=ORIENTED_EDGE ( 'NONE', *, *, #19280, .T. ) ;
#22810=AXIS2_PLACEMENT_3D ( 'NONE', #11777, #22872, #25810 ) ;
#22814=EDGE_LOOP ( 'NONE', ( #9707, #39915, #9730, #8036 ) ) ;
#22817=DIRECTION ( 'NONE',  ( 3.071710424422018668E-17, -6.404604876783312462E-16, -1.000000000000000000 ) ) ;
#22821=DIRECTION ( 'NONE',  ( -3.071710424422018668E-17, 6.404604876783312462E-16, 1.000000000000000000 ) ) ;
#22822=AXIS2_PLACEMENT_3D ( 'NONE', #23850, #17815, #47878 ) ;
#22824=DIRECTION ( 'NONE',  ( 0.9687793358424819923, -0.2479245821708680464, 0.000000000000000000 ) ) ;
#22827=ORIENTED_EDGE ( 'NONE', *, *, #31030, .F. ) ;
#22830=LINE ( 'NONE', #3607, #9399 ) ;
#22831=ORIENTED_EDGE ( 'NONE', *, *, #27670, .F. ) ;
#22835=ORIENTED_EDGE ( 'NONE', *, *, #11805, .F. ) ;
#22846=AXIS2_PLACEMENT_3D ( 'NONE', #3128, #2879, #47704 ) ;
#22847=ORIENTED_EDGE ( 'NONE', *, *, #17702, .F. ) ;
#22852=AXIS2_PLACEMENT_3D ( 'NONE', #21265, #36721, #3010 ) ;
#22857=EDGE_CURVE ( 'NONE', #43487, #43698, #39810, .T. ) ;
#22866=DIRECTION ( 'NONE',  ( -0.8447509909909768355, 0.5351595679979596065, 0.000000000000000000 ) ) ;
#22867=DIRECTION ( 'NONE',  ( -0.7506333037770538397, 0.6607190350373941534, 0.000000000000000000 ) ) ;
#22869=VERTEX_POINT ( 'NONE', #41443 ) ;
#22870=DIRECTION ( 'NONE',  ( 0.9687793358424821033, -0.2479245821708677133, 0.000000000000000000 ) ) ;
#22871=EDGE_CURVE ( 'NONE', #32161, #34423, #41207, .T. ) ;
#22872=DIRECTION ( 'NONE',  ( -3.071710424422018668E-17, 6.404604876783312462E-16, 1.000000000000000000 ) ) ;
#22874=ORIENTED_EDGE ( 'NONE', *, *, #1031, .T. ) ;
#22876=AXIS2_PLACEMENT_3D ( 'NONE', #5648, #13231, #6109 ) ;
#22891=DIRECTION ( 'NONE',  ( 0.9687793358424821033, -0.2479245821708680464, 0.000000000000000000 ) ) ;
#22892=AXIS2_PLACEMENT_3D ( 'NONE', #15077, #19274, #809 ) ;
#22905=DIRECTION ( 'NONE',  ( 0.6607190350373968180, 0.7506333037770515082, 0.000000000000000000 ) ) ;
#22932=EDGE_CURVE ( 'NONE', #19285, #7976, #3205, .T. ) ;
#22933=ORIENTED_EDGE ( 'NONE', *, *, #12349, .T. ) ;
#22937=VERTEX_POINT ( 'NONE', #14017 ) ;
#22943=DIRECTION ( 'NONE',  ( 3.071710424422018668E-17, -6.404604876783312462E-16, -1.000000000000000000 ) ) ;
#22965=CIRCLE ( 'NONE', #1715, 1.999999999999999556 ) ;
#22966=DIRECTION ( 'NONE',  ( 0.9687793358424821033, -0.2479245821708677133, 0.000000000000000000 ) ) ;
#22975=CIRCLE ( 'NONE', #28448, 2.000000000000001776 ) ;
#22978=VECTOR ( 'NONE', #15114, 1000.000000000000000 ) ;
#22993=EDGE_LOOP ( 'NONE', ( #36132, #5426, #31775, #42200 ) ) ;
#22994=CYLINDRICAL_SURFACE ( 'NONE', #22892, 4.686499999999997002 ) ;
#23003=DIRECTION ( 'NONE',  ( -3.071710424422018668E-17, 6.404604876783312462E-16, 1.000000000000000000 ) ) ;
#23014=FACE_OUTER_BOUND ( 'NONE', #2299, .T. ) ;
#23026=DIRECTION ( 'NONE',  ( 0.9687793358424821033, -0.2479245821708679909, 0.000000000000000000 ) ) ;
#23030=ORIENTED_EDGE ( 'NONE', *, *, #25630, .F. ) ;
#23031=ORIENTED_EDGE ( 'NONE', *, *, #11852, .T. ) ;
#23035=CYLINDRICAL_SURFACE ( 'NONE', #19781, 5.249999999999998224 ) ;
#23038=DIRECTION ( 'NONE',  ( -3.071710424422018668E-17, 6.404604876783312462E-16, 1.000000000000000000 ) ) ;
#23058=ORIENTED_EDGE ( 'NONE', *, *, #20324, .F. ) ;
#23061=CARTESIAN_POINT ( 'NONE',  ( -22.63183829035100914, -15.47396055967928952, 52.02966884056656482 ) ) ;
#23072=EDGE_CURVE ( 'NONE', #47558, #37481, #23385, .T. ) ;
#23096=LINE ( 'NONE', #23330, #507 ) ;
#23100=ORIENTED_EDGE ( 'NONE', *, *, #1893, .F. ) ;
#23111=ORIENTED_EDGE ( 'NONE', *, *, #38859, .F. ) ;
#23112=DIRECTION ( 'NONE',  ( -3.071710424422018668E-17, 6.404604876783312462E-16, 1.000000000000000000 ) ) ;
#23114=EDGE_LOOP ( 'NONE', ( #28483, #23690, #41956, #11531 ) ) ;
#23116=DIRECTION ( 'NONE',  ( -0.3964226963016468375, -0.9180681052388937058, 0.000000000000000000 ) ) ;
#23119=ORIENTED_EDGE ( 'NONE', *, *, #17808, .F. ) ;
#23124=ORIENTED_EDGE ( 'NONE', *, *, #3198, .F. ) ;
#23143=ORIENTED_EDGE ( 'NONE', *, *, #19658, .F. ) ;
#23144=ADVANCED_FACE ( 'NONE', ( #46766 ), #20427, .T. ) ;
#23154=ORIENTED_EDGE ( 'NONE', *, *, #35579, .F. ) ;
#23156=AXIS2_PLACEMENT_3D ( 'NONE', #33762, #7944, #30103 ) ;
#23197=EDGE_LOOP ( 'NONE', ( #176, #13556, #36541, #4502 ) ) ;
#23201=DIRECTION ( 'NONE',  ( -3.071710424422018668E-17, 6.404604876783312462E-16, 1.000000000000000000 ) ) ;
#23221=ORIENTED_EDGE ( 'NONE', *, *, #19714, .F. ) ;
#23223=EDGE_CURVE ( 'NONE', #34094, #32811, #46040, .T. ) ;
#23238=CARTESIAN_POINT ( 'NONE',  ( -16.36862302632751209, -10.24310716135927812, 52.02966884056656482 ) ) ;
#23241=DIRECTION ( 'NONE',  ( -3.071710424422018668E-17, 6.404604876783312462E-16, 1.000000000000000000 ) ) ;
#23244=EDGE_CURVE ( 'NONE', #18974, #46408, #44552, .T. ) ;
#23247=ORIENTED_EDGE ( 'NONE', *, *, #1038, .F. ) ;
#23250=ORIENTED_EDGE ( 'NONE', *, *, #30365, .T. ) ;
#23255=EDGE_LOOP ( 'NONE', ( #14525, #14144, #7690, #7258 ) ) ;
#23261=DIRECTION ( 'NONE',  ( -0.7506333037770542838, 0.6607190350373937093, 0.000000000000000000 ) ) ;
#23264=ORIENTED_EDGE ( 'NONE', *, *, #2952, .F. ) ;
#23267=LINE ( 'NONE', #30904, #12283 ) ;
#23285=ORIENTED_EDGE ( 'NONE', *, *, #4735, .F. ) ;
#23292=DIRECTION ( 'NONE',  ( -3.071710424422018668E-17, 6.404604876783312462E-16, 1.000000000000000000 ) ) ;
#23303=DIRECTION ( 'NONE',  ( 0.9687793358424821033, -0.2479245821708680464, 0.000000000000000000 ) ) ;
#23309=ORIENTED_EDGE ( 'NONE', *, *, #11497, .T. ) ;
#23312=CYLINDRICAL_SURFACE ( 'NONE', #16900, 1.999999999999999556 ) ;
#23313=DIRECTION ( 'NONE',  ( -3.071710424422018668E-17, 6.404604876783312462E-16, 1.000000000000000000 ) ) ;
#23315=CARTESIAN_POINT ( 'NONE',  ( -13.44904343725875684, -12.32681728777199481, 49.52966884056655772 ) ) ;
#23324=EDGE_CURVE ( 'NONE', #32458, #14076, #8377, .T. ) ;
#23325=AXIS2_PLACEMENT_3D ( 'NONE', #30511, #42305, #16171 ) ;
#23326=CIRCLE ( 'NONE', #4437, 5.249999999999998224 ) ;
#23330=CARTESIAN_POINT ( 'NONE',  ( -14.24626305875727184, -11.36469298288595731, 49.52966884056655772 ) ) ;
#23334=CYLINDRICAL_SURFACE ( 'NONE', #10110, 2.000000000000001332 ) ;
#23338=CARTESIAN_POINT ( 'NONE',  ( -22.60969001043771698, -13.98939405582217432, 49.52966884056655772 ) ) ;
#23348=CYLINDRICAL_SURFACE ( 'NONE', #23468, 4.686499999999997002 ) ;
#23363=EDGE_LOOP ( 'NONE', ( #10812, #28028, #37827, #42898 ) ) ;
#23374=VERTEX_POINT ( 'NONE', #19885 ) ;
#23381=EDGE_CURVE ( 'NONE', #36678, #29084, #27223, .T. ) ;
#23385=LINE ( 'NONE', #37400, #35884 ) ;
#23394=VERTEX_POINT ( 'NONE', #1394 ) ;
#23405=CARTESIAN_POINT ( 'NONE',  ( -21.43863153483710349, -12.36809147865652747, 52.02966884056656482 ) ) ;
#23413=CARTESIAN_POINT ( 'NONE',  ( -22.17153284776674482, -17.05070671513899683, 50.77966884056655772 ) ) ;
#23423=ORIENTED_EDGE ( 'NONE', *, *, #18084, .T. ) ;
#23439=AXIS2_PLACEMENT_3D ( 'NONE', #1785, #27643, #27161 ) ;
#23449=ORIENTED_EDGE ( 'NONE', *, *, #24056, .F. ) ;
#23450=EDGE_CURVE ( 'NONE', #19139, #7346, #45762, .T. ) ;
#23452=DIRECTION ( 'NONE',  ( 0.9687793358424821033, -0.2479245821708677133, 0.000000000000000000 ) ) ;
#23467=VECTOR ( 'NONE', #37429, 1000.000000000000000 ) ;
#23468=AXIS2_PLACEMENT_3D ( 'NONE', #9304, #12746, #20384 ) ;
#23474=DIRECTION ( 'NONE',  ( 0.9687793358424821033, -0.2479245821708680464, 0.000000000000000000 ) ) ;
#23481=CARTESIAN_POINT ( 'NONE',  ( -17.42409385541299471, -14.80920654474435771, 49.52966884056655772 ) ) ;
#23484=CARTESIAN_POINT ( 'NONE',  ( -12.85169559483840374, -15.89028456787280952, 49.52966884056655772 ) ) ;
#23507=AXIS2_PLACEMENT_3D ( 'NONE', #34208, #499, #21920 ) ;
#23524=DIRECTION ( 'NONE',  ( -3.071710424422018668E-17, 6.404604876783312462E-16, 1.000000000000000000 ) ) ;
#23528=DIRECTION ( 'NONE',  ( -3.071710424422018668E-17, 6.404604876783312462E-16, 1.000000000000000000 ) ) ;
#23532=CIRCLE ( 'NONE', #16443, 4.686499999999999666 ) ;
#23541=AXIS2_PLACEMENT_3D ( 'NONE', #9253, #39286, #20815 ) ;
#23542=DIRECTION ( 'NONE',  ( -3.071710424422018668E-17, 6.404604876783312462E-16, 1.000000000000000000 ) ) ;
#23546=DIRECTION ( 'NONE',  ( -3.071710424422018668E-17, 6.404604876783312462E-16, 1.000000000000000000 ) ) ;
#23555=DIRECTION ( 'NONE',  ( 0.8447509909909731718, -0.5351595679979654907, 0.000000000000000000 ) ) ;
#23556=ADVANCED_FACE ( 'NONE', ( #2614 ), #13672, .T. ) ;
#23559=EDGE_LOOP ( 'NONE', ( #35386, #11178, #24471, #3883 ) ) ;
#23570=FACE_OUTER_BOUND ( 'NONE', #22993, .T. ) ;
#23582=ORIENTED_EDGE ( 'NONE', *, *, #17244, .F. ) ;
#23586=CARTESIAN_POINT ( 'NONE',  ( -15.95285335075216970, -19.84884456522215146, 52.02966884056656482 ) ) ;
#23592=DIRECTION ( 'NONE',  ( -3.071710424422018668E-17, 6.404604876783312462E-16, 1.000000000000000000 ) ) ;
#23593=EDGE_LOOP ( 'NONE', ( #6529, #11082, #28128, #26672 ) ) ;
#23596=DIRECTION ( 'NONE',  ( 0.3688590060343580612, -0.9294853595766560117, 0.000000000000000000 ) ) ;
#23598=ORIENTED_EDGE ( 'NONE', *, *, #28165, .F. ) ;
#23602=VECTOR ( 'NONE', #19948, 1000.000000000000000 ) ;
#23608=CARTESIAN_POINT ( 'NONE',  ( -17.42409385541299471, -14.80920654474435771, 49.52966884056655772 ) ) ;
#23610=ORIENTED_EDGE ( 'NONE', *, *, #45395, .F. ) ;
#23617=ADVANCED_FACE ( 'NONE', ( #37291 ), #26480, .T. ) ;
#23624=VECTOR ( 'NONE', #47502, 1000.000000000000000 ) ;
#23627=DIRECTION ( 'NONE',  ( -3.071710424422018668E-17, 6.404604876783312462E-16, 1.000000000000000000 ) ) ;
#23636=DIRECTION ( 'NONE',  ( -0.8603395911234870130, -0.5097212845717461471, 0.000000000000000000 ) ) ;
#23642=AXIS2_PLACEMENT_3D ( 'NONE', #29571, #10856, #40895 ) ;
#23645=ORIENTED_EDGE ( 'NONE', *, *, #7381, .T. ) ;
#23646=VECTOR ( 'NONE', #46527, 1000.000000000000000 ) ;
#23649=ORIENTED_EDGE ( 'NONE', *, *, #38846, .F. ) ;
#23667=ORIENTED_EDGE ( 'NONE', *, *, #13742, .F. ) ;
#23690=ORIENTED_EDGE ( 'NONE', *, *, #4845, .T. ) ;
#23696=CARTESIAN_POINT ( 'NONE',  ( -17.83128375312269753, -10.14042954887026049, 49.52966884056655772 ) ) ;
#23715=AXIS2_PLACEMENT_3D ( 'NONE', #47215, #36580, #2865 ) ;
#23728=DIRECTION ( 'NONE',  ( 0.9687793358424822143, -0.2479245821708672415, 0.000000000000000000 ) ) ;
#23756=ADVANCED_FACE ( 'NONE', ( #15872 ), #8758, .T. ) ;
#23758=EDGE_CURVE ( 'NONE', #36333, #48460, #21863, .T. ) ;
#23766=DIRECTION ( 'NONE',  ( 0.9687793358424819923, -0.2479245821708678243, 0.000000000000000000 ) ) ;
#23778=AXIS2_PLACEMENT_3D ( 'NONE', #6484, #33036, #9931 ) ;
#23803=VERTEX_POINT ( 'NONE', #34832 ) ;
#23843=DIRECTION ( 'NONE',  ( 0.9687793358424821033, -0.2479245821708677133, 0.000000000000000000 ) ) ;
#23845=CARTESIAN_POINT ( 'NONE',  ( -16.17583575424048092, -10.27959207348368587, 52.02966884056656482 ) ) ;
#23850=CARTESIAN_POINT ( 'NONE',  ( -17.42409385541299471, -14.80920654474434883, 62.02966884056656482 ) ) ;
#23869=VERTEX_POINT ( 'NONE', #9955 ) ;
#23871=DIRECTION ( 'NONE',  ( -3.071710424422018668E-17, 6.404604876783312462E-16, 1.000000000000000000 ) ) ;
#23874=DIRECTION ( 'NONE',  ( -0.8447509909909771686, 0.5351595679979589404, 0.000000000000000000 ) ) ;
#23878=VERTEX_POINT ( 'NONE', #39263 ) ;
#23883=EDGE_CURVE ( 'NONE', #16869, #38050, #4537, .T. ) ;
#23898=ORIENTED_EDGE ( 'NONE', *, *, #32523, .F. ) ;
#23908=CARTESIAN_POINT ( 'NONE',  ( -17.42409385541299471, -14.80920654474435594, 52.02966884056656482 ) ) ;
#23918=ORIENTED_EDGE ( 'NONE', *, *, #28547, .T. ) ;
#23951=ORIENTED_EDGE ( 'NONE', *, *, #7749, .F. ) ;
#23954=DIRECTION ( 'NONE',  ( 3.071710424422018668E-17, -6.404604876783312462E-16, -1.000000000000000000 ) ) ;
#23980=CARTESIAN_POINT ( 'NONE',  ( -12.67665486305926237, -12.56770637434968485, 49.52966884056655772 ) ) ;
#24012=ADVANCED_FACE ( 'NONE', ( #10205 ), #29631, .T. ) ;
#24014=ADVANCED_FACE ( 'NONE', ( #22247 ), #6984, .T. ) ;
#24028=CARTESIAN_POINT ( 'NONE',  ( -13.95487512861695834, -17.97781459419518058, 52.02966884056656482 ) ) ;
#24029=FACE_OUTER_BOUND ( 'NONE', #41364, .T. ) ;
#24044=ORIENTED_EDGE ( 'NONE', *, *, #47941, .T. ) ;
#24054=CARTESIAN_POINT ( 'NONE',  ( -17.63665770386090514, -10.11555421891855922, 52.02966884056656482 ) ) ;
#24056=EDGE_CURVE ( 'NONE', #18974, #1509, #12371, .T. ) ;
#24070=CARTESIAN_POINT ( 'NONE',  ( -19.89283007060495123, -10.81159512726059191, 49.52966884056655772 ) ) ;
#24111=VERTEX_POINT ( 'NONE', #20011 ) ;
#24121=ORIENTED_EDGE ( 'NONE', *, *, #35721, .T. ) ;
#24138=VERTEX_POINT ( 'NONE', #4501 ) ;
#24143=ORIENTED_EDGE ( 'NONE', *, *, #13800, .F. ) ;
#24144=DIRECTION ( 'NONE',  ( 0.9687793358424821033, -0.2479245821708679909, 0.000000000000000000 ) ) ;
#24147=PLANE ( 'NONE',  #29007 ) ;
#24151=CARTESIAN_POINT ( 'NONE',  ( -17.42409385541299471, -14.80920654474435771, 49.52966884056655772 ) ) ;
#24175=DIRECTION ( 'NONE',  ( -3.071710424422018668E-17, 6.404604876783312462E-16, 1.000000000000000000 ) ) ;
#24176=AXIS2_PLACEMENT_3D ( 'NONE', #26916, #41930, #28367 ) ;
#24201=ORIENTED_EDGE ( 'NONE', *, *, #31986, .T. ) ;
#24207=CARTESIAN_POINT ( 'NONE',  ( -22.07864594086649390, -14.26292169798353804, 52.02966884056656482 ) ) ;
#24209=ORIENTED_EDGE ( 'NONE', *, *, #11005, .T. ) ;
#24221=AXIS2_PLACEMENT_3D ( 'NONE', #26382, #6940, #33496 ) ;
#24224=DIRECTION ( 'NONE',  ( 0.9180681052388952601, -0.3964226963016427852, 0.000000000000000000 ) ) ;
#24248=DIRECTION ( 'NONE',  ( -0.5351595679979681552, -0.8447509909909712844, 0.000000000000000000 ) ) ;
#24257=VERTEX_POINT ( 'NONE', #22188 ) ;
#24262=CARTESIAN_POINT ( 'NONE',  ( -17.42409385541299471, -14.80920654474434883, 62.02966884056656482 ) ) ;
#24264=ORIENTED_EDGE ( 'NONE', *, *, #23223, .F. ) ;
#24268=CYLINDRICAL_SURFACE ( 'NONE', #36062, 4.686499999999997002 ) ;
#24270=AXIS2_PLACEMENT_3D ( 'NONE', #22069, #3851, #25513 ) ;
#24273=AXIS2_PLACEMENT_3D ( 'NONE', #787, #11618, #41660 ) ;
#24282=ORIENTED_EDGE ( 'NONE', *, *, #46303, .T. ) ;
#24285=VECTOR ( 'NONE', #32065, 1000.000000000000000 ) ;
#24303=CARTESIAN_POINT ( 'NONE',  ( -14.51911023200684703, -18.48675360735852280, 49.52966884056656482 ) ) ;
#24317=FACE_OUTER_BOUND ( 'NONE', #371, .T. ) ;
#24320=ORIENTED_EDGE ( 'NONE', *, *, #33371, .F. ) ;
#24321=DIRECTION ( 'NONE',  ( -3.071710424422018668E-17, 6.404604876783312462E-16, 1.000000000000000000 ) ) ;
#24338=CARTESIAN_POINT ( 'NONE',  ( -17.61266704711333375, -10.12650194148654137, 49.52966884056655772 ) ) ;
#24344=CIRCLE ( 'NONE', #28277, 5.249999999999998224 ) ;
#24345=AXIS2_PLACEMENT_3D ( 'NONE', #27829, #12569, #32011 ) ;
#24353=LINE ( 'NONE', #5153, #23646 ) ;
#24355=VECTOR ( 'NONE', #15579, 1000.000000000000000 ) ;
#24359=ORIENTED_EDGE ( 'NONE', *, *, #32338, .F. ) ;
#24378=EDGE_LOOP ( 'NONE', ( #34984, #3817, #23111, #7596 ) ) ;
#24393=FACE_OUTER_BOUND ( 'NONE', #23593, .T. ) ;
#24394=AXIS2_PLACEMENT_3D ( 'NONE', #14111, #19906, #47408 ) ;
#24395=ORIENTED_EDGE ( 'NONE', *, *, #22351, .F. ) ;
#24396=VERTEX_POINT ( 'NONE', #26866 ) ;
#24399=ORIENTED_EDGE ( 'NONE', *, *, #186, .T. ) ;
#24428=EDGE_CURVE ( 'NONE', #15180, #32458, #48576, .T. ) ;
#24433=DIRECTION ( 'NONE',  ( -0.7700094066334561838, -0.6380325334150231953, 0.000000000000000000 ) ) ;
#24438=ORIENTED_EDGE ( 'NONE', *, *, #16951, .F. ) ;
#24445=DIRECTION ( 'NONE',  ( 0.9687793358424821033, -0.2479245821708677133, 0.000000000000000000 ) ) ;
#24448=AXIS2_PLACEMENT_3D ( 'NONE', #45827, #18983, #33987 ) ;
#24471=ORIENTED_EDGE ( 'NONE', *, *, #32046, .F. ) ;
#24474=EDGE_CURVE ( 'NONE', #39405, #31233, #30322, .T. ) ;
#24490=EDGE_CURVE ( 'NONE', #9114, #30036, #3016, .T. ) ;
#24493=EDGE_CURVE ( 'NONE', #1460, #39153, #5420, .T. ) ;
#24497=ORIENTED_EDGE ( 'NONE', *, *, #7164, .T. ) ;
#24513=DIRECTION ( 'NONE',  ( -3.071710424422018668E-17, 6.404604876783312462E-16, 1.000000000000000000 ) ) ;
#24514=DIRECTION ( 'NONE',  ( 0.9687793358424821033, -0.2479245821708677133, 0.000000000000000000 ) ) ;
#24523=CARTESIAN_POINT ( 'NONE',  ( -22.10677449762105340, -15.19398901379252820, 49.52966884056655772 ) ) ;
#24528=FACE_OUTER_BOUND ( 'NONE', #24750, .T. ) ;
#24538=AXIS2_PLACEMENT_3D ( 'NONE', #13961, #44061, #36862 ) ;
#24540=DIRECTION ( 'NONE',  ( -3.071710424422018668E-17, 6.404604876783312462E-16, 1.000000000000000000 ) ) ;
#24546=AXIS2_PLACEMENT_3D ( 'NONE', #38222, #4506, #11653 ) ;
#24605=CARTESIAN_POINT ( 'NONE',  ( -14.33701861991839976, -19.05567172067550530, 50.77966884056656482 ) ) ;
#24633=EDGE_CURVE ( 'NONE', #241, #2214, #9334, .T. ) ;
#24639=FACE_OUTER_BOUND ( 'NONE', #11029, .T. ) ;
#24640=DIRECTION ( 'NONE',  ( 0.9687793358424821033, -0.2479245821708679909, 0.000000000000000000 ) ) ;
#24641=EDGE_CURVE ( 'NONE', #11090, #38015, #6921, .T. ) ;
#24643=ORIENTED_EDGE ( 'NONE', *, *, #36623, .F. ) ;
#24653=CYLINDRICAL_SURFACE ( 'NONE', #39663, 5.249999999999998224 ) ;
#24658=CARTESIAN_POINT ( 'NONE',  ( -17.42409385541299471, -14.80920654474435771, 49.52966884056655772 ) ) ;
#24664=CARTESIAN_POINT ( 'NONE',  ( -15.64104502085146642, -10.46221995643221092, 52.02966884056656482 ) ) ;
#24665=EDGE_CURVE ( 'NONE', #2342, #36695, #6803, .T. ) ;
#24668=DIRECTION ( 'NONE',  ( -3.071710424422018668E-17, 6.404604876783312462E-16, 1.000000000000000000 ) ) ;
#24670=AXIS2_PLACEMENT_3D ( 'NONE', #15993, #25040, #40057 ) ;
#24677=DIRECTION ( 'NONE',  ( -3.071710424422018668E-17, 6.404604876783312462E-16, 1.000000000000000000 ) ) ;
#24684=DIRECTION ( 'NONE',  ( -3.071710424422018668E-17, 6.404604876783312462E-16, 1.000000000000000000 ) ) ;
#24696=ADVANCED_FACE ( 'NONE', ( #35078 ), #4567, .T. ) ;
#24700=LINE ( 'NONE', #35751, #40856 ) ;
#24713=CIRCLE ( 'NONE', #48373, 2.000000000000000444 ) ;
#24716=AXIS2_PLACEMENT_3D ( 'NONE', #46369, #12626, #1539 ) ;
#24731=DIRECTION ( 'NONE',  ( 0.9687793358424821033, -0.2479245821708677133, 0.000000000000000000 ) ) ;
#24738=CARTESIAN_POINT ( 'NONE',  ( -17.42409385541299471, -14.80920654474435594, 52.02966884056656482 ) ) ;
#24739=AXIS2_PLACEMENT_3D ( 'NONE', #46079, #4968, #35223 ) ;
#24744=DIRECTION ( 'NONE',  ( -3.071710424422018668E-17, 6.404604876783312462E-16, 1.000000000000000000 ) ) ;
#24745=AXIS2_PLACEMENT_3D ( 'NONE', #28981, #6583, #39822 ) ;
#24750=EDGE_LOOP ( 'NONE', ( #27688, #42480, #30344, #6991 ) ) ;
#24752=CARTESIAN_POINT ( 'NONE',  ( -17.42409385541299471, -14.80920654474435771, 49.52966884056655772 ) ) ;
#24758=CYLINDRICAL_SURFACE ( 'NONE', #45637, 5.249999999999998224 ) ;
#24764=ORIENTED_EDGE ( 'NONE', *, *, #25130, .T. ) ;
#24768=ORIENTED_EDGE ( 'NONE', *, *, #25544, .T. ) ;
#24774=DIRECTION ( 'NONE',  ( 0.9687793358424819923, -0.2479245821708678243, 0.000000000000000000 ) ) ;
#24792=CARTESIAN_POINT ( 'NONE',  ( -17.42409385541299471, -14.80920654474434883, 62.02966884056656482 ) ) ;
#24796=DIRECTION ( 'NONE',  ( 0.9687793358424817702, -0.2479245821708688791, 0.000000000000000000 ) ) ;
#24818=CARTESIAN_POINT ( 'NONE',  ( -17.42409385541299471, -14.80920654474435771, 49.52966884056655772 ) ) ;
#24826=EDGE_CURVE ( 'NONE', #8859, #30479, #16370, .T. ) ;
#24845=ORIENTED_EDGE ( 'NONE', *, *, #31850, .T. ) ;
#24869=CIRCLE ( 'NONE', #31155, 2.000000000000000000 ) ;
#24871=FACE_OUTER_BOUND ( 'NONE', #7999, .T. ) ;
#24876=CARTESIAN_POINT ( 'NONE',  ( -15.00927913818083859, -10.79274639537912783, 49.52966884056655772 ) ) ;
#24880=CARTESIAN_POINT ( 'NONE',  ( -17.42409385541299471, -14.80920654474435594, 52.02966884056656482 ) ) ;
#24885=ADVANCED_FACE ( 'NONE', ( #20575 ), #9493, .T. ) ;
#24886=DIRECTION ( 'NONE',  ( 0.9687793358424804380, -0.2479245821708739583, 0.000000000000000000 ) ) ;
#24887=CARTESIAN_POINT ( 'NONE',  ( -17.42409385541299471, -14.80920654474434883, 62.02966884056656482 ) ) ;
#24891=EDGE_CURVE ( 'NONE', #6295, #28161, #31650, .T. ) ;
#24899=DIRECTION ( 'NONE',  ( 0.8603395911234834603, 0.5097212845717522534, 0.000000000000000000 ) ) ;
#24911=CYLINDRICAL_SURFACE ( 'NONE', #33070, 5.249999999999998224 ) ;
#24919=CARTESIAN_POINT ( 'NONE',  ( -21.70267066777908838, -12.86772875551263873, 52.02966884056656482 ) ) ;
#24924=CARTESIAN_POINT ( 'NONE',  ( -12.82020749880560651, -17.33244462614775827, 50.77966884056655772 ) ) ;
#24931=ORIENTED_EDGE ( 'NONE', *, *, #9683, .F. ) ;
#24951=LINE ( 'NONE', #2053, #40153 ) ;
#24959=ADVANCED_FACE ( 'NONE', ( #15089 ), #105, .T. ) ;
#24964=DIRECTION ( 'NONE',  ( -3.071710424422018668E-17, 6.404604876783312462E-16, 1.000000000000000000 ) ) ;
#24965=ADVANCED_FACE ( 'NONE', ( #10684 ), #33302, .T. ) ;
#24976=CARTESIAN_POINT ( 'NONE',  ( -12.43150676794136089, -13.18545343111794033, 49.52966884056655772 ) ) ;
#25002=CARTESIAN_POINT ( 'NONE',  ( -21.09639645740537617, -17.74003392703708926, 49.52966884056655772 ) ) ;
#25008=AXIS2_PLACEMENT_3D ( 'NONE', #9670, #24684, #12854 ) ;
#25010=ORIENTED_EDGE ( 'NONE', *, *, #15721, .F. ) ;
#25013=CARTESIAN_POINT ( 'NONE',  ( -19.80621920301059902, -19.48766556757794177, 52.02966884056656482 ) ) ;
#25018=CIRCLE ( 'NONE', #47780, 2.000000000000003109 ) ;
#25022=EDGE_CURVE ( 'NONE', #19030, #13430, #30145, .T. ) ;
#25028=CARTESIAN_POINT ( 'NONE',  ( -21.09639645740537617, -17.74003392703708926, 49.52966884056655772 ) ) ;
#25029=VERTEX_POINT ( 'NONE', #29400 ) ;
#25033=ADVANCED_FACE ( 'NONE', ( #36519 ), #21767, .T. ) ;
#25035=FACE_OUTER_BOUND ( 'NONE', #13578, .T. ) ;
#25039=AXIS2_PLACEMENT_3D ( 'NONE', #34170, #41830, #23116 ) ;
#25040=DIRECTION ( 'NONE',  ( -3.071710424422018668E-17, 6.404604876783312462E-16, 1.000000000000000000 ) ) ;
#25045=ORIENTED_EDGE ( 'NONE', *, *, #31080, .T. ) ;
#25051=VECTOR ( 'NONE', #30200, 1000.000000000000000 ) ;
#25066=CYLINDRICAL_SURFACE ( 'NONE', #39699, 5.249999999999998224 ) ;
#25077=CARTESIAN_POINT ( 'NONE',  ( -21.43863153483710349, -12.36809147865652925, 49.52966884056655772 ) ) ;
#25092=LINE ( 'NONE', #40348, #23624 ) ;
#25096=ORIENTED_EDGE ( 'NONE', *, *, #12349, .F. ) ;
#25099=ORIENTED_EDGE ( 'NONE', *, *, #19073, .F. ) ;
#25101=EDGE_CURVE ( 'NONE', #15953, #1752, #17970, .T. ) ;
#25111=AXIS2_PLACEMENT_3D ( 'NONE', #6235, #43181, #17297 ) ;
#25112=AXIS2_PLACEMENT_3D ( 'NONE', #45833, #41151, #38169 ) ;
#25130=EDGE_CURVE ( 'NONE', #4347, #3170, #34514, .T. ) ;
#25136=VERTEX_POINT ( 'NONE', #35022 ) ;
#25158=DIRECTION ( 'NONE',  ( 0.2479245821708712660, 0.9687793358424811041, 0.000000000000000000 ) ) ;
#25170=EDGE_CURVE ( 'NONE', #24138, #47558, #45545, .T. ) ;
#25178=CYLINDRICAL_SURFACE ( 'NONE', #24221, 1.999999999999999556 ) ;
#25191=DIRECTION ( 'NONE',  ( 3.071710424422018668E-17, -6.404604876783312462E-16, -1.000000000000000000 ) ) ;
#25202=ORIENTED_EDGE ( 'NONE', *, *, #26062, .T. ) ;
#25209=CIRCLE ( 'NONE', #36989, 2.000000000000000888 ) ;
#25213=CARTESIAN_POINT ( 'NONE',  ( -20.60192465206874246, -18.25372010660273503, 49.52966884056656482 ) ) ;
#25221=CYLINDRICAL_SURFACE ( 'NONE', #39560, 1.999999999999999112 ) ;
#25224=CIRCLE ( 'NONE', #16562, 1.999999999999999556 ) ;
#25249=AXIS2_PLACEMENT_3D ( 'NONE', #19852, #34853, #31894 ) ;
#25253=LINE ( 'NONE', #7022, #35407 ) ;
#25254=VECTOR ( 'NONE', #37108, 1000.000000000000000 ) ;
#25282=DIRECTION ( 'NONE',  ( -3.071710424422018668E-17, 6.404604876783312462E-16, 1.000000000000000000 ) ) ;
#25283=AXIS2_PLACEMENT_3D ( 'NONE', #13309, #16770, #24433 ) ;
#25302=EDGE_CURVE ( 'NONE', #17349, #44188, #19551, .T. ) ;
#25306=ORIENTED_EDGE ( 'NONE', *, *, #14715, .T. ) ;
#25316=CARTESIAN_POINT ( 'NONE',  ( -17.77658133828675702, -19.49442885748621990, 49.52966884056656482 ) ) ;
#25375=ORIENTED_EDGE ( 'NONE', *, *, #32338, .T. ) ;
#25377=EDGE_CURVE ( 'NONE', #48505, #4743, #10624, .T. ) ;
#25378=CYLINDRICAL_SURFACE ( 'NONE', #39838, 4.686499999999997002 ) ;
#25392=CARTESIAN_POINT ( 'NONE',  ( -21.34628024798174550, -12.22231469401973847, 49.52966884056655772 ) ) ;
#25404=VERTEX_POINT ( 'NONE', #2739 ) ;
#25407=DIRECTION ( 'NONE',  ( 0.9687793358424819923, -0.2479245821708678243, 0.000000000000000000 ) ) ;
#25441=EDGE_CURVE ( 'NONE', #25847, #20972, #20361, .T. ) ;
#25443=CARTESIAN_POINT ( 'NONE',  ( -15.80316865820435446, -9.815700611529285524, 52.02966884056656482 ) ) ;
#25468=CIRCLE ( 'NONE', #4254, 1.999999999999999334 ) ;
#25475=EDGE_LOOP ( 'NONE', ( #29844, #38919, #34928, #46069 ) ) ;
#25480=DIRECTION ( 'NONE',  ( 3.071710424422018668E-17, -6.404604876783312462E-16, -1.000000000000000000 ) ) ;
#25486=DIRECTION ( 'NONE',  ( -3.071710424422018668E-17, 6.404604876783312462E-16, 1.000000000000000000 ) ) ;
#25489=AXIS2_PLACEMENT_3D ( 'NONE', #29172, #25715, #36766 ) ;
#25509=DIRECTION ( 'NONE',  ( -3.071710424422018668E-17, 6.404604876783312462E-16, 1.000000000000000000 ) ) ;
#25510=DIRECTION ( 'NONE',  ( -0.09332174201254901658, -0.9956360040033422898, 0.000000000000000000 ) ) ;
#25513=DIRECTION ( 'NONE',  ( 0.9180681052388952601, -0.3964226963016432292, 0.000000000000000000 ) ) ;
#25515=EDGE_LOOP ( 'NONE', ( #33715, #2129, #29521, #5316 ) ) ;
#25529=AXIS2_PLACEMENT_3D ( 'NONE', #39029, #1117, #31655 ) ;
#25537=ADVANCED_FACE ( 'NONE', ( #19958 ), #4448, .T. ) ;
#25542=ORIENTED_EDGE ( 'NONE', *, *, #18647, .F. ) ;
#25544=EDGE_CURVE ( 'NONE', #20471, #42275, #35288, .T. ) ;
#25554=DIRECTION ( 'NONE',  ( -3.071710424422018668E-17, 6.404604876783312462E-16, 1.000000000000000000 ) ) ;
#25565=CIRCLE ( 'NONE', #20863, 1.999999999999998668 ) ;
#25574=CARTESIAN_POINT ( 'NONE',  ( -16.56761320685650318, -19.87745396966068157, 49.52966884056656482 ) ) ;
#25581=DIRECTION ( 'NONE',  ( -0.9757441136919988711, -0.2189141945955433433, 0.000000000000000000 ) ) ;
#25603=EDGE_LOOP ( 'NONE', ( #26886, #22704, #838, #45719 ) ) ;
#25630=EDGE_CURVE ( 'NONE', #28899, #39514, #21925, .T. ) ;
#25632=CARTESIAN_POINT ( 'NONE',  ( -17.42409385541299471, -14.80920654474435771, 49.52966884056655772 ) ) ;
#25633=ORIENTED_EDGE ( 'NONE', *, *, #46838, .F. ) ;
#25636=CARTESIAN_POINT ( 'NONE',  ( -17.26599293058224305, -9.561587646847172550, 50.77966884056655772 ) ) ;
#25642=EDGE_LOOP ( 'NONE', ( #1775, #28370, #9414, #10611 ) ) ;
#25645=VERTEX_POINT ( 'NONE', #20926 ) ;
#25657=CARTESIAN_POINT ( 'NONE',  ( -14.38502091232239621, -11.22596901536237013, 49.52966884056655772 ) ) ;
#25666=VECTOR ( 'NONE', #19936, 1000.000000000000000 ) ;
#25667=ORIENTED_EDGE ( 'NONE', *, *, #1432, .F. ) ;
#25670=ORIENTED_EDGE ( 'NONE', *, *, #9178, .F. ) ;
#25692=CARTESIAN_POINT ( 'NONE',  ( -21.75868347184070473, -16.62218431696164345, 49.52966884056655772 ) ) ;
#25693=CARTESIAN_POINT ( 'NONE',  ( -17.42409385541299471, -14.80920654474435771, 49.52966884056655772 ) ) ;
#25708=DIRECTION ( 'NONE',  ( -3.071710424422018668E-17, 6.404604876783312462E-16, 1.000000000000000000 ) ) ;
#25712=CYLINDRICAL_SURFACE ( 'NONE', #32149, 1.999999999999999112 ) ;
#25713=CARTESIAN_POINT ( 'NONE',  ( -12.74563483257940177, -17.19133189234193893, 50.77966884056655772 ) ) ;
#25715=DIRECTION ( 'NONE',  ( -3.071710424422018668E-17, 6.404604876783312462E-16, 1.000000000000000000 ) ) ;
#25725=VERTEX_POINT ( 'NONE', #26082 ) ;
#25732=AXIS2_PLACEMENT_3D ( 'NONE', #24070, #19645, #8818 ) ;
#25752=CARTESIAN_POINT ( 'NONE',  ( -15.10382451463400955, -18.89477942154363888, 49.52966884056656482 ) ) ;
#25758=ADVANCED_FACE ( 'NONE', ( #48468 ), #40844, .T. ) ;
#25765=VERTEX_POINT ( 'NONE', #29284 ) ;
#25766=DIRECTION ( 'NONE',  ( -0.9687793358424822143, 0.2479245821708672415, 0.000000000000000000 ) ) ;
#25770=EDGE_LOOP ( 'NONE', ( #42614, #29682, #10708, #12745 ) ) ;
#25778=EDGE_CURVE ( 'NONE', #15450, #40523, #47909, .T. ) ;
#25787=VECTOR ( 'NONE', #15956, 1000.000000000000000 ) ;
#25794=CARTESIAN_POINT ( 'NONE',  ( -19.25408589567127038, -10.49476435801947893, 52.02966884056656482 ) ) ;
#25798=ORIENTED_EDGE ( 'NONE', *, *, #15998, .F. ) ;
#25804=VERTEX_POINT ( 'NONE', #48226 ) ;
#25805=CIRCLE ( 'NONE', #4585, 4.686499999999997890 ) ;
#25810=DIRECTION ( 'NONE',  ( -0.9687793358424819923, 0.2479245821708680464, 0.000000000000000000 ) ) ;
#25812=DIRECTION ( 'NONE',  ( -0.9180681052388980357, 0.3964226963016364014, 0.000000000000000000 ) ) ;
#25816=ORIENTED_EDGE ( 'NONE', *, *, #12416, .T. ) ;
#25825=EDGE_LOOP ( 'NONE', ( #41250, #31903, #632, #47447, #42875, #14633, #48177, #12300, #12079, #18394, #45706, #48446, #29912, #4533, #9393, #43162, #18414, #38486, #9117, #36914, #45143, #45140, #25998, #28508, #6722, #23582, #6891, #14881, #25099, #1202, #10232, #8363, #8672, #39753, #26695, #29961, #36084, #40776, #42923, #14857, #30942, #18768, #6553, #16173, #7761, #31741, #3151, #14652, #6422, #35446, #1593, #4859, #9922, #33066, #21107, #22670, #13595, #17890, #3513, #13855, #25995, #7996, #1973, #23951, #491, #31408, #48693, #11300, #36472, #13806, #13764, #28996, #20284, #12161, #20332, #36279, #31538, #35414, #41943, #20201, #19344, #21711, #39527, #16988, #8673, #10469, #41353, #32117, #21332, #4459, #26013, #13662, #2541, #40595, #13138, #16152, #38872, #31140, #30879, #16007, #45736, #9380, #22847, #14341, #36371, #4631, #17669, #28924, #14870, #48331, #24395, #36967, #30581, #9716, #7854, #33176, #9266, #29562, #24438, #21425, #14819, #28904, #18829, #16221, #27393, #47222, #32764, #2402, #23154, #42524, #18711, #23221, #30009, #8580, #31946, #1462, #36579, #35006, #10615, #42626, #40075, #25633, #15604, #41924, #47525, #3468, #25096, #33145, #242, #23119, #666, #12444, #690, #48361, #39038, #11311, #13549, #5138, #22523, #5043, #29381, #2954, #16132, #47266, #9407 ) ) ;
#25826=FACE_OUTER_BOUND ( 'NONE', #22814, .T. ) ;
#25844=AXIS2_PLACEMENT_3D ( 'NONE', #29835, #44861, #26139 ) ;
#25847=VERTEX_POINT ( 'NONE', #48722 ) ;
#25850=CARTESIAN_POINT ( 'NONE',  ( -21.09639645740537617, -17.74003392703708926, 52.02966884056656482 ) ) ;
#25851=CARTESIAN_POINT ( 'NONE',  ( -20.46316679850361808, -18.39244407412632043, 52.02966884056656482 ) ) ;
#25871=VECTOR ( 'NONE', #20536, 1000.000000000000000 ) ;
#25880=DIRECTION ( 'NONE',  ( -3.071710424422018668E-17, 6.404604876783312462E-16, 1.000000000000000000 ) ) ;
#25890=DIRECTION ( 'NONE',  ( -3.071710424422018668E-17, 6.404604876783312462E-16, 1.000000000000000000 ) ) ;
#25902=EDGE_CURVE ( 'NONE', #39406, #12959, #35324, .T. ) ;
#25907=EDGE_CURVE ( 'NONE', #24257, #28351, #26692, .T. ) ;
#25908=DIRECTION ( 'NONE',  ( 0.6380325334150255268, -0.7700094066334542964, 0.000000000000000000 ) ) ;
#25916=EDGE_CURVE ( 'NONE', #29955, #25765, #6237, .T. ) ;
#25920=AXIS2_PLACEMENT_3D ( 'NONE', #47043, #1750, #16742 ) ;
#25922=VERTEX_POINT ( 'NONE', #30274 ) ;
#25930=DIRECTION ( 'NONE',  ( -3.071710424422018668E-17, 6.404604876783312462E-16, 1.000000000000000000 ) ) ;
#25932=ORIENTED_EDGE ( 'NONE', *, *, #27908, .T. ) ;
#25943=CARTESIAN_POINT ( 'NONE',  ( -22.09908899289463591, -14.48102562737866705, 49.52966884056655772 ) ) ;
#25945=CIRCLE ( 'NONE', #14867, 5.249999999999998224 ) ;
#25950=CARTESIAN_POINT ( 'NONE',  ( -16.50530592306966682, -19.40475993746870387, 49.52966884056656482 ) ) ;
#25952=AXIS2_PLACEMENT_3D ( 'NONE', #8598, #23627, #9578 ) ;
#25957=DIRECTION ( 'NONE',  ( -3.071710424422018668E-17, 6.404604876783312462E-16, 1.000000000000000000 ) ) ;
#25972=ADVANCED_FACE ( 'NONE', ( #2146 ), #17149, .T. ) ;
#25979=CIRCLE ( 'NONE', #40112, 1.999999999999999556 ) ;
#25986=AXIS2_PLACEMENT_3D ( 'NONE', #1198, #12528, #23874 ) ;
#25995=ORIENTED_EDGE ( 'NONE', *, *, #11260, .F. ) ;
#25996=DIRECTION ( 'NONE',  ( 3.071710424422018668E-17, -6.404604876783312462E-16, -1.000000000000000000 ) ) ;
#25998=ORIENTED_EDGE ( 'NONE', *, *, #46016, .F. ) ;
#26000=DIRECTION ( 'NONE',  ( 0.9687793358424821033, -0.2479245821708677133, 0.000000000000000000 ) ) ;
#26013=ORIENTED_EDGE ( 'NONE', *, *, #4240, .F. ) ;
#26034=AXIS2_PLACEMENT_3D ( 'NONE', #44050, #29486, #18390 ) ;
#26038=DIRECTION ( 'NONE',  ( 0.9979768094191903138, 0.06357898915123821881, 0.000000000000000000 ) ) ;
#26043=AXIS2_PLACEMENT_3D ( 'NONE', #39270, #10212, #20572 ) ;
#26056=CIRCLE ( 'NONE', #16583, 4.686499999999999666 ) ;
#26057=CARTESIAN_POINT ( 'NONE',  ( -16.87780900865216438, -10.15465445929086030, 52.02966884056656482 ) ) ;
#26062=EDGE_CURVE ( 'NONE', #19139, #30521, #33717, .T. ) ;
#26066=CIRCLE ( 'NONE', #43371, 4.686499999999998778 ) ;
#26067=CARTESIAN_POINT ( 'NONE',  ( -22.46373187589079379, -16.28044704940516496, 49.52966884056655772 ) ) ;
#26069=ORIENTED_EDGE ( 'NONE', *, *, #9645, .T. ) ;
#26074=ORIENTED_EDGE ( 'NONE', *, *, #22792, .F. ) ;
#26082=CARTESIAN_POINT ( 'NONE',  ( -18.34288178775629419, -10.21365315202000446, 49.52966884056655772 ) ) ;
#26097=DIRECTION ( 'NONE',  ( -3.071710424422018668E-17, 6.404604876783312462E-16, 1.000000000000000000 ) ) ;
#26098=ORIENTED_EDGE ( 'NONE', *, *, #36754, .T. ) ;
#26105=EDGE_CURVE ( 'NONE', #41118, #14238, #41622, .T. ) ;
#26130=EDGE_CURVE ( 'NONE', #11361, #31233, #23532, .T. ) ;
#26134=DIRECTION ( 'NONE',  ( -3.071710424422018668E-17, 6.404604876783312462E-16, 1.000000000000000000 ) ) ;
#26139=DIRECTION ( 'NONE',  ( 0.9687793358424819923, -0.2479245821708680464, 0.000000000000000000 ) ) ;
#26151=DIRECTION ( 'NONE',  ( -3.071710424422018668E-17, 6.404604876783312462E-16, 1.000000000000000000 ) ) ;
#26163=ADVANCED_BREP_SHAPE_REPRESENTATION ( '', ( #14655, #29031 ), #29815 ) ;
#26164=DIRECTION ( 'NONE',  ( -3.071710424422018668E-17, 6.404604876783312462E-16, 1.000000000000000000 ) ) ;
#26172=CARTESIAN_POINT ( 'NONE',  ( -20.96187357126569850, -17.88286835634646721, 49.52966884056655772 ) ) ;
#26174=EDGE_CURVE ( 'NONE', #36726, #29955, #22830, .T. ) ;
#26216=DIRECTION ( 'NONE',  ( 3.071710424422018668E-17, -6.404604876783312462E-16, -1.000000000000000000 ) ) ;
#26237=LINE ( 'NONE', #7536, #30765 ) ;
#26239=AXIS2_PLACEMENT_3D ( 'NONE', #35503, #32310, #24445 ) ;
#26242=ADVANCED_FACE ( 'NONE', ( #32333 ), #9688, .T. ) ;
#26244=DIRECTION ( 'NONE',  ( -3.071710424422018668E-17, 6.404604876783312462E-16, 1.000000000000000000 ) ) ;
#26257=VERTEX_POINT ( 'NONE', #46628 ) ;
#26261=ADVANCED_FACE ( 'NONE', ( #47358 ), #40197, .T. ) ;
#26266=VERTEX_POINT ( 'NONE', #2037 ) ;
#26276=CARTESIAN_POINT ( 'NONE',  ( -17.26958401828953171, -19.65204229739824626, 52.02966884056656482 ) ) ;
#26282=AXIS2_PLACEMENT_3D ( 'NONE', #42003, #4104, #19103 ) ;
#26290=CARTESIAN_POINT ( 'NONE',  ( -19.94733193681641481, -19.41309290135173526, 50.77966884056656482 ) ) ;
#26304=ORIENTED_EDGE ( 'NONE', *, *, #22106, .F. ) ;
#26308=EDGE_LOOP ( 'NONE', ( #14934, #31283, #29430, #45184 ) ) ;
#26323=ORIENTED_EDGE ( 'NONE', *, *, #5799, .T. ) ;
#26333=FACE_OUTER_BOUND ( 'NONE', #13976, .T. ) ;
#26336=FACE_OUTER_BOUND ( 'NONE', #38288, .T. ) ;
#26343=AXIS2_PLACEMENT_3D ( 'NONE', #37816, #4111, #42253 ) ;
#26349=DIRECTION ( 'NONE',  ( -3.071710424422018668E-17, 6.404604876783312462E-16, 1.000000000000000000 ) ) ;
#26353=ADVANCED_FACE ( 'NONE', ( #18493 ), #29350, .T. ) ;
#26370=VERTEX_POINT ( 'NONE', #2995 ) ;
#26373=FACE_OUTER_BOUND ( 'NONE', #1121, .T. ) ;
#26382=CARTESIAN_POINT ( 'NONE',  ( -18.36828968083242231, -10.20659317963781021, 49.52966884056655772 ) ) ;
#26391=EDGE_CURVE ( 'NONE', #10333, #31013, #44771, .T. ) ;
#26396=CARTESIAN_POINT ( 'NONE',  ( -13.08575159502176177, -11.85263988192353324, 49.52966884056655772 ) ) ;
#26417=CARTESIAN_POINT ( 'NONE',  ( -21.13745558015973103, -11.09794736473739718, 52.02966884056656482 ) ) ;
#26425=DIRECTION ( 'NONE',  ( -3.071710424422018668E-17, 6.404604876783312462E-16, 1.000000000000000000 ) ) ;
#26427=ORIENTED_EDGE ( 'NONE', *, *, #8810, .F. ) ;
#26435=DIRECTION ( 'NONE',  ( -3.071710424422018668E-17, 6.404604876783312462E-16, 1.000000000000000000 ) ) ;
#26452=AXIS2_PLACEMENT_3D ( 'NONE', #47715, #13955, #33397 ) ;
#26454=ORIENTED_EDGE ( 'NONE', *, *, #32523, .T. ) ;
#26463=VERTEX_POINT ( 'NONE', #21403 ) ;
#26473=CARTESIAN_POINT ( 'NONE',  ( -13.07710726710083193, -16.59225537930583982, 49.52966884056655772 ) ) ;
#26476=CIRCLE ( 'NONE', #41417, 1.999999999999999556 ) ;
#26480=CYLINDRICAL_SURFACE ( 'NONE', #13962, 5.249999999999998224 ) ;
#26486=AXIS2_PLACEMENT_3D ( 'NONE', #19325, #25996, #29683 ) ;
#26510=ORIENTED_EDGE ( 'NONE', *, *, #41370, .F. ) ;
#26523=ORIENTED_EDGE ( 'NONE', *, *, #3472, .T. ) ;
#26544=EDGE_CURVE ( 'NONE', #31360, #38039, #13016, .T. ) ;
#26552=FACE_OUTER_BOUND ( 'NONE', #25642, .T. ) ;
#26559=CIRCLE ( 'NONE', #10836, 4.686499999999999666 ) ;
#26583=ADVANCED_FACE ( 'NONE', ( #9106 ), #4933, .T. ) ;
#26593=CARTESIAN_POINT ( 'NONE',  ( -17.42558057905623059, -9.559206755253619292, 50.77966884056655772 ) ) ;
#26596=VECTOR ( 'NONE', #29095, 1000.000000000000000 ) ;
#26601=ADVANCED_FACE ( 'NONE', ( #28043 ), #45813, .T. ) ;
#26603=EDGE_CURVE ( 'NONE', #39108, #24138, #29858, .T. ) ;
#26608=ORIENTED_EDGE ( 'NONE', *, *, #33042, .F. ) ;
#26619=CIRCLE ( 'NONE', #24273, 4.686499999999999666 ) ;
#26652=EDGE_LOOP ( 'NONE', ( #33595, #23898, #11200, #4201 ) ) ;
#26672=ORIENTED_EDGE ( 'NONE', *, *, #16951, .T. ) ;
#26678=ORIENTED_EDGE ( 'NONE', *, *, #11670, .F. ) ;
#26687=CARTESIAN_POINT ( 'NONE',  ( -16.34301583228449317, -10.23680828416977739, 49.52966884056655772 ) ) ;
#26692=CIRCLE ( 'NONE', #15669, 5.249999999999998224 ) ;
#26695=ORIENTED_EDGE ( 'NONE', *, *, #28225, .F. ) ;
#26700=DIRECTION ( 'NONE',  ( -3.071710424422018668E-17, 6.404604876783312462E-16, 1.000000000000000000 ) ) ;
#26706=DIRECTION ( 'NONE',  ( -3.071710424422018668E-17, 6.404604876783312462E-16, 1.000000000000000000 ) ) ;
#26717=LINE ( 'NONE', #33842, #48086 ) ;
#26726=FACE_OUTER_BOUND ( 'NONE', #14591, .T. ) ;
#26729=CIRCLE ( 'NONE', #3131, 5.249999999999998224 ) ;
#26730=EDGE_LOOP ( 'NONE', ( #23058, #11995, #1471, #45 ) ) ;
#26739=CARTESIAN_POINT ( 'NONE',  ( -12.38445583493520630, -13.33796604008351494, 49.52966884056655772 ) ) ;
#26751=VECTOR ( 'NONE', #6028, 1000.000000000000000 ) ;
#26763=ORIENTED_EDGE ( 'NONE', *, *, #33848, .F. ) ;
#26770=CARTESIAN_POINT ( 'NONE',  ( -18.55662820153069248, -10.26160847489872197, 52.02966884056656482 ) ) ;
#26781=VERTEX_POINT ( 'NONE', #9600 ) ;
#26790=DIRECTION ( 'NONE',  ( 0.9687793358424821033, -0.2479245821708677133, 0.000000000000000000 ) ) ;
#26798=EDGE_CURVE ( 'NONE', #47056, #48460, #34576, .T. ) ;
#26801=DIRECTION ( 'NONE',  ( 3.071710424422018668E-17, -6.404604876783312462E-16, -1.000000000000000000 ) ) ;
#26802=AXIS2_PLACEMENT_3D ( 'NONE', #7288, #33849, #40752 ) ;
#26804=FACE_OUTER_BOUND ( 'NONE', #43901, .T. ) ;
#26819=ORIENTED_EDGE ( 'NONE', *, *, #34675, .T. ) ;
#26822=CIRCLE ( 'NONE', #40939, 2.000000000000000000 ) ;
#26829=LINE ( 'NONE', #30530, #4686 ) ;
#26835=( NAMED_UNIT ( * ) PLANE_ANGLE_UNIT ( ) SI_UNIT ( $, .RADIAN. ) );
#26866=CARTESIAN_POINT ( 'NONE',  ( -13.10965166868813903, -12.97921450448603409, 49.52966884056655772 ) ) ;
#26868=DIRECTION ( 'NONE',  ( -3.071710424422018668E-17, 6.404604876783312462E-16, 1.000000000000000000 ) ) ;
#26875=CARTESIAN_POINT ( 'NONE',  ( -14.98297878932515381, -10.79466886532025605, 52.02966884056656482 ) ) ;
#26880=DIRECTION ( 'NONE',  ( 0.9687793358424819923, -0.2479245821708676023, 0.000000000000000000 ) ) ;
#26886=ORIENTED_EDGE ( 'NONE', *, *, #33095, .F. ) ;
#26887=CIRCLE ( 'NONE', #11945, 5.249999999999998224 ) ;
#26893=CARTESIAN_POINT ( 'NONE',  ( -22.10120296142702045, -17.19398125327358073, 52.02966884056656482 ) ) ;
#26894=EDGE_CURVE ( 'NONE', #47558, #16040, #25945, .T. ) ;
#26895=DIRECTION ( 'NONE',  ( 0.7700094066334515208, 0.6380325334150288574, 0.000000000000000000 ) ) ;
#26906=ORIENTED_EDGE ( 'NONE', *, *, #8371, .T. ) ;
#26916=CARTESIAN_POINT ( 'NONE',  ( -19.20714268997449281, -19.15619313305651161, 49.52966884056656482 ) ) ;
#26923=ORIENTED_EDGE ( 'NONE', *, *, #36523, .F. ) ;
#26933=CYLINDRICAL_SURFACE ( 'NONE', #33844, 1.999999999999999112 ) ;
#26938=ORIENTED_EDGE ( 'NONE', *, *, #23450, .F. ) ;
#26960=DIRECTION ( 'NONE',  ( 0.9687793358424821033, -0.2479245821708679909, 0.000000000000000000 ) ) ;
#26961=EDGE_CURVE ( 'NONE', #30371, #22574, #41661, .T. ) ;
#26969=DIRECTION ( 'NONE',  ( -3.071710424422018668E-17, 6.404604876783312462E-16, 1.000000000000000000 ) ) ;
#26973=CARTESIAN_POINT ( 'NONE',  ( -13.08575159502176177, -11.85263988192353324, 52.02966884056656482 ) ) ;
#26980=DIRECTION ( 'NONE',  ( -0.9757441136919988711, -0.2189141945955436208, 0.000000000000000000 ) ) ;
#26989=VERTEX_POINT ( 'NONE', #32119 ) ;
#27018=ORIENTED_EDGE ( 'NONE', *, *, #48131, .T. ) ;
#27025=CARTESIAN_POINT ( 'NONE',  ( -13.40955617598886995, -17.25032161083215598, 52.02966884056656482 ) ) ;
#27027=DIRECTION ( 'NONE',  ( -3.071710424422018668E-17, 6.404604876783312462E-16, 1.000000000000000000 ) ) ;
#27028=ORIENTED_EDGE ( 'NONE', *, *, #6855, .T. ) ;
#27034=ORIENTED_EDGE ( 'NONE', *, *, #28165, .T. ) ;
#27052=AXIS2_PLACEMENT_3D ( 'NONE', #42249, #23542, #46430 ) ;
#27061=DIRECTION ( 'NONE',  ( -3.071710424422018668E-17, 6.404604876783312462E-16, 1.000000000000000000 ) ) ;
#27070=ORIENTED_EDGE ( 'NONE', *, *, #8617, .T. ) ;
#27073=DIRECTION ( 'NONE',  ( 0.9687793358424819923, -0.2479245821708680464, 0.000000000000000000 ) ) ;
#27077=EDGE_CURVE ( 'NONE', #12698, #45155, #47858, .T. ) ;
#27086=CYLINDRICAL_SURFACE ( 'NONE', #30485, 5.249999999999998224 ) ;
#27093=CARTESIAN_POINT ( 'NONE',  ( -17.42409385541299471, -14.80920654474435771, 49.52966884056655772 ) ) ;
#27117=AXIS2_PLACEMENT_3D ( 'NONE', #39356, #16196, #42330 ) ;
#27123=DIRECTION ( 'NONE',  ( 0.2479245821708712938, 0.9687793358424811041, 0.000000000000000000 ) ) ;
#27132=ADVANCED_FACE ( 'NONE', ( #17797 ), #2564, .T. ) ;
#27133=ORIENTED_EDGE ( 'NONE', *, *, #31847, .F. ) ;
#27134=CYLINDRICAL_SURFACE ( 'NONE', #5994, 4.686499999999997002 ) ;
#27141=DIRECTION ( 'NONE',  ( -0.9757441136919988711, -0.2189141945955433433, 0.000000000000000000 ) ) ;
#27145=CYLINDRICAL_SURFACE ( 'NONE', #13448, 4.686499999999997002 ) ;
#27154=VERTEX_POINT ( 'NONE', #18040 ) ;
#27161=DIRECTION ( 'NONE',  ( 0.9687793358424821033, -0.2479245821708677133, 0.000000000000000000 ) ) ;
#27174=EDGE_LOOP ( 'NONE', ( #30187, #27255, #16503, #39964 ) ) ;
#27211=ORIENTED_EDGE ( 'NONE', *, *, #26798, .T. ) ;
#27214=ADVANCED_FACE ( 'NONE', ( #38211 ), #34038, .T. ) ;
#27219=EDGE_LOOP ( 'NONE', ( #2278, #11026, #12194, #34121 ) ) ;
#27222=LINE ( 'NONE', #45461, #30167 ) ;
#27223=CIRCLE ( 'NONE', #5992, 1.999999999999999556 ) ;
#27248=VERTEX_POINT ( 'NONE', #37732 ) ;
#27249=ORIENTED_EDGE ( 'NONE', *, *, #35579, .T. ) ;
#27255=ORIENTED_EDGE ( 'NONE', *, *, #34201, .T. ) ;
#27262=CIRCLE ( 'NONE', #39061, 2.000000000000001332 ) ;
#27264=CARTESIAN_POINT ( 'NONE',  ( -17.42409385541299471, -14.80920654474435771, 49.52966884056655772 ) ) ;
#27273=VERTEX_POINT ( 'NONE', #33792 ) ;
#27289=ORIENTED_EDGE ( 'NONE', *, *, #3753, .T. ) ;
#27303=DIRECTION ( 'NONE',  ( -3.071710424422018668E-17, 6.404604876783312462E-16, 1.000000000000000000 ) ) ;
#27305=CARTESIAN_POINT ( 'NONE',  ( -12.89447938415233175, -16.05746464591689104, 49.52966884056655772 ) ) ;
#27325=AXIS2_PLACEMENT_3D ( 'NONE', #12028, #5127, #8337 ) ;
#27353=AXIS2_PLACEMENT_3D ( 'NONE', #3967, #41632, #31038 ) ;
#27360=VECTOR ( 'NONE', #5899, 1000.000000000000000 ) ;
#27362=AXIS2_PLACEMENT_3D ( 'NONE', #13442, #21583, #17388 ) ;
#27375=FACE_OUTER_BOUND ( 'NONE', #18916, .T. ) ;
#27393=ORIENTED_EDGE ( 'NONE', *, *, #22295, .F. ) ;
#27395=EDGE_CURVE ( 'NONE', #25922, #16677, #10967, .T. ) ;
#27404=DIRECTION ( 'NONE',  ( -3.071710424422018668E-17, 6.404604876783312462E-16, 1.000000000000000000 ) ) ;
#27427=DIRECTION ( 'NONE',  ( 0.9687793358424821033, -0.2479245821708679909, 0.000000000000000000 ) ) ;
#27447=ORIENTED_EDGE ( 'NONE', *, *, #17702, .T. ) ;
#27456=LINE ( 'NONE', #8504, #11917 ) ;
#27468=CARTESIAN_POINT ( 'NONE',  ( -12.91230480768039790, -16.07689808402359688, 49.52966884056655772 ) ) ;
#27472=ORIENTED_EDGE ( 'NONE', *, *, #35721, .F. ) ;
#27476=DIRECTION ( 'NONE',  ( -3.071710424422018668E-17, 6.404604876783312462E-16, 1.000000000000000000 ) ) ;
#27483=CARTESIAN_POINT ( 'NONE',  ( -17.42409385541299471, -14.80920654474435771, 49.52966884056655772 ) ) ;
#27489=ORIENTED_EDGE ( 'NONE', *, *, #37472, .F. ) ;
#27513=CARTESIAN_POINT ( 'NONE',  ( -20.86860741727135959, -11.63137574808859931, 49.52966884056655772 ) ) ;
#27521=DIRECTION ( 'NONE',  ( -3.071710424422018668E-17, 6.404604876783312462E-16, 1.000000000000000000 ) ) ;
#27524=VECTOR ( 'NONE', #26801, 1000.000000000000000 ) ;
#27525=LINE ( 'NONE', #38847, #11730 ) ;
#27542=CIRCLE ( 'NONE', #3932, 2.000000000000000888 ) ;
#27549=ORIENTED_EDGE ( 'NONE', *, *, #25377, .T. ) ;
#27573=CARTESIAN_POINT ( 'NONE',  ( -12.23849770038826712, -15.62901903366650380, 49.52966884056655772 ) ) ;
#27574=CARTESIAN_POINT ( 'NONE',  ( -16.17583575424048092, -10.27959207348368587, 52.02966884056656482 ) ) ;
#27584=CARTESIAN_POINT ( 'NONE',  ( -12.88390949798720619, -15.97110509908812936, 49.52966884056655772 ) ) ;
#27592=AXIS2_PLACEMENT_3D ( 'NONE', #3942, #45078, #30296 ) ;
#27599=VERTEX_POINT ( 'NONE', #15008 ) ;
#27612=FACE_OUTER_BOUND ( 'NONE', #39176, .T. ) ;
#27615=ORIENTED_EDGE ( 'NONE', *, *, #46462, .T. ) ;
#27626=CARTESIAN_POINT ( 'NONE',  ( -22.09908899289463591, -14.48102562737866705, 49.52966884056655772 ) ) ;
#27643=DIRECTION ( 'NONE',  ( -3.071710424422018668E-17, 6.404604876783312462E-16, 1.000000000000000000 ) ) ;
#27670=EDGE_CURVE ( 'NONE', #8529, #16401, #993, .T. ) ;
#27673=AXIS2_PLACEMENT_3D ( 'NONE', #15233, #7149, #6653 ) ;
#27681=DIRECTION ( 'NONE',  ( -0.8447509909909771686, 0.5351595679979589404, 0.000000000000000000 ) ) ;
#27688=ORIENTED_EDGE ( 'NONE', *, *, #18660, .F. ) ;
#27705=DIRECTION ( 'NONE',  ( -3.071710424422018668E-17, 6.404604876783312462E-16, 1.000000000000000000 ) ) ;
#27706=LINE ( 'NONE', #42737, #42773 ) ;
#27726=CYLINDRICAL_SURFACE ( 'NONE', #11016, 1.999999999999999556 ) ;
#27730=ORIENTED_EDGE ( 'NONE', *, *, #3199, .T. ) ;
#27734=DIRECTION ( 'NONE',  ( -3.071710424422018668E-17, 6.404604876783312462E-16, 1.000000000000000000 ) ) ;
#27743=ADVANCED_FACE ( 'NONE', ( #42613 ), #32707, .T. ) ;
#27751=EDGE_LOOP ( 'NONE', ( #20605, #29767, #2122, #6146 ) ) ;
#27763=EDGE_CURVE ( 'NONE', #13430, #6817, #29891, .T. ) ;
#27795=EDGE_LOOP ( 'NONE', ( #37547, #30301, #48600, #1817 ) ) ;
#27804=DIRECTION ( 'NONE',  ( -3.071710424422018668E-17, 6.404604876783312462E-16, 1.000000000000000000 ) ) ;
#27817=EDGE_CURVE ( 'NONE', #13690, #13051, #25979, .T. ) ;
#27821=AXIS2_PLACEMENT_3D ( 'NONE', #36231, #9676, #47091 ) ;
#27829=CARTESIAN_POINT ( 'NONE',  ( -12.73044152958719977, -14.59664269629646682, 49.52966884056655772 ) ) ;
#27833=ORIENTED_EDGE ( 'NONE', *, *, #8114, .F. ) ;
#27848=CARTESIAN_POINT ( 'NONE',  ( -12.17647495751581133, -14.96730746957505254, 49.52966884056655772 ) ) ;
#27854=CIRCLE ( 'NONE', #25489, 4.686499999999998778 ) ;
#27857=CIRCLE ( 'NONE', #35713, 4.686499999999997002 ) ;
#27859=CARTESIAN_POINT ( 'NONE',  ( -17.42409385541299471, -14.80920654474435594, 52.02966884056656482 ) ) ;
#27870=CARTESIAN_POINT ( 'NONE',  ( -22.11774618123879677, -15.02177039319221130, 52.02966884056656482 ) ) ;
#27872=FACE_OUTER_BOUND ( 'NONE', #22226, .T. ) ;
#27888=CIRCLE ( 'NONE', #27117, 1.999999999999999556 ) ;
#27894=VERTEX_POINT ( 'NONE', #37363 ) ;
#27908=EDGE_CURVE ( 'NONE', #15441, #1628, #9473, .T. ) ;
#27915=ORIENTED_EDGE ( 'NONE', *, *, #8810, .T. ) ;
#27926=EDGE_CURVE ( 'NONE', #28111, #17101, #14689, .T. ) ;
#27929=DIRECTION ( 'NONE',  ( -3.071710424422018668E-17, 6.404604876783312462E-16, 1.000000000000000000 ) ) ;
#27938=FACE_OUTER_BOUND ( 'NONE', #5118, .T. ) ;
#27953=FACE_OUTER_BOUND ( 'NONE', #42267, .T. ) ;
#27956=VECTOR ( 'NONE', #4069, 1000.000000000000000 ) ;
#27961=CARTESIAN_POINT ( 'NONE',  ( -17.42409385541299471, -14.80920654474435771, 49.52966884056655772 ) ) ;
#27964=DIRECTION ( 'NONE',  ( 0.9687793358424819923, -0.2479245821708680464, 0.000000000000000000 ) ) ;
#27972=CARTESIAN_POINT ( 'NONE',  ( -17.42409385541299471, -14.80920654474435771, 49.52966884056655772 ) ) ;
#28003=CARTESIAN_POINT ( 'NONE',  ( -21.51080377022508472, -17.10312989180209087, 49.52966884056655772 ) ) ;
#28026=AXIS2_PLACEMENT_3D ( 'NONE', #28353, #43616, #2233 ) ;
#28028=ORIENTED_EDGE ( 'NONE', *, *, #22871, .F. ) ;
#28034=CYLINDRICAL_SURFACE ( 'NONE', #37814, 1.999999999999999556 ) ;
#28035=ORIENTED_EDGE ( 'NONE', *, *, #18402, .T. ) ;
#28036=DIRECTION ( 'NONE',  ( 0.9687793358424821033, -0.2479245821708677133, 0.000000000000000000 ) ) ;
#28043=FACE_OUTER_BOUND ( 'NONE', #6865, .T. ) ;
#28053=ORIENTED_EDGE ( 'NONE', *, *, #22106, .T. ) ;
#28063=DIRECTION ( 'NONE',  ( -3.071710424422018668E-17, 6.404604876783312462E-16, 1.000000000000000000 ) ) ;
#28065=DIRECTION ( 'NONE',  ( -3.071710424422018668E-17, 6.404604876783312462E-16, 1.000000000000000000 ) ) ;
#28068=CARTESIAN_POINT ( 'NONE',  ( -12.82020749880560651, -17.33244462614775827, 52.02966884056656482 ) ) ;
#28076=DIRECTION ( 'NONE',  ( 0.9687793358424822143, -0.2479245821708672415, 0.000000000000000000 ) ) ;
#28090=EDGE_CURVE ( 'NONE', #33207, #36361, #33014, .T. ) ;
#28092=AXIS2_PLACEMENT_3D ( 'NONE', #27961, #20592, #1130 ) ;
#28097=ADVANCED_FACE ( 'NONE', ( #16897 ), #35854, .T. ) ;
#28111=VERTEX_POINT ( 'NONE', #47204 ) ;
#28126=DIRECTION ( 'NONE',  ( -0.9687793358424822143, 0.2479245821708672415, 0.000000000000000000 ) ) ;
#28128=ORIENTED_EDGE ( 'NONE', *, *, #15869, .F. ) ;
#28130=CIRCLE ( 'NONE', #40740, 2.000000000000000444 ) ;
#28131=VECTOR ( 'NONE', #21416, 1000.000000000000000 ) ;
#28138=EDGE_CURVE ( 'NONE', #38954, #17561, #34617, .T. ) ;
#28141=ORIENTED_EDGE ( 'NONE', *, *, #34037, .F. ) ;
#28161=VERTEX_POINT ( 'NONE', #5842 ) ;
#28165=EDGE_CURVE ( 'NONE', #7346, #70, #13414, .T. ) ;
#28189=DIRECTION ( 'NONE',  ( 0.9687793358424819923, -0.2479245821708678243, 0.000000000000000000 ) ) ;
#28192=VERTEX_POINT ( 'NONE', #36813 ) ;
#28208=AXIS2_PLACEMENT_3D ( 'NONE', #24523, #16850, #36049 ) ;
#28210=ORIENTED_EDGE ( 'NONE', *, *, #40941, .T. ) ;
#28213=AXIS2_PLACEMENT_3D ( 'NONE', #32654, #25509, #43755 ) ;
#28217=ORIENTED_EDGE ( 'NONE', *, *, #19658, .T. ) ;
#28225=EDGE_CURVE ( 'NONE', #43774, #11839, #25209, .T. ) ;
#28237=CIRCLE ( 'NONE', #25111, 1.999999999999999112 ) ;
#28248=EDGE_LOOP ( 'NONE', ( #24359, #30117, #10951, #23610 ) ) ;
#28257=CARTESIAN_POINT ( 'NONE',  ( -17.42409385541299471, -14.80920654474435771, 49.52966884056655772 ) ) ;
#28277=AXIS2_PLACEMENT_3D ( 'NONE', #24880, #5451, #5697 ) ;
#28285=CARTESIAN_POINT ( 'NONE',  ( -12.17409406592225629, -14.80771982110106855, 49.52966884056655772 ) ) ;
#28294=EDGE_CURVE ( 'NONE', #13051, #15441, #40772, .T. ) ;
#28323=VECTOR ( 'NONE', #25191, 1000.000000000000000 ) ;
#28329=DIRECTION ( 'NONE',  ( -3.071710424422018668E-17, 6.404604876783312462E-16, 1.000000000000000000 ) ) ;
#28340=DIRECTION ( 'NONE',  ( -3.071710424422018668E-17, 6.404604876783312462E-16, 1.000000000000000000 ) ) ;
#28342=ORIENTED_EDGE ( 'NONE', *, *, #26105, .T. ) ;
#28347=DIRECTION ( 'NONE',  ( 0.2479245821708711550, 0.9687793358424812151, 0.000000000000000000 ) ) ;
#28351=VERTEX_POINT ( 'NONE', #12199 ) ;
#28353=CARTESIAN_POINT ( 'NONE',  ( -17.42409385541299471, -14.80920654474435771, 49.52966884056655772 ) ) ;
#28359=DIRECTION ( 'NONE',  ( -0.2479245821708774278, -0.9687793358424795498, 0.000000000000000000 ) ) ;
#28360=EDGE_CURVE ( 'NONE', #23803, #12455, #34842, .T. ) ;
#28361=LINE ( 'NONE', #17253, #22538 ) ;
#28367=DIRECTION ( 'NONE',  ( 0.9979768094191903138, 0.06357898915123821881, 0.000000000000000000 ) ) ;
#28370=ORIENTED_EDGE ( 'NONE', *, *, #28090, .T. ) ;
#28375=CYLINDRICAL_SURFACE ( 'NONE', #41968, 1.999999999999999112 ) ;
#28380=CARTESIAN_POINT ( 'NONE',  ( -14.83720200468841810, -10.88702015217558206, 52.02966884056656482 ) ) ;
#28383=VERTEX_POINT ( 'NONE', #9002 ) ;
#28388=DIRECTION ( 'NONE',  ( 0.9687793358424821033, -0.2479245821708677133, 0.000000000000000000 ) ) ;
#28404=LINE ( 'NONE', #10418, #28323 ) ;
#28407=DIRECTION ( 'NONE',  ( 0.9687793358424821033, -0.2479245821708679909, 0.000000000000000000 ) ) ;
#28419=EDGE_CURVE ( 'NONE', #12756, #25645, #47250, .T. ) ;
#28436=AXIS2_PLACEMENT_3D ( 'NONE', #4625, #20376, #46721 ) ;
#28437=LINE ( 'NONE', #28672, #9272 ) ;
#28448=AXIS2_PLACEMENT_3D ( 'NONE', #9996, #46938, #32170 ) ;
#28454=CARTESIAN_POINT ( 'NONE',  ( -17.81160558974998764, -14.71003671187600936, 49.52966884056655772 ) ) ;
#28459=EDGE_LOOP ( 'NONE', ( #35606, #4383, #14077, #9866 ) ) ;
#28471=ORIENTED_EDGE ( 'NONE', *, *, #18905, .T. ) ;
#28481=EDGE_CURVE ( 'NONE', #31312, #29256, #40150, .T. ) ;
#28483=ORIENTED_EDGE ( 'NONE', *, *, #24891, .T. ) ;
#28491=DIRECTION ( 'NONE',  ( -3.071710424422018668E-17, 6.404604876783312462E-16, 1.000000000000000000 ) ) ;
#28507=DIRECTION ( 'NONE',  ( 0.9687793358424821033, -0.2479245821708679909, 0.000000000000000000 ) ) ;
#28508=ORIENTED_EDGE ( 'NONE', *, *, #16294, .F. ) ;
#28517=DIRECTION ( 'NONE',  ( -3.071710424422018668E-17, 6.404604876783312462E-16, 1.000000000000000000 ) ) ;
#28530=EDGE_CURVE ( 'NONE', #26257, #20160, #18232, .T. ) ;
#28547=EDGE_CURVE ( 'NONE', #16476, #29955, #32314, .T. ) ;
#28568=CIRCLE ( 'NONE', #11279, 4.686499999999998778 ) ;
#28572=DIRECTION ( 'NONE',  ( 0.9979768094191903138, 0.06357898915123796901, 0.000000000000000000 ) ) ;
#28582=ORIENTED_EDGE ( 'NONE', *, *, #33737, .T. ) ;
#28586=CYLINDRICAL_SURFACE ( 'NONE', #48117, 4.686499999999997002 ) ;
#28596=DIRECTION ( 'NONE',  ( -3.071710424422018668E-17, 6.404604876783312462E-16, 1.000000000000000000 ) ) ;
#28617=DIRECTION ( 'NONE',  ( -3.071710424422018668E-17, 6.404604876783312462E-16, 1.000000000000000000 ) ) ;
#28625=EDGE_CURVE ( 'NONE', #16073, #7976, #20505, .T. ) ;
#28628=ORIENTED_EDGE ( 'NONE', *, *, #26894, .T. ) ;
#28631=CARTESIAN_POINT ( 'NONE',  ( -20.98629261354270170, -17.87291272402722697, 49.52966884056655772 ) ) ;
#28642=AXIS2_PLACEMENT_3D ( 'NONE', #6753, #14828, #3533 ) ;
#28667=CARTESIAN_POINT ( 'NONE',  ( -14.38502091232239621, -11.22596901536237013, 49.52966884056655772 ) ) ;
#28672=CARTESIAN_POINT ( 'NONE',  ( -22.41668094288463919, -16.43295965837073780, 50.77966884056655772 ) ) ;
#28673=DIRECTION ( 'NONE',  ( -3.071710424422018668E-17, 6.404604876783312462E-16, 1.000000000000000000 ) ) ;
#28675=ORIENTED_EDGE ( 'NONE', *, *, #17632, .F. ) ;
#28700=AXIS2_PLACEMENT_3D ( 'NONE', #38832, #27027, #12734 ) ;
#28708=EDGE_CURVE ( 'NONE', #6216, #42831, #31275, .T. ) ;
#28715=CARTESIAN_POINT ( 'NONE',  ( -12.67665486305926237, -12.56770637434968307, 50.77966884056655772 ) ) ;
#28720=FACE_OUTER_BOUND ( 'NONE', #15692, .T. ) ;
#28721=ORIENTED_EDGE ( 'NONE', *, *, #47908, .F. ) ;
#28734=DIRECTION ( 'NONE',  ( -3.071710424422018668E-17, 6.404604876783312462E-16, 1.000000000000000000 ) ) ;
#28737=AXIS2_PLACEMENT_3D ( 'NONE', #31412, #17351, #17099 ) ;
#28747=ORIENTED_EDGE ( 'NONE', *, *, #7460, .F. ) ;
#28760=VERTEX_POINT ( 'NONE', #36885 ) ;
#28765=CYLINDRICAL_SURFACE ( 'NONE', #80, 5.249999999999998224 ) ;
#28780=FACE_OUTER_BOUND ( 'NONE', #38735, .T. ) ;
#28789=EDGE_CURVE ( 'NONE', #44272, #19285, #38588, .T. ) ;
#28792=CARTESIAN_POINT ( 'NONE',  ( -14.21171452256333012, -10.65672306833167937, 50.77966884056655772 ) ) ;
#28798=DIRECTION ( 'NONE',  ( -3.071710424422018668E-17, 6.404604876783312462E-16, 1.000000000000000000 ) ) ;
#28817=LINE ( 'NONE', #40152, #34764 ) ;
#28841=EDGE_LOOP ( 'NONE', ( #40527, #6751, #33492, #38674 ) ) ;
#28849=ORIENTED_EDGE ( 'NONE', *, *, #32974, .T. ) ;
#28852=DIRECTION ( 'NONE',  ( -3.071710424422018668E-17, 6.404604876783312462E-16, 1.000000000000000000 ) ) ;
#28853=DIRECTION ( 'NONE',  ( -3.071710424422018668E-17, 6.404604876783312462E-16, 1.000000000000000000 ) ) ;
#28872=CARTESIAN_POINT ( 'NONE',  ( -21.97169192525862869, -15.94174089086207147, 49.52966884056655772 ) ) ;
#28878=CARTESIAN_POINT ( 'NONE',  ( -21.01334446694451685, -11.79580940901521835, 49.52966884056655772 ) ) ;
#28884=VERTEX_POINT ( 'NONE', #40585 ) ;
#28899=VERTEX_POINT ( 'NONE', #47516 ) ;
#28900=EDGE_CURVE ( 'NONE', #3266, #24111, #13749, .T. ) ;
#28904=ORIENTED_EDGE ( 'NONE', *, *, #36858, .F. ) ;
#28907=CIRCLE ( 'NONE', #36749, 4.686499999999998778 ) ;
#28922=LINE ( 'NONE', #43231, #43936 ) ;
#28924=ORIENTED_EDGE ( 'NONE', *, *, #1912, .F. ) ;
#28933=CARTESIAN_POINT ( 'NONE',  ( -13.71283467540607504, -11.09584481999758232, 50.77966884056655772 ) ) ;
#28945=CIRCLE ( 'NONE', #20192, 4.686499999999999666 ) ;
#28952=EDGE_CURVE ( 'NONE', #42513, #22563, #708, .T. ) ;
#28957=AXIS2_PLACEMENT_3D ( 'NONE', #38046, #27705, #12200 ) ;
#28966=ORIENTED_EDGE ( 'NONE', *, *, #14348, .F. ) ;
#28970=DIRECTION ( 'NONE',  ( -3.071710424422018668E-17, 6.404604876783312462E-16, 1.000000000000000000 ) ) ;
#28981=CARTESIAN_POINT ( 'NONE',  ( -17.42409385541299471, -14.80920654474435771, 49.52966884056655772 ) ) ;
#28996=ORIENTED_EDGE ( 'NONE', *, *, #13844, .F. ) ;
#29003=CARTESIAN_POINT ( 'NONE',  ( -12.74138925215518015, -14.62063335304397427, 49.52966884056655772 ) ) ;
#29007=AXIS2_PLACEMENT_3D ( 'NONE', #5440, #13038, #9624 ) ;
#29009=CARTESIAN_POINT ( 'NONE',  ( -21.13535303541994281, -18.52256826949110291, 52.02966884056656482 ) ) ;
#29011=CARTESIAN_POINT ( 'NONE',  ( -17.42409385541299471, -14.80920654474435594, 52.02966884056656482 ) ) ;
#29031=AXIS2_PLACEMENT_3D ( 'NONE', #29301, #44568, #33698 ) ;
#29035=CARTESIAN_POINT ( 'NONE',  ( -19.23707162763026801, -10.47461692831664060, 49.52966884056655772 ) ) ;
#29058=DIRECTION ( 'NONE',  ( 0.2189141945955467017, -0.9757441136919982050, 0.000000000000000000 ) ) ;
#29070=VECTOR ( 'NONE', #39105, 1000.000000000000000 ) ;
#29084=VERTEX_POINT ( 'NONE', #46500 ) ;
#29094=CARTESIAN_POINT ( 'NONE',  ( -16.17583575424048092, -10.27959207348368764, 49.52966884056655772 ) ) ;
#29095=DIRECTION ( 'NONE',  ( -3.071710424422018668E-17, 6.404604876783312462E-16, 1.000000000000000000 ) ) ;
#29097=ADVANCED_FACE ( 'NONE', ( #31464 ), #947, .T. ) ;
#29107=AXIS2_PLACEMENT_3D ( 'NONE', #43883, #35500, #20736 ) ;
#29112=CIRCLE ( 'NONE', #2400, 5.249999999999998224 ) ;
#29128=EDGE_LOOP ( 'NONE', ( #47223, #416, #29864, #29764 ) ) ;
#29144=CIRCLE ( 'NONE', #821, 1.999999999999999778 ) ;
#29156=VERTEX_POINT ( 'NONE', #6083 ) ;
#29158=CARTESIAN_POINT ( 'NONE',  ( -17.42409385541299471, -14.80920654474434883, 62.02966884056656482 ) ) ;
#29163=EDGE_CURVE ( 'NONE', #32600, #17349, #26056, .T. ) ;
#29172=CARTESIAN_POINT ( 'NONE',  ( -17.42409385541299471, -14.80920654474435594, 52.02966884056656482 ) ) ;
#29174=VERTEX_POINT ( 'NONE', #47461 ) ;
#29177=EDGE_CURVE ( 'NONE', #33352, #21704, #45725, .T. ) ;
#29189=LINE ( 'NONE', #14371, #46501 ) ;
#29194=ORIENTED_EDGE ( 'NONE', *, *, #34713, .F. ) ;
#29199=VERTEX_POINT ( 'NONE', #13696 ) ;
#29207=AXIS2_PLACEMENT_3D ( 'NONE', #41346, #26097, #32741 ) ;
#29224=ORIENTED_EDGE ( 'NONE', *, *, #25902, .F. ) ;
#29225=DIRECTION ( 'NONE',  ( -3.071710424422018668E-17, 6.404604876783312462E-16, 1.000000000000000000 ) ) ;
#29235=EDGE_CURVE ( 'NONE', #14018, #26370, #22120, .T. ) ;
#29252=EDGE_CURVE ( 'NONE', #18613, #38614, #7184, .T. ) ;
#29256=VERTEX_POINT ( 'NONE', #177 ) ;
#29258=DIRECTION ( 'NONE',  ( -3.071710424422018668E-17, 6.404604876783312462E-16, 1.000000000000000000 ) ) ;
#29260=DIRECTION ( 'NONE',  ( 0.9687793358424817702, -0.2479245821708688791, 0.000000000000000000 ) ) ;
#29284=CARTESIAN_POINT ( 'NONE',  ( -22.01964724813734620, -15.72799447708766962, 49.52966884056655772 ) ) ;
#29286=DIRECTION ( 'NONE',  ( 0.9687793358424819923, -0.2479245821708680464, 0.000000000000000000 ) ) ;
#29287=LINE ( 'NONE', #10340, #46388 ) ;
#29301=CARTESIAN_POINT ( 'NONE',  ( 0.000000000000000000, 0.000000000000000000, 0.000000000000000000 ) ) ;
#29302=EDGE_CURVE ( 'NONE', #6531, #42275, #44907, .T. ) ;
#29315=CARTESIAN_POINT ( 'NONE',  ( -15.03931914688375571, -19.48631565075837457, 52.02966884056656482 ) ) ;
#29316=EDGE_CURVE ( 'NONE', #14945, #44591, #14986, .T. ) ;
#29332=CARTESIAN_POINT ( 'NONE',  ( -13.33852097861372421, -12.48893720396535478, 49.52966884056655772 ) ) ;
#29341=CARTESIAN_POINT ( 'NONE',  ( -21.67230677980763431, -11.72453687863643523, 52.02966884056656482 ) ) ;
#29350=CYLINDRICAL_SURFACE ( 'NONE', #45580, 5.249999999999998224 ) ;
#29365=DIRECTION ( 'NONE',  ( -3.071710424422018668E-17, 6.404604876783312462E-16, 1.000000000000000000 ) ) ;
#29368=CARTESIAN_POINT ( 'NONE',  ( -20.96187357126569850, -17.88286835634646721, 52.02966884056656482 ) ) ;
#29375=CIRCLE ( 'NONE', #26239, 5.249999999999998224 ) ;
#29381=ORIENTED_EDGE ( 'NONE', *, *, #32710, .F. ) ;
#29385=DIRECTION ( 'NONE',  ( 0.9956360040033426229, -0.09332174201254549162, 0.000000000000000000 ) ) ;
#29388=EDGE_CURVE ( 'NONE', #30767, #33361, #46482, .T. ) ;
#29396=LINE ( 'NONE', #32830, #43868 ) ;
#29399=ORIENTED_EDGE ( 'NONE', *, *, #43452, .T. ) ;
#29400=CARTESIAN_POINT ( 'NONE',  ( -15.65212752116712558, -9.867280269464723474, 49.52966884056655772 ) ) ;
#29405=VECTOR ( 'NONE', #30447, 1000.000000000000000 ) ;
#29410=FACE_OUTER_BOUND ( 'NONE', #20860, .T. ) ;
#29411=CARTESIAN_POINT ( 'NONE',  ( -19.20714268997449281, -19.15619313305651161, 49.52966884056656482 ) ) ;
#29415=ORIENTED_EDGE ( 'NONE', *, *, #33556, .T. ) ;
#29427=CARTESIAN_POINT ( 'NONE',  ( -12.23896285002386719, -13.98645721660588137, 52.02966884056656482 ) ) ;
#29430=ORIENTED_EDGE ( 'NONE', *, *, #8261, .T. ) ;
#29441=CARTESIAN_POINT ( 'NONE',  ( -12.74141321320493958, -14.42442407569615348, 49.52966884056655772 ) ) ;
#29445=EDGE_CURVE ( 'NONE', #5150, #23878, #37059, .T. ) ;
#29454=DIRECTION ( 'NONE',  ( -3.071710424422018668E-17, 6.404604876783312462E-16, 1.000000000000000000 ) ) ;
#29472=AXIS2_PLACEMENT_3D ( 'NONE', #17227, #13046, #35461 ) ;
#29477=DIRECTION ( 'NONE',  ( -3.071710424422018668E-17, 6.404604876783312462E-16, 1.000000000000000000 ) ) ;
#29486=DIRECTION ( 'NONE',  ( -3.071710424422018668E-17, 6.404604876783312462E-16, 1.000000000000000000 ) ) ;
#29493=CARTESIAN_POINT ( 'NONE',  ( -13.52486571068042487, -17.40907233461224379, 52.02966884056656482 ) ) ;
#29497=AXIS2_PLACEMENT_3D ( 'NONE', #29598, #48301, #40670 ) ;
#29499=CARTESIAN_POINT ( 'NONE',  ( -17.42409385541299471, -14.80920654474435771, 49.52966884056655772 ) ) ;
#29507=ORIENTED_EDGE ( 'NONE', *, *, #39407, .T. ) ;
#29511=ADVANCED_FACE ( 'NONE', ( #24528 ), #10465, .T. ) ;
#29514=DIRECTION ( 'NONE',  ( -3.071710424422018668E-17, 6.404604876783312462E-16, 1.000000000000000000 ) ) ;
#29521=ORIENTED_EDGE ( 'NONE', *, *, #3154, .T. ) ;
#29537=AXIS2_PLACEMENT_3D ( 'NONE', #24887, #35950, #16749 ) ;
#29538=EDGE_LOOP ( 'NONE', ( #34026, #47851, #15644, #13255 ) ) ;
#29541=DIRECTION ( 'NONE',  ( -3.071710424422018668E-17, 6.404604876783312462E-16, 1.000000000000000000 ) ) ;
#29550=ORIENTED_EDGE ( 'NONE', *, *, #7922, .T. ) ;
#29556=CARTESIAN_POINT ( 'NONE',  ( -21.99019323879806365, -13.75373571565882536, 52.02966884056656482 ) ) ;
#29561=VECTOR ( 'NONE', #38877, 1000.000000000000000 ) ;
#29562=ORIENTED_EDGE ( 'NONE', *, *, #8208, .F. ) ;
#29566=ORIENTED_EDGE ( 'NONE', *, *, #32718, .T. ) ;
#29571=CARTESIAN_POINT ( 'NONE',  ( -17.42409385541299471, -14.80920654474435771, 49.52966884056655772 ) ) ;
#29581=CYLINDRICAL_SURFACE ( 'NONE', #41536, 2.000000000000003109 ) ;
#29582=CARTESIAN_POINT ( 'NONE',  ( -17.42409385541299471, -14.80920654474435771, 49.52966884056655772 ) ) ;
#29583=DIRECTION ( 'NONE',  ( -0.9956360040033419567, 0.09332174201255252766, 0.000000000000000000 ) ) ;
#29593=DIRECTION ( 'NONE',  ( -3.071710424422018668E-17, 6.404604876783312462E-16, 1.000000000000000000 ) ) ;
#29598=CARTESIAN_POINT ( 'NONE',  ( -17.42409385541299471, -14.80920654474435771, 49.52966884056655772 ) ) ;
#29625=DIRECTION ( 'NONE',  ( -0.5097212845717550289, 0.8603395911234820170, 0.000000000000000000 ) ) ;
#29629=PLANE ( 'NONE',  #7898 ) ;
#29631=CYLINDRICAL_SURFACE ( 'NONE', #36772, 2.000000000000001776 ) ;
#29641=CARTESIAN_POINT ( 'NONE',  ( -12.73887154267113253, -15.16169402761810048, 49.52966884056655772 ) ) ;
#29664=LINE ( 'NONE', #41229, #42478 ) ;
#29668=EDGE_CURVE ( 'NONE', #25804, #45155, #29995, .T. ) ;
#29671=CARTESIAN_POINT ( 'NONE',  ( -17.42409385541299471, -14.80920654474434883, 62.02966884056656482 ) ) ;
#29682=ORIENTED_EDGE ( 'NONE', *, *, #3154, .F. ) ;
#29683=DIRECTION ( 'NONE',  ( -0.9687793358424819923, 0.2479245821708680464, 0.000000000000000000 ) ) ;
#29692=LINE ( 'NONE', #37803, #25051 ) ;
#29714=AXIS2_PLACEMENT_3D ( 'NONE', #15014, #45592, #12081 ) ;
#29715=DIRECTION ( 'NONE',  ( 0.9979768094191903138, 0.06357898915123796901, 0.000000000000000000 ) ) ;
#29721=AXIS2_PLACEMENT_3D ( 'NONE', #21828, #44743, #3107 ) ;
#29727=CARTESIAN_POINT ( 'NONE',  ( -20.32907747881911575, -11.13165948213017131, 49.52966884056655772 ) ) ;
#29732=ADVANCED_FACE ( 'NONE', ( #33820 ), #15339, .T. ) ;
#29734=ADVANCED_FACE ( 'NONE', ( #29410 ), #38736, .T. ) ;
#29736=CARTESIAN_POINT ( 'NONE',  ( -12.75531685953890282, -14.40201664703461049, 49.52966884056655772 ) ) ;
#29744=CARTESIAN_POINT ( 'NONE',  ( -17.42409385541299471, -14.80920654474435594, 52.02966884056656482 ) ) ;
#29746=CARTESIAN_POINT ( 'NONE',  ( -16.75933984047804515, -20.01695097968237036, 50.77966884056656482 ) ) ;
#29747=AXIS2_PLACEMENT_3D ( 'NONE', #29641, #3532, #47872 ) ;
#29752=CIRCLE ( 'NONE', #22690, 1.999999999999999334 ) ;
#29762=CARTESIAN_POINT ( 'NONE',  ( -20.59270190486383356, -18.27842527154038166, 52.02966884056656482 ) ) ;
#29764=ORIENTED_EDGE ( 'NONE', *, *, #12760, .T. ) ;
#29767=ORIENTED_EDGE ( 'NONE', *, *, #18443, .T. ) ;
#29769=ADVANCED_FACE ( 'NONE', ( #34800 ), #42447, .T. ) ;
#29796=CARTESIAN_POINT ( 'NONE',  ( -14.24626305875727184, -11.36469298288595553, 52.02966884056656482 ) ) ;
#29797=DIRECTION ( 'NONE',  ( -0.9687793358424822143, 0.2479245821708672415, 0.000000000000000000 ) ) ;
#29802=DIRECTION ( 'NONE',  ( -3.071710424422018668E-17, 6.404604876783312462E-16, 1.000000000000000000 ) ) ;
#29806=EDGE_CURVE ( 'NONE', #28884, #4347, #38665, .T. ) ;
#29815=( GEOMETRIC_REPRESENTATION_CONTEXT ( 3 ) GLOBAL_UNCERTAINTY_ASSIGNED_CONTEXT ( ( #44025 ) ) GLOBAL_UNIT_ASSIGNED_CONTEXT ( ( #31009, #26835, #46029 ) ) REPRESENTATION_CONTEXT ( 'NONE', 'WORKASPACE' ) );
#29819=AXIS2_PLACEMENT_3D ( 'NONE', #11248, #28798, #36169 ) ;
#29824=DIRECTION ( 'NONE',  ( -0.3964226963016467820, -0.9180681052388935948, 0.000000000000000000 ) ) ;
#29828=CIRCLE ( 'NONE', #16416, 2.000000000000001332 ) ;
#29831=CARTESIAN_POINT ( 'NONE',  ( -15.46621039653938112, -10.55127575485719760, 49.52966884056655772 ) ) ;
#29835=CARTESIAN_POINT ( 'NONE',  ( -21.99649211598757859, -13.72812852161587038, 49.52966884056655772 ) ) ;
#29844=ORIENTED_EDGE ( 'NONE', *, *, #22726, .F. ) ;
#29858=CIRCLE ( 'NONE', #37711, 4.686499999999997890 ) ;
#29860=DIRECTION ( 'NONE',  ( 0.9687793358424821033, -0.2479245821708680464, 0.000000000000000000 ) ) ;
#29864=ORIENTED_EDGE ( 'NONE', *, *, #13237, .F. ) ;
#29869=LINE ( 'NONE', #45375, #905 ) ;
#29874=CARTESIAN_POINT ( 'NONE',  ( -21.98892968875003717, -15.92178434430670642, 49.52966884056655772 ) ) ;
#29882=EDGE_CURVE ( 'NONE', #17452, #19689, #35999, .T. ) ;
#29891=CIRCLE ( 'NONE', #41697, 4.686499999999999666 ) ;
#29899=CARTESIAN_POINT ( 'NONE',  ( -22.09321184435721719, -14.28490438881294367, 49.52966884056655772 ) ) ;
#29907=DIRECTION ( 'NONE',  ( 0.9687793358424822143, -0.2479245821708672415, 0.000000000000000000 ) ) ;
#29908=CARTESIAN_POINT ( 'NONE',  ( -15.10382451463400955, -18.89477942154363532, 52.02966884056656482 ) ) ;
#29912=ORIENTED_EDGE ( 'NONE', *, *, #37338, .F. ) ;
#29917=CARTESIAN_POINT ( 'NONE',  ( -21.01334446694451685, -11.79580940901521657, 52.02966884056656482 ) ) ;
#29923=AXIS2_PLACEMENT_3D ( 'NONE', #32717, #44082, #21170 ) ;
#29927=AXIS2_PLACEMENT_3D ( 'NONE', #36375, #14668, #32462 ) ;
#29929=DIRECTION ( 'NONE',  ( -0.9687793358424822143, 0.2479245821708672415, 0.000000000000000000 ) ) ;
#29941=DIRECTION ( 'NONE',  ( 0.9757441136919974278, 0.2189141945955503377, 0.000000000000000000 ) ) ;
#29955=VERTEX_POINT ( 'NONE', #2036 ) ;
#29960=DIRECTION ( 'NONE',  ( 0.9687793358424821033, -0.2479245821708677133, 0.000000000000000000 ) ) ;
#29961=ORIENTED_EDGE ( 'NONE', *, *, #8617, .F. ) ;
#29967=AXIS2_PLACEMENT_3D ( 'NONE', #1794, #35747, #43415 ) ;
#29971=ORIENTED_EDGE ( 'NONE', *, *, #6560, .F. ) ;
#29975=AXIS2_PLACEMENT_3D ( 'NONE', #27972, #5587, #16645 ) ;
#29993=LINE ( 'NONE', #26290, #35885 ) ;
#29995=CIRCLE ( 'NONE', #43388, 2.000000000000000888 ) ;
#30009=ORIENTED_EDGE ( 'NONE', *, *, #40366, .F. ) ;
#30011=VERTEX_POINT ( 'NONE', #3188 ) ;
#30014=ADVANCED_FACE ( 'NONE', ( #10586 ), #44565, .T. ) ;
#30026=DIRECTION ( 'NONE',  ( -3.071710424422018668E-17, 6.404604876783312462E-16, 1.000000000000000000 ) ) ;
#30032=AXIS2_PLACEMENT_3D ( 'NONE', #7286, #17845, #7529 ) ;
#30036=VERTEX_POINT ( 'NONE', #44822 ) ;
#30051=AXIS2_PLACEMENT_3D ( 'NONE', #20780, #35785, #2064 ) ;
#30053=CYLINDRICAL_SURFACE ( 'NONE', #27592, 4.686499999999997002 ) ;
#30064=ADVANCED_FACE ( 'NONE', ( #26333 ), #22395, .T. ) ;
#30075=EDGE_LOOP ( 'NONE', ( #40447, #42157, #18587, #33476 ) ) ;
#30076=CARTESIAN_POINT ( 'NONE',  ( -15.13017050835524913, -18.89591645955643884, 49.52966884056656482 ) ) ;
#30087=LINE ( 'NONE', #25636, #23467 ) ;
#30103=DIRECTION ( 'NONE',  ( 0.9687793358424821033, -0.2479245821708679909, 0.000000000000000000 ) ) ;
#30117=ORIENTED_EDGE ( 'NONE', *, *, #44807, .T. ) ;
#30121=DIRECTION ( 'NONE',  ( -3.071710424422018668E-17, 6.404604876783312462E-16, 1.000000000000000000 ) ) ;
#30126=AXIS2_PLACEMENT_3D ( 'NONE', #7230, #44187, #36732 ) ;
#30135=CARTESIAN_POINT ( 'NONE',  ( -17.42409385541299471, -14.80920654474435771, 49.52966884056655772 ) ) ;
#30140=CARTESIAN_POINT ( 'NONE',  ( -17.42409385541299471, -14.80920654474435594, 52.02966884056656482 ) ) ;
#30145=LINE ( 'NONE', #25950, #39977 ) ;
#30157=ADVANCED_FACE ( 'NONE', ( #19922 ), #19189, .T. ) ;
#30160=EDGE_CURVE ( 'NONE', #30521, #10974, #36269, .T. ) ;
#30167=VECTOR ( 'NONE', #23292, 1000.000000000000000 ) ;
#30178=CYLINDRICAL_SURFACE ( 'NONE', #15036, 4.686499999999997002 ) ;
#30187=ORIENTED_EDGE ( 'NONE', *, *, #37615, .T. ) ;
#30200=DIRECTION ( 'NONE',  ( -3.071710424422018668E-17, 6.404604876783312462E-16, 1.000000000000000000 ) ) ;
#30215=DIRECTION ( 'NONE',  ( -3.071710424422018668E-17, 6.404604876783312462E-16, 1.000000000000000000 ) ) ;
#30223=ORIENTED_EDGE ( 'NONE', *, *, #36652, .T. ) ;
#30228=CARTESIAN_POINT ( 'NONE',  ( -14.33942418930512019, -10.56099362034968614, 52.02966884056656482 ) ) ;
#30252=DIRECTION ( 'NONE',  ( -3.071710424422018668E-17, 6.404604876783312462E-16, 1.000000000000000000 ) ) ;
#30263=CYLINDRICAL_SURFACE ( 'NONE', #17782, 1.999999999999999556 ) ;
#30274=CARTESIAN_POINT ( 'NONE',  ( -21.76886496386750736, -13.05243499865791890, 52.02966884056656482 ) ) ;
#30282=CYLINDRICAL_SURFACE ( 'NONE', #43788, 1.999999999999999112 ) ;
#30288=CARTESIAN_POINT ( 'NONE',  ( -22.58237342315448615, -13.83214364962418053, 52.02966884056656482 ) ) ;
#30289=CARTESIAN_POINT ( 'NONE',  ( -13.02585106727260822, -13.15662797718154309, 49.52966884056655772 ) ) ;
#30291=CYLINDRICAL_SURFACE ( 'NONE', #44658, 2.000000000000001332 ) ;
#30292=EDGE_CURVE ( 'NONE', #17919, #44193, #47369, .T. ) ;
#30295=CYLINDRICAL_SURFACE ( 'NONE', #20158, 2.000000000000001332 ) ;
#30296=DIRECTION ( 'NONE',  ( 0.9687793358424821033, -0.2479245821708679909, 0.000000000000000000 ) ) ;
#30301=ORIENTED_EDGE ( 'NONE', *, *, #3362, .F. ) ;
#30310=DIRECTION ( 'NONE',  ( 3.071710424422018668E-17, -6.404604876783312462E-16, -1.000000000000000000 ) ) ;
#30322=LINE ( 'NONE', #42116, #48614 ) ;
#30335=CIRCLE ( 'NONE', #15356, 2.000000000000001776 ) ;
#30344=ORIENTED_EDGE ( 'NONE', *, *, #28419, .T. ) ;
#30346=FACE_OUTER_BOUND ( 'NONE', #23197, .T. ) ;
#30365=EDGE_CURVE ( 'NONE', #16073, #16677, #14853, .T. ) ;
#30366=DIRECTION ( 'NONE',  ( -3.071710424422018668E-17, 6.404604876783312462E-16, 1.000000000000000000 ) ) ;
#30370=LINE ( 'NONE', #38456, #47442 ) ;
#30371=VERTEX_POINT ( 'NONE', #44951 ) ;
#30378=CYLINDRICAL_SURFACE ( 'NONE', #35443, 4.686499999999997002 ) ;
#30379=CARTESIAN_POINT ( 'NONE',  ( -17.42409385541299471, -14.80920654474435771, 49.52966884056655772 ) ) ;
#30385=DIRECTION ( 'NONE',  ( -3.071710424422018668E-17, 6.404604876783312462E-16, 1.000000000000000000 ) ) ;
#30398=CARTESIAN_POINT ( 'NONE',  ( -15.10382451463400955, -18.89477942154363888, 49.52966884056656482 ) ) ;
#30402=ORIENTED_EDGE ( 'NONE', *, *, #3955, .F. ) ;
#30412=DIRECTION ( 'NONE',  ( -3.071710424422018668E-17, 6.404604876783312462E-16, 1.000000000000000000 ) ) ;
#30414=CARTESIAN_POINT ( 'NONE',  ( -21.75868347184070473, -16.62218431696164345, 52.02966884056656482 ) ) ;
#30415=CARTESIAN_POINT ( 'NONE',  ( -17.42409385541299471, -14.80920654474435594, 52.02966884056656482 ) ) ;
#30420=CARTESIAN_POINT ( 'NONE',  ( -17.42409385541299471, -14.80920654474434883, 62.02966884056656482 ) ) ;
#30425=EDGE_CURVE ( 'NONE', #43774, #35420, #48366, .T. ) ;
#30431=VERTEX_POINT ( 'NONE', #38012 ) ;
#30447=DIRECTION ( 'NONE',  ( -3.071710424422018668E-17, 6.404604876783312462E-16, 1.000000000000000000 ) ) ;
#30460=EDGE_CURVE ( 'NONE', #8065, #1168, #8843, .T. ) ;
#30466=ORIENTED_EDGE ( 'NONE', *, *, #7328, .T. ) ;
#30473=CARTESIAN_POINT ( 'NONE',  ( -19.20714268997449281, -19.15619313305651161, 49.52966884056656482 ) ) ;
#30474=ADVANCED_FACE ( 'NONE', ( #35292 ), #46395, .T. ) ;
#30479=VERTEX_POINT ( 'NONE', #42460 ) ;
#30485=AXIS2_PLACEMENT_3D ( 'NONE', #38152, #38394, #42843 ) ;
#30496=CARTESIAN_POINT ( 'NONE',  ( -17.42409385541299471, -14.80920654474434883, 62.02966884056656482 ) ) ;
#30497=DIRECTION ( 'NONE',  ( 3.071710424422018668E-17, -6.404604876783312462E-16, -1.000000000000000000 ) ) ;
#30502=DIRECTION ( 'NONE',  ( -3.071710424422018668E-17, 6.404604876783312462E-16, 1.000000000000000000 ) ) ;
#30504=ORIENTED_EDGE ( 'NONE', *, *, #11058, .F. ) ;
#30511=CARTESIAN_POINT ( 'NONE',  ( -17.42409385541299471, -14.80920654474435594, 52.02966884056656482 ) ) ;
#30514=DIRECTION ( 'NONE',  ( -3.071710424422018668E-17, 6.404604876783312462E-16, 1.000000000000000000 ) ) ;
#30521=VERTEX_POINT ( 'NONE', #20539 ) ;
#30530=CARTESIAN_POINT ( 'NONE',  ( -13.07932274695846964, -16.56597809083076100, 49.52966884056655772 ) ) ;
#30531=CARTESIAN_POINT ( 'NONE',  ( -17.09591293804728807, -10.13421140726271297, 49.52966884056655772 ) ) ;
#30539=CIRCLE ( 'NONE', #17128, 2.000000000000000888 ) ;
#30549=AXIS2_PLACEMENT_3D ( 'NONE', #41268, #18865, #37309 ) ;
#30565=EDGE_CURVE ( 'NONE', #30011, #19030, #36327, .T. ) ;
#30569=AXIS2_PLACEMENT_3D ( 'NONE', #9869, #47304, #24886 ) ;
#30574=AXIS2_PLACEMENT_3D ( 'NONE', #10943, #44443, #33822 ) ;
#30577=DIRECTION ( 'NONE',  ( -3.071710424422018668E-17, 6.404604876783312462E-16, 1.000000000000000000 ) ) ;
#30581=ORIENTED_EDGE ( 'NONE', *, *, #34370, .F. ) ;
#30587=AXIS2_PLACEMENT_3D ( 'NONE', #30496, #11771, #26790 ) ;
#30595=CARTESIAN_POINT ( 'NONE',  ( -17.42409385541299471, -14.80920654474434883, 62.02966884056656482 ) ) ;
#30614=ORIENTED_EDGE ( 'NONE', *, *, #18582, .T. ) ;
#30623=CARTESIAN_POINT ( 'NONE',  ( -13.42648243792925378, -12.34047032955235679, 49.52966884056655772 ) ) ;
#30627=CARTESIAN_POINT ( 'NONE',  ( -17.42409385541299471, -14.80920654474435771, 49.52966884056655772 ) ) ;
#30641=AXIS2_PLACEMENT_3D ( 'NONE', #32082, #35526, #43167 ) ;
#30643=DIRECTION ( 'NONE',  ( -3.071710424422018668E-17, 6.404604876783312462E-16, 1.000000000000000000 ) ) ;
#30644=VERTEX_POINT ( 'NONE', #47605 ) ;
#30658=VECTOR ( 'NONE', #43843, 1000.000000000000000 ) ;
#30659=LINE ( 'NONE', #12403, #5953 ) ;
#30668=DIRECTION ( 'NONE',  ( -3.071710424422018668E-17, 6.404604876783312462E-16, 1.000000000000000000 ) ) ;
#30675=AXIS2_PLACEMENT_3D ( 'NONE', #20345, #12225, #20594 ) ;
#30677=CARTESIAN_POINT ( 'NONE',  ( -17.42409385541299471, -14.80920654474434883, 62.02966884056656482 ) ) ;
#30689=CARTESIAN_POINT ( 'NONE',  ( -13.71073213066623531, -18.52046572475129338, 49.52966884056656482 ) ) ;
#30690=LINE ( 'NONE', #30931, #7725 ) ;
#30695=AXIS2_PLACEMENT_3D ( 'NONE', #48467, #3173, #47746 ) ;
#30705=EDGE_LOOP ( 'NONE', ( #11878, #44289, #3112, #3239 ) ) ;
#30720=ORIENTED_EDGE ( 'NONE', *, *, #32261, .F. ) ;
#30731=DIRECTION ( 'NONE',  ( -0.9687793358424819923, 0.2479245821708680464, 0.000000000000000000 ) ) ;
#30754=ORIENTED_EDGE ( 'NONE', *, *, #27395, .F. ) ;
#30765=VECTOR ( 'NONE', #33857, 1000.000000000000000 ) ;
#30767=VERTEX_POINT ( 'NONE', #34257 ) ;
#30768=FACE_OUTER_BOUND ( 'NONE', #5064, .T. ) ;
#30780=SHAPE_REPRESENTATION_RELATIONSHIP ( 'NONE' , 'NONE' ,  #2486, #26163 ) ;
#30784=CIRCLE ( 'NONE', #44067, 1.999999999999999556 ) ;
#30796=EDGE_LOOP ( 'NONE', ( #16269, #34902, #15109, #24768 ) ) ;
#30836=EDGE_LOOP ( 'NONE', ( #34365, #44081, #27833, #23 ) ) ;
#30840=CARTESIAN_POINT ( 'NONE',  ( -15.03931914688375571, -19.48631565075837457, 50.77966884056656482 ) ) ;
#30845=ORIENTED_EDGE ( 'NONE', *, *, #47908, .T. ) ;
#30847=( NAMED_UNIT ( * ) SI_UNIT ( $, .STERADIAN. ) SOLID_ANGLE_UNIT ( ) );
#30850=ADVANCED_FACE ( 'NONE', ( #5459 ), #9391, .T. ) ;
#30851=EDGE_CURVE ( 'NONE', #25136, #17454, #28817, .T. ) ;
#30854=CARTESIAN_POINT ( 'NONE',  ( -17.42409385541299471, -14.80920654474435594, 52.02966884056656482 ) ) ;
#30855=ORIENTED_EDGE ( 'NONE', *, *, #38370, .T. ) ;
#30862=ORIENTED_EDGE ( 'NONE', *, *, #8626, .F. ) ;
#30871=CARTESIAN_POINT ( 'NONE',  ( -16.29155950929526497, -19.35680461458998636, 49.52966884056656482 ) ) ;
#30876=DIRECTION ( 'NONE',  ( -3.071710424422018668E-17, 6.404604876783312462E-16, 1.000000000000000000 ) ) ;
#30879=ORIENTED_EDGE ( 'NONE', *, *, #21294, .F. ) ;
#30881=LINE ( 'NONE', #45894, #24355 ) ;
#30903=EDGE_CURVE ( 'NONE', #6216, #36884, #17460, .T. ) ;
#30904=CARTESIAN_POINT ( 'NONE',  ( -17.23552066371262725, -19.49191114800217406, 49.52966884056656482 ) ) ;
#30909=ADVANCED_FACE ( 'NONE', ( #9644 ), #28586, .T. ) ;
#30919=CARTESIAN_POINT ( 'NONE',  ( -17.42409385541299471, -14.80920654474434883, 62.02966884056656482 ) ) ;
#30923=EDGE_LOOP ( 'NONE', ( #37733, #30402, #21169, #35687 ) ) ;
#30930=CARTESIAN_POINT ( 'NONE',  ( -17.42409385541299471, -14.80920654474435771, 49.52966884056655772 ) ) ;
#30931=CARTESIAN_POINT ( 'NONE',  ( -12.74698474939898318, -12.42443183621510094, 50.77966884056655772 ) ) ;
#30935=AXIS2_PLACEMENT_3D ( 'NONE', #29874, #33283, #21992 ) ;
#30942=ORIENTED_EDGE ( 'NONE', *, *, #24490, .F. ) ;
#30950=CARTESIAN_POINT ( 'NONE',  ( -20.48780003469585154, -11.24700778661463829, 49.52966884056655772 ) ) ;
#30955=VERTEX_POINT ( 'NONE', #39901 ) ;
#30961=EDGE_LOOP ( 'NONE', ( #296, #47310, #2773, #27034 ) ) ;
#30966=CIRCLE ( 'NONE', #33279, 4.686499999999999666 ) ;
#30969=ADVANCED_FACE ( 'NONE', ( #18952 ), #41352, .T. ) ;
#30971=FACE_OUTER_BOUND ( 'NONE', #23363, .T. ) ;
#30973=DIRECTION ( 'NONE',  ( 0.9687793358424819923, -0.2479245821708678243, 0.000000000000000000 ) ) ;
#30988=CARTESIAN_POINT ( 'NONE',  ( -13.50190746284422794, -17.39609839546894676, 49.52966884056655772 ) ) ;
#31001=CARTESIAN_POINT ( 'NONE',  ( -12.43058792219793141, -16.43013174195301218, 50.77966884056655772 ) ) ;
#31009=( LENGTH_UNIT ( ) NAMED_UNIT ( * ) SI_UNIT ( .MILLI., .METRE. ) );
#31011=CARTESIAN_POINT ( 'NONE',  ( -17.42409385541299471, -14.80920654474435771, 49.52966884056655772 ) ) ;
#31013=VERTEX_POINT ( 'NONE', #44338 ) ;
#31015=DIRECTION ( 'NONE',  ( 3.071710424422018668E-17, -6.404604876783312462E-16, -1.000000000000000000 ) ) ;
#31024=CIRCLE ( 'NONE', #34915, 2.000000000000000444 ) ;
#31026=CARTESIAN_POINT ( 'NONE',  ( -17.42409385541299471, -14.80920654474435771, 49.52966884056655772 ) ) ;
#31030=EDGE_CURVE ( 'NONE', #44219, #6337, #45790, .T. ) ;
#31038=DIRECTION ( 'NONE',  ( 0.9294853595766545684, 0.3688590060343616139, 0.000000000000000000 ) ) ;
#31041=CARTESIAN_POINT ( 'NONE',  ( -17.42409385541299471, -14.80920654474435594, 52.02966884056656482 ) ) ;
#31049=CARTESIAN_POINT ( 'NONE',  ( -14.94170459844064780, -18.78425696289860269, 52.02966884056656482 ) ) ;
#31052=VERTEX_POINT ( 'NONE', #48490 ) ;
#31057=DIRECTION ( 'NONE',  ( 0.9687793358424817702, -0.2479245821708684350, 0.000000000000000000 ) ) ;
#31067=DIRECTION ( 'NONE',  ( -3.071710424422018668E-17, 6.404604876783312462E-16, 1.000000000000000000 ) ) ;
#31069=ADVANCED_FACE ( 'NONE', ( #33701 ), #30053, .T. ) ;
#31077=ADVANCED_FACE ( 'NONE', ( #45312 ), #14723, .T. ) ;
#31080=EDGE_CURVE ( 'NONE', #46754, #2300, #4792, .T. ) ;
#31093=AXIS2_PLACEMENT_3D ( 'NONE', #2209, #17219, #39881 ) ;
#31098=DIRECTION ( 'NONE',  ( 0.8447509909909733938, -0.5351595679979650466, 0.000000000000000000 ) ) ;
#31099=LINE ( 'NONE', #38724, #15218 ) ;
#31110=ORIENTED_EDGE ( 'NONE', *, *, #3753, .F. ) ;
#31122=CARTESIAN_POINT ( 'NONE',  ( -17.42409385541299471, -14.80920654474435771, 49.52966884056655772 ) ) ;
#31131=EDGE_CURVE ( 'NONE', #19773, #10407, #21316, .T. ) ;
#31140=ORIENTED_EDGE ( 'NONE', *, *, #17147, .F. ) ;
#31150=CARTESIAN_POINT ( 'NONE',  ( -17.42409385541299471, -14.80920654474435771, 49.52966884056655772 ) ) ;
#31154=VECTOR ( 'NONE', #46882, 1000.000000000000000 ) ;
#31155=AXIS2_PLACEMENT_3D ( 'NONE', #14427, #36608, #7093 ) ;
#31163=CARTESIAN_POINT ( 'NONE',  ( -20.01098570613759975, -18.73139293731311383, 49.52966884056656482 ) ) ;
#31164=ORIENTED_EDGE ( 'NONE', *, *, #5542, .T. ) ;
#31167=DIRECTION ( 'NONE',  ( 0.8603395911234833493, 0.5097212845717526974, 0.000000000000000000 ) ) ;
#31199=AXIS2_PLACEMENT_3D ( 'NONE', #36085, #10000, #22055 ) ;
#31205=EDGE_LOOP ( 'NONE', ( #4913, #43460 ) ) ;
#31215=ADVANCED_FACE ( 'NONE', ( #35419 ), #28765, .T. ) ;
#31218=DIRECTION ( 'NONE',  ( -0.7506333037770538397, 0.6607190350373941534, 0.000000000000000000 ) ) ;
#31228=CIRCLE ( 'NONE', #5291, 2.000000000000002220 ) ;
#31233=VERTEX_POINT ( 'NONE', #35655 ) ;
#31237=LINE ( 'NONE', #42584, #33517 ) ;
#31270=ORIENTED_EDGE ( 'NONE', *, *, #19708, .T. ) ;
#31272=ADVANCED_FACE ( 'NONE', ( #46759 ), #28034, .T. ) ;
#31275=LINE ( 'NONE', #27584, #18115 ) ;
#31279=FACE_OUTER_BOUND ( 'NONE', #42893, .T. ) ;
#31283=ORIENTED_EDGE ( 'NONE', *, *, #14686, .T. ) ;
#31289=AXIS2_PLACEMENT_3D ( 'NONE', #2568, #36036, #46662 ) ;
#31292=CARTESIAN_POINT ( 'NONE',  ( -13.40955617598886995, -17.25032161083215954, 49.52966884056655772 ) ) ;
#31293=EDGE_CURVE ( 'NONE', #14076, #8151, #41298, .T. ) ;
#31296=CARTESIAN_POINT ( 'NONE',  ( -12.17647495751581133, -14.96730746957505076, 52.02966884056656482 ) ) ;
#31297=AXIS2_PLACEMENT_3D ( 'NONE', #20322, #42250, #42972 ) ;
#31312=VERTEX_POINT ( 'NONE', #44288 ) ;
#31328=ORIENTED_EDGE ( 'NONE', *, *, #15396, .T. ) ;
#31335=VECTOR ( 'NONE', #5792, 1000.000000000000000 ) ;
#31346=DIRECTION ( 'NONE',  ( 0.9687793358424821033, -0.2479245821708677133, 0.000000000000000000 ) ) ;
#31360=VERTEX_POINT ( 'NONE', #29003 ) ;
#31362=AXIS2_PLACEMENT_3D ( 'NONE', #24919, #39933, #17018 ) ;
#31364=DIRECTION ( 'NONE',  ( 0.9687793358424817702, -0.2479245821708684905, 0.000000000000000000 ) ) ;
#31371=EDGE_LOOP ( 'NONE', ( #37692, #45500, #31731, #15156 ) ) ;
#31385=ORIENTED_EDGE ( 'NONE', *, *, #33889, .T. ) ;
#31391=AXIS2_PLACEMENT_3D ( 'NONE', #48176, #6336, #21834 ) ;
#31399=CIRCLE ( 'NONE', #10185, 4.686499999999998778 ) ;
#31405=ORIENTED_EDGE ( 'NONE', *, *, #34946, .T. ) ;
#31408=ORIENTED_EDGE ( 'NONE', *, *, #20171, .F. ) ;
#31412=CARTESIAN_POINT ( 'NONE',  ( -17.42409385541299471, -14.80920654474435771, 49.52966884056655772 ) ) ;
#31416=EDGE_LOOP ( 'NONE', ( #42295, #24143, #31328, #6879 ) ) ;
#31422=ORIENTED_EDGE ( 'NONE', *, *, #22044, .T. ) ;
#31427=CARTESIAN_POINT ( 'NONE',  ( -22.41668094288463919, -16.43295965837073780, 49.52966884056655772 ) ) ;
#31430=AXIS2_PLACEMENT_3D ( 'NONE', #6877, #48229, #14466 ) ;
#31432=EDGE_LOOP ( 'NONE', ( #25375, #46660, #15029, #6 ) ) ;
#31447=CARTESIAN_POINT ( 'NONE',  ( -21.02292652713908794, -10.98678540089889744, 52.02966884056656482 ) ) ;
#31459=EDGE_CURVE ( 'NONE', #39406, #45116, #41769, .T. ) ;
#31464=FACE_OUTER_BOUND ( 'NONE', #26652, .T. ) ;
#31468=EDGE_LOOP ( 'NONE', ( #43378, #47711, #2499, #38944 ) ) ;
#31472=ORIENTED_EDGE ( 'NONE', *, *, #10906, .T. ) ;
#31478=CIRCLE ( 'NONE', #2407, 0.3999999999999978018 ) ;
#31498=VECTOR ( 'NONE', #46669, 1000.000000000000000 ) ;
#31514=ORIENTED_EDGE ( 'NONE', *, *, #7460, .T. ) ;
#31529=FACE_OUTER_BOUND ( 'NONE', #17623, .T. ) ;
#31530=CARTESIAN_POINT ( 'NONE',  ( -22.10255287824656989, -12.42708119714673565, 52.02966884056656482 ) ) ;
#31538=ORIENTED_EDGE ( 'NONE', *, *, #45709, .F. ) ;
#31548=AXIS2_PLACEMENT_3D ( 'NONE', #15301, #30366, #22474 ) ;
#31565=VECTOR ( 'NONE', #47102, 1000.000000000000000 ) ;
#31581=AXIS2_PLACEMENT_3D ( 'NONE', #40104, #47495, #29260 ) ;
#31596=VECTOR ( 'NONE', #4697, 1000.000000000000000 ) ;
#31598=DIRECTION ( 'NONE',  ( -3.071710424422018668E-17, 6.404604876783312462E-16, 1.000000000000000000 ) ) ;
#31611=VECTOR ( 'NONE', #7102, 1000.000000000000000 ) ;
#31613=ORIENTED_EDGE ( 'NONE', *, *, #13484, .T. ) ;
#31617=CARTESIAN_POINT ( 'NONE',  ( -17.42409385541299471, -14.80920654474435771, 49.52966884056655772 ) ) ;
#31628=FACE_OUTER_BOUND ( 'NONE', #30705, .T. ) ;
#31649=CARTESIAN_POINT ( 'NONE',  ( -13.88631413956031579, -11.73554473314222157, 49.52966884056655772 ) ) ;
#31650=LINE ( 'NONE', #47633, #43932 ) ;
#31654=CARTESIAN_POINT ( 'NONE',  ( -21.00733138479494855, -11.77013360165372013, 49.52966884056655772 ) ) ;
#31655=DIRECTION ( 'NONE',  ( 0.9687793358424821033, -0.2479245821708677133, 0.000000000000000000 ) ) ;
#31657=VERTEX_POINT ( 'NONE', #14608 ) ;
#31664=ORIENTED_EDGE ( 'NONE', *, *, #7328, .F. ) ;
#31697=ORIENTED_EDGE ( 'NONE', *, *, #19073, .T. ) ;
#31704=CYLINDRICAL_SURFACE ( 'NONE', #43650, 5.249999999999998224 ) ;
#31710=DIRECTION ( 'NONE',  ( -3.071710424422018668E-17, 6.404604876783312462E-16, 1.000000000000000000 ) ) ;
#31715=EDGE_CURVE ( 'NONE', #44810, #39108, #35487, .T. ) ;
#31728=LINE ( 'NONE', #12992, #10248 ) ;
#31729=CARTESIAN_POINT ( 'NONE',  ( -18.34288178775629419, -10.21365315202000446, 49.52966884056655772 ) ) ;
#31731=ORIENTED_EDGE ( 'NONE', *, *, #36083, .F. ) ;
#31732=ORIENTED_EDGE ( 'NONE', *, *, #32261, .T. ) ;
#31735=AXIS2_PLACEMENT_3D ( 'NONE', #36513, #2799, #47866 ) ;
#31736=CARTESIAN_POINT ( 'NONE',  ( -21.70267066777908838, -12.86772875551264050, 49.52966884056655772 ) ) ;
#31741=ORIENTED_EDGE ( 'NONE', *, *, #13484, .F. ) ;
#31747=EDGE_LOOP ( 'NONE', ( #38675, #41626, #29971, #46109 ) ) ;
#31757=VERTEX_POINT ( 'NONE', #29427 ) ;
#31761=CARTESIAN_POINT ( 'NONE',  ( -16.31151605585062825, -19.37404237808139484, 49.52966884056656482 ) ) ;
#31768=EDGE_LOOP ( 'NONE', ( #37337, #1426, #34773, #33665 ) ) ;
#31775=ORIENTED_EDGE ( 'NONE', *, *, #28360, .F. ) ;
#31808=DIRECTION ( 'NONE',  ( 0.9687793358424821033, -0.2479245821708680464, 0.000000000000000000 ) ) ;
#31834=VECTOR ( 'NONE', #20580, 1000.000000000000000 ) ;
#31847=EDGE_CURVE ( 'NONE', #20066, #43487, #885, .T. ) ;
#31850=EDGE_CURVE ( 'NONE', #10797, #36678, #26717, .T. ) ;
#31855=DIRECTION ( 'NONE',  ( 0.9687793358424817702, -0.2479245821708688791, 0.000000000000000000 ) ) ;
#31863=AXIS2_PLACEMENT_3D ( 'NONE', #45616, #11868, #11371 ) ;
#31879=FACE_OUTER_BOUND ( 'NONE', #44378, .T. ) ;
#31882=CARTESIAN_POINT ( 'NONE',  ( -12.82854046268865034, -13.89041861240101206, 49.52966884056655772 ) ) ;
#31892=CARTESIAN_POINT ( 'NONE',  ( -22.41759978862804914, -13.18828134753566417, 49.52966884056655772 ) ) ;
#31894=DIRECTION ( 'NONE',  ( -0.2189141945955536961, 0.9757441136919967617, 0.000000000000000000 ) ) ;
#31898=FACE_OUTER_BOUND ( 'NONE', #37941, .T. ) ;
#31903=ORIENTED_EDGE ( 'NONE', *, *, #30903, .F. ) ;
#31922=CARTESIAN_POINT ( 'NONE',  ( -20.32907747881911575, -11.13165948213016776, 52.02966884056656482 ) ) ;
#31924=ORIENTED_EDGE ( 'NONE', *, *, #25377, .F. ) ;
#31930=ORIENTED_EDGE ( 'NONE', *, *, #43854, .T. ) ;
#31939=DIRECTION ( 'NONE',  ( -3.071710424422018668E-17, 6.404604876783312462E-16, 1.000000000000000000 ) ) ;
#31940=CARTESIAN_POINT ( 'NONE',  ( -12.23849770038826534, -15.62901903366650380, 50.77966884056655772 ) ) ;
#31945=CARTESIAN_POINT ( 'NONE',  ( -22.09287085128708839, -15.21639644245407297, 49.52966884056655772 ) ) ;
#31946=ORIENTED_EDGE ( 'NONE', *, *, #2736, .F. ) ;
#31950=ORIENTED_EDGE ( 'NONE', *, *, #35320, .F. ) ;
#31969=CARTESIAN_POINT ( 'NONE',  ( -13.52486571068042487, -17.40907233461224735, 49.52966884056655772 ) ) ;
#31986=EDGE_CURVE ( 'NONE', #42245, #44810, #15238, .T. ) ;
#32011=DIRECTION ( 'NONE',  ( 0.3964226963016397320, 0.9180681052388968144, 0.000000000000000000 ) ) ;
#32021=DIRECTION ( 'NONE',  ( -3.071710424422018668E-17, 6.404604876783312462E-16, 1.000000000000000000 ) ) ;
#32033=EDGE_LOOP ( 'NONE', ( #32949, #47176, #32230, #16214 ) ) ;
#32044=CYLINDRICAL_SURFACE ( 'NONE', #687, 1.999999999999999556 ) ;
#32046=EDGE_CURVE ( 'NONE', #40523, #14963, #11085, .T. ) ;
#32049=ORIENTED_EDGE ( 'NONE', *, *, #9628, .T. ) ;
#32065=DIRECTION ( 'NONE',  ( -3.071710424422018668E-17, 6.404604876783312462E-16, 1.000000000000000000 ) ) ;
#32066=CARTESIAN_POINT ( 'NONE',  ( -13.02884944951828494, -13.18282747993466941, 49.52966884056655772 ) ) ;
#32069=DIRECTION ( 'NONE',  ( 3.071710424422018668E-17, -6.404604876783312462E-16, -1.000000000000000000 ) ) ;
#32070=AXIS2_PLACEMENT_3D ( 'NONE', #25316, #48194, #10051 ) ;
#32071=CIRCLE ( 'NONE', #39166, 2.000000000000000000 ) ;
#32077=ORIENTED_EDGE ( 'NONE', *, *, #41059, .T. ) ;
#32082=CARTESIAN_POINT ( 'NONE',  ( -20.98629261354270170, -17.87291272402722697, 49.52966884056655772 ) ) ;
#32084=AXIS2_PLACEMENT_3D ( 'NONE', #29332, #17270, #2734 ) ;
#32100=VERTEX_POINT ( 'NONE', #8862 ) ;
#32111=CARTESIAN_POINT ( 'NONE',  ( -17.42409385541299471, -14.80920654474435771, 49.52966884056655772 ) ) ;
#32117=ORIENTED_EDGE ( 'NONE', *, *, #45166, .F. ) ;
#32119=CARTESIAN_POINT ( 'NONE',  ( -20.86860741727135959, -11.63137574808859753, 52.02966884056656482 ) ) ;
#32121=EDGE_CURVE ( 'NONE', #978, #4347, #38883, .T. ) ;
#32129=FACE_OUTER_BOUND ( 'NONE', #41620, .T. ) ;
#32142=ORIENTED_EDGE ( 'NONE', *, *, #22371, .T. ) ;
#32149=AXIS2_PLACEMENT_3D ( 'NONE', #29411, #40727, #29907 ) ;
#32150=AXIS2_PLACEMENT_3D ( 'NONE', #22413, #37404, #3700 ) ;
#32161=VERTEX_POINT ( 'NONE', #15480 ) ;
#32170=DIRECTION ( 'NONE',  ( 0.8603395911234834603, 0.5097212845717522534, 0.000000000000000000 ) ) ;
#32173=ORIENTED_EDGE ( 'NONE', *, *, #11450, .F. ) ;
#32187=EDGE_LOOP ( 'NONE', ( #26608, #30720, #3601, #43136 ) ) ;
#32220=ORIENTED_EDGE ( 'NONE', *, *, #26544, .T. ) ;
#32230=ORIENTED_EDGE ( 'NONE', *, *, #33737, .F. ) ;
#32233=AXIS2_PLACEMENT_3D ( 'NONE', #17931, #2686, #44801 ) ;
#32261=EDGE_CURVE ( 'NONE', #20521, #38839, #47723, .T. ) ;
#32274=CARTESIAN_POINT ( 'NONE',  ( -17.42409385541299471, -14.80920654474435594, 52.02966884056656482 ) ) ;
#32277=EDGE_CURVE ( 'NONE', #1628, #13690, #6118, .T. ) ;
#32309=ORIENTED_EDGE ( 'NONE', *, *, #33095, .T. ) ;
#32310=DIRECTION ( 'NONE',  ( -3.071710424422018668E-17, 6.404604876783312462E-16, 1.000000000000000000 ) ) ;
#32314=CIRCLE ( 'NONE', #23642, 5.249999999999998224 ) ;
#32323=DIRECTION ( 'NONE',  ( -3.071710424422018668E-17, 6.404604876783312462E-16, 1.000000000000000000 ) ) ;
#32333=FACE_OUTER_BOUND ( 'NONE', #26308, .T. ) ;
#32338=EDGE_CURVE ( 'NONE', #11839, #33399, #14677, .T. ) ;
#32347=EDGE_LOOP ( 'NONE', ( #12235, #1546, #46001, #19924 ) ) ;
#32357=AXIS2_PLACEMENT_3D ( 'NONE', #41981, #19317, #34085 ) ;
#32361=CIRCLE ( 'NONE', #25283, 2.000000000000000444 ) ;
#32364=DIRECTION ( 'NONE',  ( -3.071710424422018668E-17, 6.404604876783312462E-16, 1.000000000000000000 ) ) ;
#32366=AXIS2_PLACEMENT_3D ( 'NONE', #27859, #24175, #5467 ) ;
#32383=DIRECTION ( 'NONE',  ( -3.071710424422018668E-17, 6.404604876783312462E-16, 1.000000000000000000 ) ) ;
#32399=CIRCLE ( 'NONE', #44191, 5.249999999999998224 ) ;
#32414=AXIS2_PLACEMENT_3D ( 'NONE', #31617, #35540, #27427 ) ;
#32416=EDGE_LOOP ( 'NONE', ( #16594, #26510, #27070, #1878 ) ) ;
#32417=DIRECTION ( 'NONE',  ( 0.9687793358424821033, -0.2479245821708679909, 0.000000000000000000 ) ) ;
#32418=ORIENTED_EDGE ( 'NONE', *, *, #3831, .F. ) ;
#32421=CARTESIAN_POINT ( 'NONE',  ( -13.71283467540607504, -11.09584481999758054, 52.02966884056656482 ) ) ;
#32423=CARTESIAN_POINT ( 'NONE',  ( -21.93588290314558620, -13.54151500546508657, 52.02966884056656482 ) ) ;
#32445=ORIENTED_EDGE ( 'NONE', *, *, #21156, .T. ) ;
#32458=VERTEX_POINT ( 'NONE', #38322 ) ;
#32462=DIRECTION ( 'NONE',  ( 0.9687793358424817702, -0.2479245821708688791, 0.000000000000000000 ) ) ;
#32471=DIRECTION ( 'NONE',  ( -3.071710424422018668E-17, 6.404604876783312462E-16, 1.000000000000000000 ) ) ;
#32489=EDGE_CURVE ( 'NONE', #36372, #41560, #19805, .T. ) ;
#32491=DIRECTION ( 'NONE',  ( 0.9687793358424821033, -0.2479245821708679909, 0.000000000000000000 ) ) ;
#32498=CYLINDRICAL_SURFACE ( 'NONE', #12219, 4.686499999999997002 ) ;
#32501=LINE ( 'NONE', #47527, #30658 ) ;
#32503=ORIENTED_EDGE ( 'NONE', *, *, #7462, .T. ) ;
#32511=CYLINDRICAL_SURFACE ( 'NONE', #40013, 1.999999999999999112 ) ;
#32513=DIRECTION ( 'NONE',  ( -0.9180681052388980357, 0.3964226963016364014, 0.000000000000000000 ) ) ;
#32523=EDGE_CURVE ( 'NONE', #17454, #47981, #22975, .T. ) ;
#32527=CIRCLE ( 'NONE', #48231, 5.249999999999998224 ) ;
#32543=CYLINDRICAL_SURFACE ( 'NONE', #11951, 2.000000000000001776 ) ;
#32552=ORIENTED_EDGE ( 'NONE', *, *, #14895, .F. ) ;
#32570=CIRCLE ( 'NONE', #35676, 5.249999999999998224 ) ;
#32590=ORIENTED_EDGE ( 'NONE', *, *, #16333, .F. ) ;
#32594=DIRECTION ( 'NONE',  ( 0.9687793358424821033, -0.2479245821708679909, 0.000000000000000000 ) ) ;
#32600=VERTEX_POINT ( 'NONE', #31922 ) ;
#32603=AXIS2_PLACEMENT_3D ( 'NONE', #23908, #6875, #36639 ) ;
#32606=DIRECTION ( 'NONE',  ( 0.06357898915123476324, -0.9979768094191905359, 0.000000000000000000 ) ) ;
#32609=DIRECTION ( 'NONE',  ( 0.9687793358424821033, -0.2479245821708679909, 0.000000000000000000 ) ) ;
#32628=LINE ( 'NONE', #40991, #20089 ) ;
#32631=ORIENTED_EDGE ( 'NONE', *, *, #4860, .F. ) ;
#32633=CIRCLE ( 'NONE', #31863, 1.999999999999998446 ) ;
#32636=AXIS2_PLACEMENT_3D ( 'NONE', #19642, #7847, #22867 ) ;
#32654=CARTESIAN_POINT ( 'NONE',  ( -17.42409385541299471, -14.80920654474435771, 49.52966884056655772 ) ) ;
#32679=EDGE_LOOP ( 'NONE', ( #4192, #32503, #5249, #2521 ) ) ;
#32682=DIRECTION ( 'NONE',  ( -3.071710424422018668E-17, 6.404604876783312462E-16, 1.000000000000000000 ) ) ;
#32687=ORIENTED_EDGE ( 'NONE', *, *, #19282, .T. ) ;
#32707=CYLINDRICAL_SURFACE ( 'NONE', #21240, 2.000000000000003109 ) ;
#32709=DIRECTION ( 'NONE',  ( -3.071710424422018668E-17, 6.404604876783312462E-16, 1.000000000000000000 ) ) ;
#32710=EDGE_CURVE ( 'NONE', #39007, #19712, #15061, .T. ) ;
#32717=CARTESIAN_POINT ( 'NONE',  ( -21.00733138479494855, -11.77013360165371836, 52.02966884056656482 ) ) ;
#32718=EDGE_CURVE ( 'NONE', #45155, #17452, #42616, .T. ) ;
#32729=EDGE_CURVE ( 'NONE', #27273, #6531, #44967, .T. ) ;
#32741=DIRECTION ( 'NONE',  ( 0.9687793358424821033, -0.2479245821708677133, 0.000000000000000000 ) ) ;
#32751=CARTESIAN_POINT ( 'NONE',  ( -22.41759978862804914, -13.18828134753566417, 50.77966884056655772 ) ) ;
#32758=ORIENTED_EDGE ( 'NONE', *, *, #47124, .T. ) ;
#32764=ORIENTED_EDGE ( 'NONE', *, *, #33889, .F. ) ;
#32771=EDGE_CURVE ( 'NONE', #42667, #31657, #3389, .T. ) ;
#32803=CIRCLE ( 'NONE', #24176, 2.000000000000000888 ) ;
#32804=DIRECTION ( 'NONE',  ( -0.8447509909909771686, 0.5351595679979589404, 0.000000000000000000 ) ) ;
#32806=CARTESIAN_POINT ( 'NONE',  ( -14.46752719259218622, -19.14754880513559954, 50.77966884056656482 ) ) ;
#32811=VERTEX_POINT ( 'NONE', #34821 ) ;
#32819=DIRECTION ( 'NONE',  ( 3.071710424422018668E-17, -6.404604876783312462E-16, -1.000000000000000000 ) ) ;
#32828=FACE_OUTER_BOUND ( 'NONE', #27174, .T. ) ;
#32830=CARTESIAN_POINT ( 'NONE',  ( -22.67409364490373491, -14.81069326838761135, 50.77966884056655772 ) ) ;
#32840=CARTESIAN_POINT ( 'NONE',  ( -16.60428136649079534, -9.623610389719635450, 50.77966884056655772 ) ) ;
#32848=ORIENTED_EDGE ( 'NONE', *, *, #34088, .T. ) ;
#32856=EDGE_CURVE ( 'NONE', #32161, #34852, #28568, .T. ) ;
#32858=ORIENTED_EDGE ( 'NONE', *, *, #1361, .T. ) ;
#32861=CYLINDRICAL_SURFACE ( 'NONE', #19001, 5.249999999999998224 ) ;
#32862=CIRCLE ( 'NONE', #7736, 4.686499999999997890 ) ;
#32884=DIRECTION ( 'NONE',  ( -3.071710424422018668E-17, 6.404604876783312462E-16, 1.000000000000000000 ) ) ;
#32889=ORIENTED_EDGE ( 'NONE', *, *, #32729, .F. ) ;
#32900=EDGE_LOOP ( 'NONE', ( #12736, #33940, #34475, #31514 ) ) ;
#32907=CARTESIAN_POINT ( 'NONE',  ( -19.86520892150080897, -18.82374422416847537, 49.52966884056656482 ) ) ;
#32910=DIRECTION ( 'NONE',  ( 0.9687793358424821033, -0.2479245821708677133, 0.000000000000000000 ) ) ;
#32936=CARTESIAN_POINT ( 'NONE',  ( -13.86189509728330904, -11.74550036546145826, 52.02966884056656482 ) ) ;
#32941=DIRECTION ( 'NONE',  ( 0.2479245821708712938, 0.9687793358424811041, 0.000000000000000000 ) ) ;
#32942=CARTESIAN_POINT ( 'NONE',  ( -17.42409385541299471, -14.80920654474435594, 52.02966884056656482 ) ) ;
#32949=ORIENTED_EDGE ( 'NONE', *, *, #24665, .T. ) ;
#32951=AXIS2_PLACEMENT_3D ( 'NONE', #41335, #8113, #22891 ) ;
#32959=LINE ( 'NONE', #24876, #546 ) ;
#32960=AXIS2_PLACEMENT_3D ( 'NONE', #7441, #18490, #18741 ) ;
#32962=DIRECTION ( 'NONE',  ( -3.071710424422018668E-17, 6.404604876783312462E-16, 1.000000000000000000 ) ) ;
#32964=CARTESIAN_POINT ( 'NONE',  ( -17.42409385541299471, -14.80920654474434883, 62.02966884056656482 ) ) ;
#32974=EDGE_CURVE ( 'NONE', #36634, #36681, #38790, .T. ) ;
#32976=DIRECTION ( 'NONE',  ( 0.9687793358424821033, -0.2479245821708679909, 0.000000000000000000 ) ) ;
#32994=CARTESIAN_POINT ( 'NONE',  ( -17.42409385541299471, -14.80920654474435771, 49.52966884056655772 ) ) ;
#33014=CIRCLE ( 'NONE', #11822, 1.999999999999998890 ) ;
#33031=ORIENTED_EDGE ( 'NONE', *, *, #43826, .F. ) ;
#33032=CARTESIAN_POINT ( 'NONE',  ( -19.23707162763026801, -10.47461692831664060, 49.52966884056655772 ) ) ;
#33036=DIRECTION ( 'NONE',  ( -3.071710424422018668E-17, 6.404604876783312462E-16, 1.000000000000000000 ) ) ;
#33042=EDGE_CURVE ( 'NONE', #38839, #25922, #9711, .T. ) ;
#33046=CARTESIAN_POINT ( 'NONE',  ( -20.02395964528090033, -18.70843468947692045, 49.52966884056656482 ) ) ;
#33048=CARTESIAN_POINT ( 'NONE',  ( -17.42409385541299471, -14.80920654474435771, 49.52966884056655772 ) ) ;
#33050=ORIENTED_EDGE ( 'NONE', *, *, #13742, .T. ) ;
#33057=ORIENTED_EDGE ( 'NONE', *, *, #16262, .F. ) ;
#33066=ORIENTED_EDGE ( 'NONE', *, *, #34201, .F. ) ;
#33070=AXIS2_PLACEMENT_3D ( 'NONE', #9417, #9173, #5483 ) ;
#33089=ORIENTED_EDGE ( 'NONE', *, *, #35401, .F. ) ;
#33095=EDGE_CURVE ( 'NONE', #15953, #14238, #30370, .T. ) ;
#33101=AXIS2_PLACEMENT_3D ( 'NONE', #5840, #28491, #24796 ) ;
#33111=DIRECTION ( 'NONE',  ( -3.071710424422018668E-17, 6.404604876783312462E-16, 1.000000000000000000 ) ) ;
#33117=ORIENTED_EDGE ( 'NONE', *, *, #37482, .T. ) ;
#33123=ORIENTED_EDGE ( 'NONE', *, *, #186, .F. ) ;
#33144=AXIS2_PLACEMENT_3D ( 'NONE', #22195, #26134, #36459 ) ;
#33145=ORIENTED_EDGE ( 'NONE', *, *, #41187, .F. ) ;
#33176=ORIENTED_EDGE ( 'NONE', *, *, #45854, .F. ) ;
#33177=DIRECTION ( 'NONE',  ( -3.071710424422018668E-17, 6.404604876783312462E-16, 1.000000000000000000 ) ) ;
#33199=ORIENTED_EDGE ( 'NONE', *, *, #25916, .T. ) ;
#33207=VERTEX_POINT ( 'NONE', #12431 ) ;
#33211=LINE ( 'NONE', #48246, #9097 ) ;
#33227=ORIENTED_EDGE ( 'NONE', *, *, #11038, .F. ) ;
#33237=AXIS2_PLACEMENT_3D ( 'NONE', #44464, #3828, #29929 ) ;
#33239=DIRECTION ( 'NONE',  ( -3.071710424422018668E-17, 6.404604876783312462E-16, 1.000000000000000000 ) ) ;
#33267=DIRECTION ( 'NONE',  ( -3.071710424422018668E-17, 6.404604876783312462E-16, 1.000000000000000000 ) ) ;
#33279=AXIS2_PLACEMENT_3D ( 'NONE', #3715, #26868, #34468 ) ;
#33283=DIRECTION ( 'NONE',  ( -3.071710424422018668E-17, 6.404604876783312462E-16, 1.000000000000000000 ) ) ;
#33287=ORIENTED_EDGE ( 'NONE', *, *, #8323, .T. ) ;
#33302=CYLINDRICAL_SURFACE ( 'NONE', #43133, 5.249999999999998224 ) ;
#33308=CIRCLE ( 'NONE', #18388, 1.999999999999999556 ) ;
#33322=ORIENTED_EDGE ( 'NONE', *, *, #5015, .T. ) ;
#33352=VERTEX_POINT ( 'NONE', #24976 ) ;
#33358=DIRECTION ( 'NONE',  ( 3.071710424422018668E-17, -6.404604876783312462E-16, -1.000000000000000000 ) ) ;
#33361=VERTEX_POINT ( 'NONE', #39016 ) ;
#33371=EDGE_CURVE ( 'NONE', #44591, #33361, #17327, .T. ) ;
#33397=DIRECTION ( 'NONE',  ( 0.9687793358424821033, -0.2479245821708677133, 0.000000000000000000 ) ) ;
#33398=DIRECTION ( 'NONE',  ( -3.071710424422018668E-17, 6.404604876783312462E-16, 1.000000000000000000 ) ) ;
#33399=VERTEX_POINT ( 'NONE', #35071 ) ;
#33417=DIRECTION ( 'NONE',  ( 0.9687793358424819923, -0.2479245821708680464, 0.000000000000000000 ) ) ;
#33426=CARTESIAN_POINT ( 'NONE',  ( -17.42558057905623414, -9.559206755253621068, 49.52966884056655772 ) ) ;
#33431=CARTESIAN_POINT ( 'NONE',  ( -12.26581428767149795, -15.78626943986449405, 50.77966884056655772 ) ) ;
#33454=EDGE_LOOP ( 'NONE', ( #28053, #35775, #8871, #3561 ) ) ;
#33457=ADVANCED_FACE ( 'NONE', ( #20569 ), #42960, .T. ) ;
#33466=CARTESIAN_POINT ( 'NONE',  ( -17.42409385541299471, -14.80920654474435771, 49.52966884056655772 ) ) ;
#33471=AXIS2_PLACEMENT_3D ( 'NONE', #47975, #30252, #22866 ) ;
#33476=ORIENTED_EDGE ( 'NONE', *, *, #18378, .F. ) ;
#33492=ORIENTED_EDGE ( 'NONE', *, *, #13354, .F. ) ;
#33496=DIRECTION ( 'NONE',  ( 0.9687793358424819923, -0.2479245821708680464, 0.000000000000000000 ) ) ;
#33500=CARTESIAN_POINT ( 'NONE',  ( -19.80621920301059546, -19.48766556757794532, 50.77966884056656482 ) ) ;
#33507=ORIENTED_EDGE ( 'NONE', *, *, #24641, .F. ) ;
#33510=CARTESIAN_POINT ( 'NONE',  ( -19.38197731428664028, -19.06713733463150007, 49.52966884056656482 ) ) ;
#33516=ORIENTED_EDGE ( 'NONE', *, *, #9645, .F. ) ;
#33517=VECTOR ( 'NONE', #12766, 1000.000000000000000 ) ;
#33537=LINE ( 'NONE', #11401, #5538 ) ;
#33540=LINE ( 'NONE', #25943, #45870 ) ;
#33541=ADVANCED_FACE ( 'NONE', ( #32828 ), #25221, .T. ) ;
#33551=AXIS2_PLACEMENT_3D ( 'NONE', #4024, #804, #7971 ) ;
#33556=EDGE_CURVE ( 'NONE', #45860, #6783, #33540, .T. ) ;
#33559=ORIENTED_EDGE ( 'NONE', *, *, #12304, .F. ) ;
#33560=AXIS2_PLACEMENT_3D ( 'NONE', #48098, #14329, #29385 ) ;
#33566=ORIENTED_EDGE ( 'NONE', *, *, #47501, .T. ) ;
#33584=ADVANCED_FACE ( 'NONE', ( #21533 ), #6747, .T. ) ;
#33590=AXIS2_PLACEMENT_3D ( 'NONE', #23845, #45779, #31218 ) ;
#33595=ORIENTED_EDGE ( 'NONE', *, *, #19431, .T. ) ;
#33598=DIRECTION ( 'NONE',  ( -3.071710424422018668E-17, 6.404604876783312462E-16, 1.000000000000000000 ) ) ;
#33624=MECHANICAL_DESIGN_GEOMETRIC_PRESENTATION_REPRESENTATION('',(#43859),#5329);
#33632=CIRCLE ( 'NONE', #30549, 5.249999999999998224 ) ;
#33638=AXIS2_PLACEMENT_3D ( 'NONE', #11605, #38422, #37944 ) ;
#33646=ORIENTED_EDGE ( 'NONE', *, *, #30292, .T. ) ;
#33653=EDGE_CURVE ( 'NONE', #8529, #33207, #7383, .T. ) ;
#33657=CIRCLE ( 'NONE', #31297, 4.686500000000000554 ) ;
#33665=ORIENTED_EDGE ( 'NONE', *, *, #34366, .F. ) ;
#33672=CARTESIAN_POINT ( 'NONE',  ( -20.01098570613759975, -18.73139293731311028, 52.02966884056656482 ) ) ;
#33676=DIRECTION ( 'NONE',  ( 0.9687793358424821033, -0.2479245821708680464, 0.000000000000000000 ) ) ;
#33685=FACE_OUTER_BOUND ( 'NONE', #28459, .T. ) ;
#33688=CIRCLE ( 'NONE', #30569, 2.000000000000000888 ) ;
#33694=CIRCLE ( 'NONE', #32150, 4.686499999999998778 ) ;
#33698=DIRECTION ( 'NONE',  ( 1.000000000000000000, 0.000000000000000000, 0.000000000000000000 ) ) ;
#33701=FACE_OUTER_BOUND ( 'NONE', #41717, .T. ) ;
#33704=CARTESIAN_POINT ( 'NONE',  ( -17.42409385541299471, -14.80920654474435771, 49.52966884056655772 ) ) ;
#33715=ORIENTED_EDGE ( 'NONE', *, *, #41927, .T. ) ;
#33716=DIRECTION ( 'NONE',  ( -3.071710424422018668E-17, 6.404604876783312462E-16, 1.000000000000000000 ) ) ;
#33717=CIRCLE ( 'NONE', #43995, 4.686499999999997890 ) ;
#33723=VERTEX_POINT ( 'NONE', #39451 ) ;
#33726=AXIS2_PLACEMENT_3D ( 'NONE', #45113, #3728, #11359 ) ;
#33733=CARTESIAN_POINT ( 'NONE',  ( -19.90648311238531676, -10.83415612659009319, 49.52966884056655772 ) ) ;
#33736=VECTOR ( 'NONE', #25957, 1000.000000000000000 ) ;
#33737=EDGE_CURVE ( 'NONE', #44867, #10407, #2259, .T. ) ;
#33751=ORIENTED_EDGE ( 'NONE', *, *, #15323, .F. ) ;
#33755=DIRECTION ( 'NONE',  ( -3.071710424422018668E-17, 6.404604876783312462E-16, 1.000000000000000000 ) ) ;
#33762=CARTESIAN_POINT ( 'NONE',  ( -17.42409385541299471, -14.80920654474435771, 49.52966884056655772 ) ) ;
#33769=CARTESIAN_POINT ( 'NONE',  ( -15.80034074178659331, -19.80179363221599331, 52.02966884056656482 ) ) ;
#33770=AXIS2_PLACEMENT_3D ( 'NONE', #10918, #17563, #32594 ) ;
#33779=PRESENTATION_STYLE_ASSIGNMENT (( #45371 ) ) ;
#33783=EDGE_CURVE ( 'NONE', #22563, #2683, #29375, .T. ) ;
#33792=CARTESIAN_POINT ( 'NONE',  ( -16.44703096029287437, -9.650926977002853846, 49.52966884056655772 ) ) ;
#33795=FACE_OUTER_BOUND ( 'NONE', #37501, .T. ) ;
#33806=AXIS2_PLACEMENT_3D ( 'NONE', #7766, #14854, #11936 ) ;
#33808=ADVANCED_FACE ( 'NONE', ( #5731 ), #28375, .T. ) ;
#33820=FACE_OUTER_BOUND ( 'NONE', #31432, .T. ) ;
#33821=AXIS2_PLACEMENT_3D ( 'NONE', #2154, #43296, #9571 ) ;
#33822=DIRECTION ( 'NONE',  ( 0.9687793358424821033, -0.2479245821708679909, 0.000000000000000000 ) ) ;
#33825=VERTEX_POINT ( 'NONE', #36682 ) ;
#33837=ORIENTED_EDGE ( 'NONE', *, *, #35252, .T. ) ;
#33840=AXIS2_PLACEMENT_3D ( 'NONE', #31150, #5065, #11970 ) ;
#33842=CARTESIAN_POINT ( 'NONE',  ( -21.81933826130772047, -16.43558560955401404, 49.52966884056655772 ) ) ;
#33844=AXIS2_PLACEMENT_3D ( 'NONE', #23484, #42440, #34056 ) ;
#33848=EDGE_CURVE ( 'NONE', #39290, #42831, #8925, .T. ) ;
#33849=DIRECTION ( 'NONE',  ( -3.071710424422018668E-17, 6.404604876783312462E-16, 1.000000000000000000 ) ) ;
#33850=CIRCLE ( 'NONE', #22852, 1.999999999999999112 ) ;
#33857=DIRECTION ( 'NONE',  ( -3.071710424422018668E-17, 6.404604876783312462E-16, 1.000000000000000000 ) ) ;
#33870=ORIENTED_EDGE ( 'NONE', *, *, #3198, .T. ) ;
#33876=CARTESIAN_POINT ( 'NONE',  ( -22.02670722051955465, -15.75340237016373202, 49.52966884056655772 ) ) ;
#33877=AXIS2_PLACEMENT_3D ( 'NONE', #15155, #30215, #29960 ) ;
#33881=VERTEX_POINT ( 'NONE', #40408 ) ;
#33883=CARTESIAN_POINT ( 'NONE',  ( -17.42409385541299471, -14.80920654474435771, 49.52966884056655772 ) ) ;
#33888=CIRCLE ( 'NONE', #7945, 5.249999999999998224 ) ;
#33889=EDGE_CURVE ( 'NONE', #25029, #17399, #32527, .T. ) ;
#33891=DIRECTION ( 'NONE',  ( -3.071710424422018668E-17, 6.404604876783312462E-16, 1.000000000000000000 ) ) ;
#33897=CIRCLE ( 'NONE', #48025, 2.000000000000000888 ) ;
#33924=VECTOR ( 'NONE', #14800, 1000.000000000000000 ) ;
#33940=ORIENTED_EDGE ( 'NONE', *, *, #16188, .F. ) ;
#33948=AXIS2_PLACEMENT_3D ( 'NONE', #9328, #39357, #35645 ) ;
#33987=DIRECTION ( 'NONE',  ( 0.9687793358424821033, -0.2479245821708680464, 0.000000000000000000 ) ) ;
#33990=DIRECTION ( 'NONE',  ( 3.071710424422018668E-17, -6.404604876783312462E-16, -1.000000000000000000 ) ) ;
#34000=EDGE_CURVE ( 'NONE', #38039, #19164, #30966, .T. ) ;
#34011=DIRECTION ( 'NONE',  ( -3.071710424422018668E-17, 6.404604876783312462E-16, 1.000000000000000000 ) ) ;
#34016=FACE_OUTER_BOUND ( 'NONE', #19939, .T. ) ;
#34026=ORIENTED_EDGE ( 'NONE', *, *, #10234, .F. ) ;
#34037=EDGE_CURVE ( 'NONE', #47981, #31013, #19144, .T. ) ;
#34038=CYLINDRICAL_SURFACE ( 'NONE', #4726, 4.686499999999997002 ) ;
#34040=ORIENTED_EDGE ( 'NONE', *, *, #28138, .T. ) ;
#34056=DIRECTION ( 'NONE',  ( 0.9687793358424822143, -0.2479245821708672415, 0.000000000000000000 ) ) ;
#34070=EDGE_CURVE ( 'NONE', #20521, #15515, #3421, .T. ) ;
#34085=DIRECTION ( 'NONE',  ( 0.9687793358424821033, -0.2479245821708677133, 0.000000000000000000 ) ) ;
#34088=EDGE_CURVE ( 'NONE', #3266, #5301, #34881, .T. ) ;
#34094=VERTEX_POINT ( 'NONE', #30076 ) ;
#34098=DIRECTION ( 'NONE',  ( 0.9687793358424821033, -0.2479245821708677133, 0.000000000000000000 ) ) ;
#34099=FACE_OUTER_BOUND ( 'NONE', #34297, .T. ) ;
#34116=DIRECTION ( 'NONE',  ( 0.9687793358424821033, -0.2479245821708677133, 0.000000000000000000 ) ) ;
#34121=ORIENTED_EDGE ( 'NONE', *, *, #5266, .T. ) ;
#34130=ORIENTED_EDGE ( 'NONE', *, *, #36754, .F. ) ;
#34166=AXIS2_PLACEMENT_3D ( 'NONE', #30473, #45254, #26038 ) ;
#34170=CARTESIAN_POINT ( 'NONE',  ( -22.11774618123879677, -15.02177039319221308, 49.52966884056655772 ) ) ;
#34187=CARTESIAN_POINT ( 'NONE',  ( -14.41069671968389265, -11.21995593321280182, 52.02966884056656482 ) ) ;
#34201=EDGE_CURVE ( 'NONE', #16040, #11402, #45908, .T. ) ;
#34208=CARTESIAN_POINT ( 'NONE',  ( -17.42409385541299471, -14.80920654474435771, 49.52966884056655772 ) ) ;
#34230=CARTESIAN_POINT ( 'NONE',  ( -17.21153000696512336, -19.50285887057015444, 49.52966884056656482 ) ) ;
#34257=CARTESIAN_POINT ( 'NONE',  ( -12.87649578556737318, -13.67667219862660843, 52.02966884056656482 ) ) ;
#34258=EDGE_CURVE ( 'NONE', #14388, #467, #45102, .T. ) ;
#34263=EDGE_LOOP ( 'NONE', ( #28966, #38150, #7104, #6319 ) ) ;
#34293=CARTESIAN_POINT ( 'NONE',  ( -22.07864594086649390, -14.26292169798353981, 49.52966884056655772 ) ) ;
#34297=EDGE_LOOP ( 'NONE', ( #29224, #3649, #34861, #46824 ) ) ;
#34325=FACE_OUTER_BOUND ( 'NONE', #23255, .T. ) ;
#34329=DIRECTION ( 'NONE',  ( -3.071710424422018668E-17, 6.404604876783312462E-16, 1.000000000000000000 ) ) ;
#34342=EDGE_CURVE ( 'NONE', #29174, #19773, #27222, .T. ) ;
#34363=EDGE_CURVE ( 'NONE', #25136, #25847, #22302, .T. ) ;
#34365=ORIENTED_EDGE ( 'NONE', *, *, #3073, .T. ) ;
#34366=EDGE_CURVE ( 'NONE', #1168, #25404, #38538, .T. ) ;
#34370=EDGE_CURVE ( 'NONE', #25725, #15450, #2681, .T. ) ;
#34383=AXIS2_PLACEMENT_3D ( 'NONE', #37288, #3573, #7532 ) ;
#34384=DIRECTION ( 'NONE',  ( 3.071710424422018668E-17, -6.404604876783312462E-16, -1.000000000000000000 ) ) ;
#34392=EDGE_CURVE ( 'NONE', #31657, #27248, #27706, .T. ) ;
#34395=ADVANCED_FACE ( 'NONE', ( #37809 ), #19340, .T. ) ;
#34398=DIRECTION ( 'NONE',  ( 0.9687793358424817702, -0.2479245821708684905, 0.000000000000000000 ) ) ;
#34400=VERTEX_POINT ( 'NONE', #30689 ) ;
#34403=CIRCLE ( 'NONE', #29714, 5.249999999999998224 ) ;
#34420=EDGE_CURVE ( 'NONE', #10683, #19164, #15637, .T. ) ;
#34423=VERTEX_POINT ( 'NONE', #43222 ) ;
#34425=CARTESIAN_POINT ( 'NONE',  ( -19.80886856394220175, -10.13209743873031954, 52.02966884056656482 ) ) ;
#34426=CARTESIAN_POINT ( 'NONE',  ( -22.09287085128708839, -15.21639644245407297, 49.52966884056655772 ) ) ;
#34431=LINE ( 'NONE', #30531, #18889 ) ;
#34432=DIRECTION ( 'NONE',  ( -3.071710424422018668E-17, 6.404604876783312462E-16, 1.000000000000000000 ) ) ;
#34437=VECTOR ( 'NONE', #29454, 1000.000000000000000 ) ;
#34441=VECTOR ( 'NONE', #45661, 1000.000000000000000 ) ;
#34450=AXIS2_PLACEMENT_3D ( 'NONE', #10149, #43897, #10630 ) ;
#34453=ORIENTED_EDGE ( 'NONE', *, *, #23381, .T. ) ;
#34460=ORIENTED_EDGE ( 'NONE', *, *, #31030, .T. ) ;
#34468=DIRECTION ( 'NONE',  ( -0.06357898915124166050, 0.9979768094191900918, 0.000000000000000000 ) ) ;
#34475=ORIENTED_EDGE ( 'NONE', *, *, #45709, .T. ) ;
#34477=CIRCLE ( 'NONE', #19557, 2.000000000000000888 ) ;
#34478=CIRCLE ( 'NONE', #15636, 5.249999999999998224 ) ;
#34482=DIRECTION ( 'NONE',  ( 0.9687793358424821033, -0.2479245821708677133, 0.000000000000000000 ) ) ;
#34492=AXIS2_PLACEMENT_3D ( 'NONE', #24262, #28673, #24514 ) ;
#34514=CIRCLE ( 'NONE', #41593, 1.999999999999999778 ) ;
#34516=CIRCLE ( 'NONE', #2297, 1.999999999999999112 ) ;
#34527=ORIENTED_EDGE ( 'NONE', *, *, #46240, .T. ) ;
#34528=DIRECTION ( 'NONE',  ( -3.071710424422018668E-17, 6.404604876783312462E-16, 1.000000000000000000 ) ) ;
#34531=ORIENTED_EDGE ( 'NONE', *, *, #3603, .T. ) ;
#34539=DIRECTION ( 'NONE',  ( 0.7506333037770493988, -0.6607190350373991494, 0.000000000000000000 ) ) ;
#34541=FACE_OUTER_BOUND ( 'NONE', #19600, .T. ) ;
#34544=ORIENTED_EDGE ( 'NONE', *, *, #40997, .F. ) ;
#34545=AXIS2_PLACEMENT_3D ( 'NONE', #45057, #15449, #7868 ) ;
#34563=EDGE_CURVE ( 'NONE', #34852, #12698, #318, .T. ) ;
#34576=CIRCLE ( 'NONE', #17246, 1.999999999999999112 ) ;
#34578=CYLINDRICAL_SURFACE ( 'NONE', #17811, 1.999999999999999112 ) ;
#34591=AXIS2_PLACEMENT_3D ( 'NONE', #44944, #595, #22776 ) ;
#34615=ORIENTED_EDGE ( 'NONE', *, *, #9148, .F. ) ;
#34617=CIRCLE ( 'NONE', #14944, 2.000000000000002665 ) ;
#34648=AXIS2_PLACEMENT_3D ( 'NONE', #12778, #45802, #23636 ) ;
#34650=CYLINDRICAL_SURFACE ( 'NONE', #43655, 2.000000000000001332 ) ;
#34663=PRODUCT_DEFINITION_SHAPE ( 'NONE', 'NONE',  #37283 ) ;
#34668=DIRECTION ( 'NONE',  ( -3.071710424422018668E-17, 6.404604876783312462E-16, 1.000000000000000000 ) ) ;
#34673=CARTESIAN_POINT ( 'NONE',  ( -17.42409385541299471, -14.80920654474435594, 52.02966884056656482 ) ) ;
#34674=ORIENTED_EDGE ( 'NONE', *, *, #13139, .F. ) ;
#34675=EDGE_CURVE ( 'NONE', #22785, #37281, #19997, .T. ) ;
#34688=DIRECTION ( 'NONE',  ( -3.071710424422018668E-17, 6.404604876783312462E-16, 1.000000000000000000 ) ) ;
#34695=AXIS2_PLACEMENT_3D ( 'NONE', #45235, #48659, #25766 ) ;
#34712=EDGE_CURVE ( 'NONE', #2810, #33723, #31099, .T. ) ;
#34713=EDGE_CURVE ( 'NONE', #36372, #34714, #44352, .T. ) ;
#34714=VERTEX_POINT ( 'NONE', #23238 ) ;
#34725=DIRECTION ( 'NONE',  ( 0.9687793358424821033, -0.2479245821708677133, 0.000000000000000000 ) ) ;
#34730=DIRECTION ( 'NONE',  ( -3.071710424422018668E-17, 6.404604876783312462E-16, 1.000000000000000000 ) ) ;
#34742=EDGE_LOOP ( 'NONE', ( #24209, #1359, #38057, #27615 ) ) ;
#34744=AXIS2_PLACEMENT_3D ( 'NONE', #21991, #18029, #21273 ) ;
#34745=CYLINDRICAL_SURFACE ( 'NONE', #1947, 2.000000000000003553 ) ;
#34751=EDGE_CURVE ( 'NONE', #44591, #33352, #32570, .T. ) ;
#34764=VECTOR ( 'NONE', #1993, 1000.000000000000000 ) ;
#34773=ORIENTED_EDGE ( 'NONE', *, *, #42205, .T. ) ;
#34800=FACE_OUTER_BOUND ( 'NONE', #35646, .T. ) ;
#34810=FACE_OUTER_BOUND ( 'NONE', #37439, .T. ) ;
#34821=CARTESIAN_POINT ( 'NONE',  ( -15.13017050835524913, -18.89591645955643529, 52.02966884056656482 ) ) ;
#34832=CARTESIAN_POINT ( 'NONE',  ( -13.88631413956031579, -11.73554473314222157, 49.52966884056655772 ) ) ;
#34838=EDGE_CURVE ( 'NONE', #23394, #27273, #7410, .T. ) ;
#34841=ORIENTED_EDGE ( 'NONE', *, *, #46041, .T. ) ;
#34842=LINE ( 'NONE', #31649, #31498 ) ;
#34847=LINE ( 'NONE', #42739, #39195 ) ;
#34852=VERTEX_POINT ( 'NONE', #2267 ) ;
#34853=DIRECTION ( 'NONE',  ( -3.071710424422018668E-17, 6.404604876783312462E-16, 1.000000000000000000 ) ) ;
#34857=ORIENTED_EDGE ( 'NONE', *, *, #4934, .F. ) ;
#34858=DIRECTION ( 'NONE',  ( -3.071710424422018668E-17, 6.404604876783312462E-16, 1.000000000000000000 ) ) ;
#34861=ORIENTED_EDGE ( 'NONE', *, *, #47788, .T. ) ;
#34868=ORIENTED_EDGE ( 'NONE', *, *, #42768, .T. ) ;
#34872=CARTESIAN_POINT ( 'NONE',  ( -21.81933826130772047, -16.43558560955401404, 49.52966884056655772 ) ) ;
#34877=ORIENTED_EDGE ( 'NONE', *, *, #5491, .T. ) ;
#34879=EDGE_CURVE ( 'NONE', #13129, #33825, #33308, .T. ) ;
#34881=CIRCLE ( 'NONE', #6561, 5.249999999999998224 ) ;
#34902=ORIENTED_EDGE ( 'NONE', *, *, #36858, .T. ) ;
#34905=LINE ( 'NONE', #8578, #17883 ) ;
#34910=CARTESIAN_POINT ( 'NONE',  ( -22.36602013069261119, -13.03724021049843351, 49.52966884056655772 ) ) ;
#34915=AXIS2_PLACEMENT_3D ( 'NONE', #48483, #15468, #44564 ) ;
#34928=ORIENTED_EDGE ( 'NONE', *, *, #23324, .T. ) ;
#34932=CARTESIAN_POINT ( 'NONE',  ( -14.90085577400961014, -10.20532018813695707, 52.02966884056656482 ) ) ;
#34937=CYLINDRICAL_SURFACE ( 'NONE', #2085, 1.999999999999999556 ) ;
#34946=EDGE_CURVE ( 'NONE', #1752, #29174, #25468, .T. ) ;
#34953=EDGE_CURVE ( 'NONE', #29256, #23803, #45933, .T. ) ;
#34957=DIRECTION ( 'NONE',  ( 0.6607190350373965959, 0.7506333037770516192, 0.000000000000000000 ) ) ;
#34962=CARTESIAN_POINT ( 'NONE',  ( -19.80886856394220175, -10.13209743873032309, 49.52966884056655772 ) ) ;
#34965=LINE ( 'NONE', #2206, #6628 ) ;
#34966=CARTESIAN_POINT ( 'NONE',  ( -18.69178539469224987, -19.32099559247695097, 52.02966884056656482 ) ) ;
#34984=ORIENTED_EDGE ( 'NONE', *, *, #24493, .F. ) ;
#34987=AXIS2_PLACEMENT_3D ( 'NONE', #15149, #3859, #11240 ) ;
#34988=CARTESIAN_POINT ( 'NONE',  ( -17.42409385541299471, -14.80920654474434883, 62.02966884056656482 ) ) ;
#35005=DIRECTION ( 'NONE',  ( -0.9956360040033419567, 0.09332174201255245827, 0.000000000000000000 ) ) ;
#35006=ORIENTED_EDGE ( 'NONE', *, *, #36287, .F. ) ;
#35010=ORIENTED_EDGE ( 'NONE', *, *, #4048, .T. ) ;
#35017=AXIS2_PLACEMENT_3D ( 'NONE', #16860, #27476, #8783 ) ;
#35022=CARTESIAN_POINT ( 'NONE',  ( -14.94170459844064780, -18.78425696289860269, 49.52966884056656482 ) ) ;
#35026=DIRECTION ( 'NONE',  ( 0.5097212845717493668, -0.8603395911234852367, 0.000000000000000000 ) ) ;
#35029=LINE ( 'NONE', #42445, #43230 ) ;
#35031=ORIENTED_EDGE ( 'NONE', *, *, #11322, .T. ) ;
#35048=CYLINDRICAL_SURFACE ( 'NONE', #40528, 4.686499999999997002 ) ;
#35071=CARTESIAN_POINT ( 'NONE',  ( -16.75933984047804515, -20.01695097968237036, 52.02966884056656482 ) ) ;
#35076=ORIENTED_EDGE ( 'NONE', *, *, #29806, .T. ) ;
#35078=FACE_OUTER_BOUND ( 'NONE', #32416, .T. ) ;
#35080=VECTOR ( 'NONE', #9549, 1000.000000000000000 ) ;
#35081=AXIS2_PLACEMENT_3D ( 'NONE', #8250, #4535, #27681 ) ;
#35082=DIRECTION ( 'NONE',  ( -3.071710424422018668E-17, 6.404604876783312462E-16, 1.000000000000000000 ) ) ;
#35087=ORIENTED_EDGE ( 'NONE', *, *, #43826, .T. ) ;
#35109=DIRECTION ( 'NONE',  ( 0.9687793358424819923, -0.2479245821708678243, 0.000000000000000000 ) ) ;
#35137=EDGE_LOOP ( 'NONE', ( #40983, #18446, #11342, #38903 ) ) ;
#35139=CARTESIAN_POINT ( 'NONE',  ( -12.74563483257940177, -17.19133189234193893, 49.52966884056655772 ) ) ;
#35142=DIRECTION ( 'NONE',  ( -3.071710424422018668E-17, 6.404604876783312462E-16, 1.000000000000000000 ) ) ;
#35161=AXIS2_PLACEMENT_3D ( 'NONE', #48641, #41757, #22304 ) ;
#35189=VECTOR ( 'NONE', #45393, 1000.000000000000000 ) ;
#35196=DIRECTION ( 'NONE',  ( -0.9687793358424819923, 0.2479245821708680464, 0.000000000000000000 ) ) ;
#35198=EDGE_LOOP ( 'NONE', ( #19630, #27447, #13634, #15367 ) ) ;
#35210=CARTESIAN_POINT ( 'NONE',  ( -17.42409385541299471, -14.80920654474434883, 62.02966884056656482 ) ) ;
#35223=DIRECTION ( 'NONE',  ( 0.9687793358424821033, -0.2479245821708677133, 0.000000000000000000 ) ) ;
#35224=VECTOR ( 'NONE', #2447, 1000.000000000000000 ) ;
#35231=EDGE_CURVE ( 'NONE', #21060, #23374, #34965, .T. ) ;
#35232=CIRCLE ( 'NONE', #45376, 4.686500000000000554 ) ;
#35247=ORIENTED_EDGE ( 'NONE', *, *, #46154, .F. ) ;
#35250=AXIS2_PLACEMENT_3D ( 'NONE', #7813, #18871, #413 ) ;
#35252=EDGE_CURVE ( 'NONE', #34423, #25804, #27857, .T. ) ;
#35262=EDGE_CURVE ( 'NONE', #2300, #20349, #1966, .T. ) ;
#35275=DIRECTION ( 'NONE',  ( 0.9687793358424819923, -0.2479245821708680464, 0.000000000000000000 ) ) ;
#35277=DIRECTION ( 'NONE',  ( -3.071710424422018668E-17, 6.404604876783312462E-16, 1.000000000000000000 ) ) ;
#35282=VERTEX_POINT ( 'NONE', #39148 ) ;
#35283=ADVANCED_FACE ( 'NONE', ( #31279 ), #46312, .T. ) ;
#35288=CIRCLE ( 'NONE', #22730, 2.000000000000001332 ) ;
#35291=AXIS2_PLACEMENT_3D ( 'NONE', #19253, #45363, #19011 ) ;
#35292=FACE_OUTER_BOUND ( 'NONE', #3041, .T. ) ;
#35295=CIRCLE ( 'NONE', #21930, 5.249999999999998224 ) ;
#35296=AXIS2_PLACEMENT_3D ( 'NONE', #38226, #30876, #34539 ) ;
#35302=ADVANCED_FACE ( 'NONE', ( #13270 ), #12568, .T. ) ;
#35320=EDGE_CURVE ( 'NONE', #13083, #70, #48305, .T. ) ;
#35324=CIRCLE ( 'NONE', #14836, 4.686499999999998778 ) ;
#35331=AXIS2_PLACEMENT_3D ( 'NONE', #47028, #28329, #6396 ) ;
#35336=DIRECTION ( 'NONE',  ( 0.9180681052388952601, -0.3964226963016431737, 0.000000000000000000 ) ) ;
#35337=CARTESIAN_POINT ( 'NONE',  ( -12.85169559483840374, -15.89028456787280952, 49.52966884056655772 ) ) ;
#35340=VECTOR ( 'NONE', #2930, 1000.000000000000000 ) ;
#35342=DIRECTION ( 'NONE',  ( -3.071710424422018668E-17, 6.404604876783312462E-16, 1.000000000000000000 ) ) ;
#35351=ORIENTED_EDGE ( 'NONE', *, *, #5463, .T. ) ;
#35365=VECTOR ( 'NONE', #23313, 1000.000000000000000 ) ;
#35373=ADVANCED_FACE ( 'NONE', ( #25826 ), #2456, .T. ) ;
#35386=ORIENTED_EDGE ( 'NONE', *, *, #27926, .F. ) ;
#35401=EDGE_CURVE ( 'NONE', #16630, #20066, #21652, .T. ) ;
#35407=VECTOR ( 'NONE', #40272, 1000.000000000000000 ) ;
#35409=CARTESIAN_POINT ( 'NONE',  ( -14.46752719259218622, -19.14754880513559598, 52.02966884056656482 ) ) ;
#35414=ORIENTED_EDGE ( 'NONE', *, *, #48263, .F. ) ;
#35419=FACE_OUTER_BOUND ( 'NONE', #21545, .T. ) ;
#35420=VERTEX_POINT ( 'NONE', #21175 ) ;
#35443=AXIS2_PLACEMENT_3D ( 'NONE', #8438, #34528, #4265 ) ;
#35446=ORIENTED_EDGE ( 'NONE', *, *, #14686, .F. ) ;
#35450=VERTEX_POINT ( 'NONE', #48228 ) ;
#35461=DIRECTION ( 'NONE',  ( 0.9687793358424821033, -0.2479245821708679909, 0.000000000000000000 ) ) ;
#35487=CIRCLE ( 'NONE', #4824, 1.999999999999999334 ) ;
#35492=DIRECTION ( 'NONE',  ( -3.071710424422018668E-17, 6.404604876783312462E-16, 1.000000000000000000 ) ) ;
#35500=DIRECTION ( 'NONE',  ( 3.071710424422018668E-17, -6.404604876783312462E-16, -1.000000000000000000 ) ) ;
#35503=CARTESIAN_POINT ( 'NONE',  ( -17.42409385541299471, -14.80920654474435594, 52.02966884056656482 ) ) ;
#35507=AXIS2_PLACEMENT_3D ( 'NONE', #29011, #43323, #21862 ) ;
#35526=DIRECTION ( 'NONE',  ( -3.071710424422018668E-17, 6.404604876783312462E-16, 1.000000000000000000 ) ) ;
#35535=DIRECTION ( 'NONE',  ( -3.071710424422018668E-17, 6.404604876783312462E-16, 1.000000000000000000 ) ) ;
#35540=DIRECTION ( 'NONE',  ( -3.071710424422018668E-17, 6.404604876783312462E-16, 1.000000000000000000 ) ) ;
#35567=LINE ( 'NONE', #31882, #31335 ) ;
#35578=DIRECTION ( 'NONE',  ( 0.9757441136919974278, 0.2189141945955501434, 0.000000000000000000 ) ) ;
#35579=EDGE_CURVE ( 'NONE', #1628, #18527, #9802, .T. ) ;
#35580=CARTESIAN_POINT ( 'NONE',  ( -19.36557164464469594, -19.08778335711045671, 52.02966884056656482 ) ) ;
#35586=ORIENTED_EDGE ( 'NONE', *, *, #32771, .T. ) ;
#35587=LINE ( 'NONE', #9752, #38307 ) ;
#35606=ORIENTED_EDGE ( 'NONE', *, *, #14894, .F. ) ;
#35637=VERTEX_POINT ( 'NONE', #39581 ) ;
#35642=CARTESIAN_POINT ( 'NONE',  ( -17.23552066371262725, -19.49191114800217051, 52.02966884056656482 ) ) ;
#35645=DIRECTION ( 'NONE',  ( 0.9687793358424821033, -0.2479245821708680464, 0.000000000000000000 ) ) ;
#35646=EDGE_LOOP ( 'NONE', ( #30845, #42752, #45451, #3012 ) ) ;
#35652=VECTOR ( 'NONE', #20977, 1000.000000000000000 ) ;
#35655=CARTESIAN_POINT ( 'NONE',  ( -21.97169192525862869, -15.94174089086206791, 52.02966884056656482 ) ) ;
#35666=EDGE_CURVE ( 'NONE', #42513, #42051, #36514, .T. ) ;
#35667=CARTESIAN_POINT ( 'NONE',  ( -17.42409385541299471, -14.80920654474435594, 52.02966884056656482 ) ) ;
#35671=ORIENTED_EDGE ( 'NONE', *, *, #26130, .F. ) ;
#35675=LINE ( 'NONE', #42620, #35224 ) ;
#35676=AXIS2_PLACEMENT_3D ( 'NONE', #23481, #822, #15572 ) ;
#35683=DIRECTION ( 'NONE',  ( -0.5351595679979683773, -0.8447509909909712844, 0.000000000000000000 ) ) ;
#35685=FACE_OUTER_BOUND ( 'NONE', #11347, .T. ) ;
#35687=ORIENTED_EDGE ( 'NONE', *, *, #18647, .T. ) ;
#35697=FACE_OUTER_BOUND ( 'NONE', #37882, .T. ) ;
#35700=EDGE_CURVE ( 'NONE', #40656, #45424, #45971, .T. ) ;
#35707=ORIENTED_EDGE ( 'NONE', *, *, #45664, .F. ) ;
#35713=AXIS2_PLACEMENT_3D ( 'NONE', #42857, #20451, #35683 ) ;
#35721=EDGE_CURVE ( 'NONE', #22869, #42245, #38079, .T. ) ;
#35741=ORIENTED_EDGE ( 'NONE', *, *, #12761, .T. ) ;
#35747=DIRECTION ( 'NONE',  ( 3.071710424422018668E-17, -6.404604876783312462E-16, -1.000000000000000000 ) ) ;
#35749=CIRCLE ( 'NONE', #34987, 5.249999999999998224 ) ;
#35750=VERTEX_POINT ( 'NONE', #36832 ) ;
#35751=CARTESIAN_POINT ( 'NONE',  ( -13.17762867948185601, -11.72213130924974678, 50.77966884056655772 ) ) ;
#35766=EDGE_CURVE ( 'NONE', #1460, #31052, #19207, .T. ) ;
#35775=ORIENTED_EDGE ( 'NONE', *, *, #29177, .T. ) ;
#35776=VERTEX_POINT ( 'NONE', #21370 ) ;
#35783=AXIS2_PLACEMENT_3D ( 'NONE', #536, #15528, #26895 ) ;
#35785=DIRECTION ( 'NONE',  ( -3.071710424422018668E-17, 6.404604876783312462E-16, 1.000000000000000000 ) ) ;
#35801=CARTESIAN_POINT ( 'NONE',  ( -20.51116909090755769, -10.56274136881318526, 49.52966884056655772 ) ) ;
#35808=FACE_OUTER_BOUND ( 'NONE', #35137, .T. ) ;
#35814=CARTESIAN_POINT ( 'NONE',  ( -13.60167271156757707, -11.21037387301822008, 52.02966884056656482 ) ) ;
#35820=VERTEX_POINT ( 'NONE', #42198 ) ;
#35823=DIRECTION ( 'NONE',  ( 0.2189141945955467017, -0.9757441136919982050, 0.000000000000000000 ) ) ;
#35844=CIRCLE ( 'NONE', #35081, 2.000000000000003109 ) ;
#35847=DIRECTION ( 'NONE',  ( 0.9687793358424817702, -0.2479245821708684350, 0.000000000000000000 ) ) ;
#35854=CYLINDRICAL_SURFACE ( 'NONE', #18079, 1.999999999999999112 ) ;
#35861=FACE_OUTER_BOUND ( 'NONE', #45247, .T. ) ;
#35876=CARTESIAN_POINT ( 'NONE',  ( -20.46316679850361808, -18.39244407412632043, 49.52966884056656482 ) ) ;
#35884=VECTOR ( 'NONE', #7897, 1000.000000000000000 ) ;
#35885=VECTOR ( 'NONE', #15920, 1000.000000000000000 ) ;
#35899=CARTESIAN_POINT ( 'NONE',  ( -17.42409385541299471, -14.80920654474435594, 52.02966884056656482 ) ) ;
#35901=ORIENTED_EDGE ( 'NONE', *, *, #15990, .T. ) ;
#35913=CARTESIAN_POINT ( 'NONE',  ( -17.63665770386090514, -10.11555421891856099, 49.52966884056655772 ) ) ;
#35934=CYLINDRICAL_SURFACE ( 'NONE', #31093, 1.999999999999999556 ) ;
#35950=DIRECTION ( 'NONE',  ( -3.071710424422018668E-17, 6.404604876783312462E-16, 1.000000000000000000 ) ) ;
#35952=CIRCLE ( 'NONE', #28092, 4.686499999999998778 ) ;
#35954=AXIS2_PLACEMENT_3D ( 'NONE', #13502, #36391, #21158 ) ;
#35958=ADVANCED_FACE ( 'NONE', ( #9919 ), #11129, .T. ) ;
#35963=CARTESIAN_POINT ( 'NONE',  ( -18.34288178775629419, -10.21365315202000268, 52.02966884056656482 ) ) ;
#35987=AXIS2_PLACEMENT_3D ( 'NONE', #48062, #22209, #36701 ) ;
#35998=ORIENTED_EDGE ( 'NONE', *, *, #29252, .F. ) ;
#35999=LINE ( 'NONE', #47587, #31565 ) ;
#36036=DIRECTION ( 'NONE',  ( -3.071710424422018668E-17, 6.404604876783312462E-16, 1.000000000000000000 ) ) ;
#36041=DIRECTION ( 'NONE',  ( -3.071710424422018668E-17, 6.404604876783312462E-16, 1.000000000000000000 ) ) ;
#36045=DIRECTION ( 'NONE',  ( 0.9687793358424821033, -0.2479245821708677133, 0.000000000000000000 ) ) ;
#36049=DIRECTION ( 'NONE',  ( 0.9687793358424822143, -0.2479245821708672415, 0.000000000000000000 ) ) ;
#36062=AXIS2_PLACEMENT_3D ( 'NONE', #2578, #17580, #21048 ) ;
#36083=EDGE_CURVE ( 'NONE', #11147, #28351, #37197, .T. ) ;
#36084=ORIENTED_EDGE ( 'NONE', *, *, #4299, .F. ) ;
#36085=CARTESIAN_POINT ( 'NONE',  ( -17.42409385541299471, -14.80920654474434883, 62.02966884056656482 ) ) ;
#36088=ORIENTED_EDGE ( 'NONE', *, *, #28900, .F. ) ;
#36121=CARTESIAN_POINT ( 'NONE',  ( -15.66732230932660741, -10.46443543628982553, 49.52966884056655772 ) ) ;
#36132=ORIENTED_EDGE ( 'NONE', *, *, #27670, .T. ) ;
#36133=ORIENTED_EDGE ( 'NONE', *, *, #37210, .T. ) ;
#36145=ADVANCED_FACE ( 'NONE', ( #30346 ), #34745, .T. ) ;
#36155=VECTOR ( 'NONE', #25480, 1000.000000000000000 ) ;
#36169=DIRECTION ( 'NONE',  ( -0.7506333037770538397, 0.6607190350373941534, 0.000000000000000000 ) ) ;
#36200=EDGE_CURVE ( 'NONE', #19733, #32100, #46004, .T. ) ;
#36204=CIRCLE ( 'NONE', #7908, 5.249999999999998224 ) ;
#36222=ADVANCED_FACE ( 'NONE', ( #5200 ), #39160, .T. ) ;
#36225=VECTOR ( 'NONE', #36403, 1000.000000000000000 ) ;
#36230=CIRCLE ( 'NONE', #858, 2.000000000000002665 ) ;
#36231=CARTESIAN_POINT ( 'NONE',  ( -18.36828968083242231, -10.20659317963781021, 49.52966884056655772 ) ) ;
#36235=EDGE_CURVE ( 'NONE', #20160, #31757, #5126, .T. ) ;
#36239=VERTEX_POINT ( 'NONE', #39649 ) ;
#36255=AXIS2_PLACEMENT_3D ( 'NONE', #17622, #44010, #10265 ) ;
#36269=CIRCLE ( 'NONE', #127, 2.000000000000000888 ) ;
#36279=ORIENTED_EDGE ( 'NONE', *, *, #6819, .F. ) ;
#36287=EDGE_CURVE ( 'NONE', #33881, #22937, #47580, .T. ) ;
#36296=CARTESIAN_POINT ( 'NONE',  ( -17.42409385541299471, -14.80920654474435771, 49.52966884056655772 ) ) ;
#36309=AXIS2_PLACEMENT_3D ( 'NONE', #44411, #25930, #48320 ) ;
#36310=DIRECTION ( 'NONE',  ( 0.5097212845717490337, -0.8603395911234853477, 0.000000000000000000 ) ) ;
#36314=VERTEX_POINT ( 'NONE', #8562 ) ;
#36322=ADVANCED_FACE ( 'NONE', ( #38329 ), #34650, .T. ) ;
#36327=CIRCLE ( 'NONE', #23778, 2.000000000000000000 ) ;
#36329=EDGE_CURVE ( 'NONE', #16401, #36429, #11404, .T. ) ;
#36331=DIRECTION ( 'NONE',  ( -3.071710424422018668E-17, 6.404604876783312462E-16, 1.000000000000000000 ) ) ;
#36333=VERTEX_POINT ( 'NONE', #23586 ) ;
#36342=ORIENTED_EDGE ( 'NONE', *, *, #44993, .T. ) ;
#36346=FACE_OUTER_BOUND ( 'NONE', #14914, .T. ) ;
#36354=CARTESIAN_POINT ( 'NONE',  ( -17.42409385541299471, -14.80920654474435594, 52.02966884056656482 ) ) ;
#36361=VERTEX_POINT ( 'NONE', #4151 ) ;
#36371=ORIENTED_EDGE ( 'NONE', *, *, #11322, .F. ) ;
#36372=VERTEX_POINT ( 'NONE', #4376 ) ;
#36375=CARTESIAN_POINT ( 'NONE',  ( -18.67235195658554403, -19.33882101600501713, 49.52966884056656482 ) ) ;
#36384=CYLINDRICAL_SURFACE ( 'NONE', #1709, 1.999999999999999112 ) ;
#36391=DIRECTION ( 'NONE',  ( -3.071710424422018668E-17, 6.404604876783312462E-16, 1.000000000000000000 ) ) ;
#36394=ORIENTED_EDGE ( 'NONE', *, *, #45968, .T. ) ;
#36403=DIRECTION ( 'NONE',  ( -3.071710424422018668E-17, 6.404604876783312462E-16, 1.000000000000000000 ) ) ;
#36406=DIRECTION ( 'NONE',  ( -3.071710424422018668E-17, 6.404604876783312462E-16, 1.000000000000000000 ) ) ;
#36417=CARTESIAN_POINT ( 'NONE',  ( -22.10677449762105340, -15.19398901379252642, 52.02966884056656482 ) ) ;
#36421=ADVANCED_FACE ( 'NONE', ( #28720 ), #1888, .T. ) ;
#36422=DIRECTION ( 'NONE',  ( 0.9687793358424821033, -0.2479245821708680464, 0.000000000000000000 ) ) ;
#36423=CARTESIAN_POINT ( 'NONE',  ( -20.86860741727135959, -11.63137574808859931, 49.52966884056655772 ) ) ;
#36428=CARTESIAN_POINT ( 'NONE',  ( -17.42409385541299471, -14.80920654474435771, 49.52966884056655772 ) ) ;
#36429=VERTEX_POINT ( 'NONE', #32421 ) ;
#36459=DIRECTION ( 'NONE',  ( 0.9687793358424817702, -0.2479245821708686570, 0.000000000000000000 ) ) ;
#36472=ORIENTED_EDGE ( 'NONE', *, *, #6046, .F. ) ;
#36473=DIRECTION ( 'NONE',  ( -0.2479245821708774278, -0.9687793358424795498, 0.000000000000000000 ) ) ;
#36513=CARTESIAN_POINT ( 'NONE',  ( -17.42409385541299471, -14.80920654474435771, 49.52966884056655772 ) ) ;
#36514=CIRCLE ( 'NONE', #10565, 5.249999999999998224 ) ;
#36519=FACE_OUTER_BOUND ( 'NONE', #30075, .T. ) ;
#36521=EDGE_CURVE ( 'NONE', #39153, #12742, #35749, .T. ) ;
#36523=EDGE_CURVE ( 'NONE', #10364, #17349, #888, .T. ) ;
#36525=EDGE_CURVE ( 'NONE', #48635, #6071, #20057, .T. ) ;
#36528=ORIENTED_EDGE ( 'NONE', *, *, #22288, .T. ) ;
#36530=DIRECTION ( 'NONE',  ( -3.071710424422018668E-17, 6.404604876783312462E-16, 1.000000000000000000 ) ) ;
#36533=DIRECTION ( 'NONE',  ( 0.5097212845717489227, -0.8603395911234855697, 0.000000000000000000 ) ) ;
#36541=ORIENTED_EDGE ( 'NONE', *, *, #36652, .F. ) ;
#36542=AXIS2_PLACEMENT_3D ( 'NONE', #42394, #8662, #22711 ) ;
#36544=EDGE_CURVE ( 'NONE', #30644, #10107, #42065, .T. ) ;
#36563=CARTESIAN_POINT ( 'NONE',  ( -17.42409385541299471, -14.80920654474434883, 62.02966884056656482 ) ) ;
#36569=AXIS2_PLACEMENT_3D ( 'NONE', #12347, #37714, #7954 ) ;
#36579=ORIENTED_EDGE ( 'NONE', *, *, #46781, .F. ) ;
#36580=DIRECTION ( 'NONE',  ( -3.071710424422018668E-17, 6.404604876783312462E-16, 1.000000000000000000 ) ) ;
#36601=ORIENTED_EDGE ( 'NONE', *, *, #27763, .T. ) ;
#36607=DIRECTION ( 'NONE',  ( 3.071710424422018668E-17, -6.404604876783312462E-16, -1.000000000000000000 ) ) ;
#36608=DIRECTION ( 'NONE',  ( -3.071710424422018668E-17, 6.404604876783312462E-16, 1.000000000000000000 ) ) ;
#36623=EDGE_CURVE ( 'NONE', #8715, #241, #19252, .T. ) ;
#36631=EDGE_CURVE ( 'NONE', #8357, #6295, #46771, .T. ) ;
#36634=VERTEX_POINT ( 'NONE', #4826 ) ;
#36639=DIRECTION ( 'NONE',  ( 0.9687793358424821033, -0.2479245821708677133, 0.000000000000000000 ) ) ;
#36650=CARTESIAN_POINT ( 'NONE',  ( -13.74654679279883851, -11.90422292133819582, 52.02966884056656482 ) ) ;
#36652=EDGE_CURVE ( 'NONE', #35637, #8478, #9248, .T. ) ;
#36672=VECTOR ( 'NONE', #36331, 1000.000000000000000 ) ;
#36674=CARTESIAN_POINT ( 'NONE',  ( -19.83890857264518104, -18.82566669410956806, 52.02966884056656482 ) ) ;
#36678=VERTEX_POINT ( 'NONE', #14109 ) ;
#36679=DIRECTION ( 'NONE',  ( 0.9687793358424821033, -0.2479245821708680464, 0.000000000000000000 ) ) ;
#36681=VERTEX_POINT ( 'NONE', #14582 ) ;
#36682=CARTESIAN_POINT ( 'NONE',  ( -13.17762867948185601, -11.72213130924974500, 52.02966884056656482 ) ) ;
#36687=ORIENTED_EDGE ( 'NONE', *, *, #45166, .T. ) ;
#36695=VERTEX_POINT ( 'NONE', #9967 ) ;
#36701=DIRECTION ( 'NONE',  ( -0.2479245821708778996, -0.9687793358424794388, 0.000000000000000000 ) ) ;
#36721=DIRECTION ( 'NONE',  ( 3.071710424422018668E-17, -6.404604876783312462E-16, -1.000000000000000000 ) ) ;
#36726=VERTEX_POINT ( 'NONE', #40421 ) ;
#36732=DIRECTION ( 'NONE',  ( -0.3964226963016469485, -0.9180681052388935948, 0.000000000000000000 ) ) ;
#36740=COLOUR_RGB ( '', 0.31764706, 0.68627451, 0.89019608) ;
#36749=AXIS2_PLACEMENT_3D ( 'NONE', #30140, #22751, #11173 ) ;
#36754=EDGE_CURVE ( 'NONE', #42831, #21817, #48259, .T. ) ;
#36766=DIRECTION ( 'NONE',  ( -0.8447509909909768355, 0.5351595679979596065, 0.000000000000000000 ) ) ;
#36767=EDGE_CURVE ( 'NONE', #18227, #15068, #24713, .T. ) ;
#36772=AXIS2_PLACEMENT_3D ( 'NONE', #14098, #47864, #6509 ) ;
#36813=CARTESIAN_POINT ( 'NONE',  ( -13.07932274695846964, -16.56597809083076100, 52.02966884056656482 ) ) ;
#36816=AXIS2_PLACEMENT_3D ( 'NONE', #31654, #46673, #43960 ) ;
#36817=DIRECTION ( 'NONE',  ( -3.071710424422018668E-17, 6.404604876783312462E-16, 1.000000000000000000 ) ) ;
#36826=VERTEX_POINT ( 'NONE', #4225 ) ;
#36832=CARTESIAN_POINT ( 'NONE',  ( -20.50876352152090121, -19.05741946913900620, 52.02966884056656482 ) ) ;
#36834=ORIENTED_EDGE ( 'NONE', *, *, #5110, .T. ) ;
#36838=CARTESIAN_POINT ( 'NONE',  ( -16.50530592306966682, -19.40475993746870387, 52.02966884056656482 ) ) ;
#36847=FACE_OUTER_BOUND ( 'NONE', #10783, .T. ) ;
#36858=EDGE_CURVE ( 'NONE', #26781, #19923, #25565, .T. ) ;
#36862=DIRECTION ( 'NONE',  ( 0.9687793358424821033, -0.2479245821708680464, 0.000000000000000000 ) ) ;
#36883=AXIS2_PLACEMENT_3D ( 'NONE', #10084, #44085, #25581 ) ;
#36884=VERTEX_POINT ( 'NONE', #7436 ) ;
#36885=CARTESIAN_POINT ( 'NONE',  ( -13.33738394060092070, -12.51528319768659436, 49.52966884056655772 ) ) ;
#36892=AXIS2_PLACEMENT_3D ( 'NONE', #36904, #48239, #36422 ) ;
#36893=CIRCLE ( 'NONE', #24345, 2.000000000000001776 ) ;
#36904=CARTESIAN_POINT ( 'NONE',  ( -17.42409385541299471, -14.80920654474435771, 49.52966884056655772 ) ) ;
#36911=DIRECTION ( 'NONE',  ( -3.071710424422018668E-17, 6.404604876783312462E-16, 1.000000000000000000 ) ) ;
#36912=CARTESIAN_POINT ( 'NONE',  ( -17.42409385541299471, -14.80920654474435771, 49.52966884056655772 ) ) ;
#36914=ORIENTED_EDGE ( 'NONE', *, *, #44929, .F. ) ;
#36916=CARTESIAN_POINT ( 'NONE',  ( -18.55662820153069248, -10.26160847489872374, 49.52966884056655772 ) ) ;
#36922=AXIS2_PLACEMENT_3D ( 'NONE', #21323, #17596, #43491 ) ;
#36941=CARTESIAN_POINT ( 'NONE',  ( -12.21634942047498384, -14.14445252980938861, 50.77966884056655772 ) ) ;
#36947=LINE ( 'NONE', #24924, #26596 ) ;
#36959=AXIS2_PLACEMENT_3D ( 'NONE', #23405, #12077, #35196 ) ;
#36967=ORIENTED_EDGE ( 'NONE', *, *, #25778, .F. ) ;
#36989=AXIS2_PLACEMENT_3D ( 'NONE', #25752, #37806, #14634 ) ;
#36992=ADVANCED_FACE ( 'NONE', ( #24393 ), #4454, .T. ) ;
#36994=CARTESIAN_POINT ( 'NONE',  ( -14.83720200468841810, -10.88702015217558206, 49.52966884056655772 ) ) ;
#37014=AXIS2_PLACEMENT_3D ( 'NONE', #15135, #33598, #37538 ) ;
#37034=CIRCLE ( 'NONE', #40996, 5.249999999999998224 ) ;
#37055=DIRECTION ( 'NONE',  ( 0.9687793358424821033, -0.2479245821708677133, 0.000000000000000000 ) ) ;
#37059=CIRCLE ( 'NONE', #41018, 2.000000000000001776 ) ;
#37068=ORIENTED_EDGE ( 'NONE', *, *, #34342, .F. ) ;
#37071=ORIENTED_EDGE ( 'NONE', *, *, #32121, .T. ) ;
#37077=AXIS2_PLACEMENT_3D ( 'NONE', #9942, #1825, #24731 ) ;
#37089=DIRECTION ( 'NONE',  ( 0.9757441136919973168, 0.2189141945955502822, 0.000000000000000000 ) ) ;
#37099=AXIS2_PLACEMENT_3D ( 'NONE', #36428, #20712, #28347 ) ;
#37108=DIRECTION ( 'NONE',  ( -3.071710424422018668E-17, 6.404604876783312462E-16, 1.000000000000000000 ) ) ;
#37110=ADVANCED_FACE ( 'NONE', ( #24871 ), #32498, .T. ) ;
#37130=ADVANCED_FACE ( 'NONE', ( #20933 ), #35934, .T. ) ;
#37132=CARTESIAN_POINT ( 'NONE',  ( -13.16616306552584525, -16.76709000361798729, 49.52966884056655772 ) ) ;
#37154=CARTESIAN_POINT ( 'NONE',  ( -18.89533436007378597, -9.769568524266553311, 50.77966884056655772 ) ) ;
#37163=EDGE_CURVE ( 'NONE', #41134, #45644, #9868, .T. ) ;
#37194=ORIENTED_EDGE ( 'NONE', *, *, #31080, .F. ) ;
#37197=LINE ( 'NONE', #33500, #22407 ) ;
#37210=EDGE_CURVE ( 'NONE', #19709, #13051, #421, .T. ) ;
#37237=DIRECTION ( 'NONE',  ( 0.9687793358424821033, -0.2479245821708677133, 0.000000000000000000 ) ) ;
#37252=AXIS2_PLACEMENT_3D ( 'NONE', #4278, #15329, #5010 ) ;
#37253=ORIENTED_EDGE ( 'NONE', *, *, #38937, .F. ) ;
#37260=ORIENTED_EDGE ( 'NONE', *, *, #45027, .T. ) ;
#37266=EDGE_CURVE ( 'NONE', #11402, #978, #12973, .T. ) ;
#37270=DIRECTION ( 'NONE',  ( 0.9687793358424817702, -0.2479245821708684905, 0.000000000000000000 ) ) ;
#37281=VERTEX_POINT ( 'NONE', #37132 ) ;
#37283=PRODUCT_DEFINITION ( 'UNKNOWN', '', #15628, #17406 ) ;
#37288=CARTESIAN_POINT ( 'NONE',  ( -21.77108044372514684, -13.02615771018284363, 52.02966884056656482 ) ) ;
#37291=FACE_OUTER_BOUND ( 'NONE', #6184, .T. ) ;
#37297=DIRECTION ( 'NONE',  ( -3.071710424422018668E-17, 6.404604876783312462E-16, 1.000000000000000000 ) ) ;
#37305=ORIENTED_EDGE ( 'NONE', *, *, #31293, .F. ) ;
#37309=DIRECTION ( 'NONE',  ( 0.9687793358424821033, -0.2479245821708680464, 0.000000000000000000 ) ) ;
#37323=ORIENTED_EDGE ( 'NONE', *, *, #45395, .T. ) ;
#37324=AXIS2_PLACEMENT_3D ( 'NONE', #32274, #32021, #43102 ) ;
#37337=ORIENTED_EDGE ( 'NONE', *, *, #9683, .T. ) ;
#37338=EDGE_CURVE ( 'NONE', #10974, #28161, #1989, .T. ) ;
#37342=EDGE_CURVE ( 'NONE', #36361, #33881, #7523, .T. ) ;
#37363=CARTESIAN_POINT ( 'NONE',  ( -12.67665486305926237, -12.56770637434968307, 52.02966884056656482 ) ) ;
#37364=ORIENTED_EDGE ( 'NONE', *, *, #1423, .T. ) ;
#37369=DIRECTION ( 'NONE',  ( -3.071710424422018668E-17, 6.404604876783312462E-16, 1.000000000000000000 ) ) ;
#37373=DIRECTION ( 'NONE',  ( -3.071710424422018668E-17, 6.404604876783312462E-16, 1.000000000000000000 ) ) ;
#37377=ORIENTED_EDGE ( 'NONE', *, *, #1716, .F. ) ;
#37387=DIRECTION ( 'NONE',  ( 0.9687793358424819923, -0.2479245821708676023, 0.000000000000000000 ) ) ;
#37395=ORIENTED_EDGE ( 'NONE', *, *, #34037, .T. ) ;
#37400=CARTESIAN_POINT ( 'NONE',  ( -20.63647318826268773, -18.96169002115701119, 50.77966884056655772 ) ) ;
#37404=DIRECTION ( 'NONE',  ( -3.071710424422018668E-17, 6.404604876783312462E-16, 1.000000000000000000 ) ) ;
#37406=ADVANCED_FACE ( 'NONE', ( #31898 ), #2343, .T. ) ;
#37420=DIRECTION ( 'NONE',  ( -3.071710424422018668E-17, 6.404604876783312462E-16, 1.000000000000000000 ) ) ;
#37429=DIRECTION ( 'NONE',  ( -3.071710424422018668E-17, 6.404604876783312462E-16, 1.000000000000000000 ) ) ;
#37439=EDGE_LOOP ( 'NONE', ( #16255, #47203, #48250, #31930 ) ) ;
#37441=DIRECTION ( 'NONE',  ( 0.9687793358424821033, -0.2479245821708677133, 0.000000000000000000 ) ) ;
#37448=CYLINDRICAL_SURFACE ( 'NONE', #36542, 2.000000000000001332 ) ;
#37464=SURFACE_STYLE_FILL_AREA ( #22470 ) ;
#37467=LINE ( 'NONE', #3762, #33924 ) ;
#37472=EDGE_CURVE ( 'NONE', #1509, #42407, #27854, .T. ) ;
#37481=VERTEX_POINT ( 'NONE', #40265 ) ;
#37482=EDGE_CURVE ( 'NONE', #7471, #35637, #19989, .T. ) ;
#37485=FACE_OUTER_BOUND ( 'NONE', #25825, .T. ) ;
#37501=EDGE_LOOP ( 'NONE', ( #22297, #45141, #18173, #41225 ) ) ;
#37506=AXIS2_PLACEMENT_3D ( 'NONE', #36994, #6978, #29625 ) ;
#37538=DIRECTION ( 'NONE',  ( 0.9687793358424821033, -0.2479245821708679909, 0.000000000000000000 ) ) ;
#37547=ORIENTED_EDGE ( 'NONE', *, *, #9148, .T. ) ;
#37569=EDGE_LOOP ( 'NONE', ( #45526, #44298, #2582, #17496 ) ) ;
#37598=DIRECTION ( 'NONE',  ( -3.071710424422018668E-17, 6.404604876783312462E-16, 1.000000000000000000 ) ) ;
#37599=CIRCLE ( 'NONE', #14802, 2.000000000000000000 ) ;
#37615=EDGE_CURVE ( 'NONE', #35750, #16040, #18815, .T. ) ;
#37625=ORIENTED_EDGE ( 'NONE', *, *, #46781, .T. ) ;
#37632=CARTESIAN_POINT ( 'NONE',  ( -12.48216758013337113, -16.58117287899024461, 52.02966884056656482 ) ) ;
#37648=AXIS2_PLACEMENT_3D ( 'NONE', #35337, #23546, #19850 ) ;
#37649=DIRECTION ( 'NONE',  ( -3.071710424422018668E-17, 6.404604876783312462E-16, 1.000000000000000000 ) ) ;
#37650=CARTESIAN_POINT ( 'NONE',  ( -14.98297878932515381, -10.79466886532025605, 49.52966884056655772 ) ) ;
#37658=ORIENTED_EDGE ( 'NONE', *, *, #12102, .T. ) ;
#37692=ORIENTED_EDGE ( 'NONE', *, *, #42350, .F. ) ;
#37705=DIRECTION ( 'NONE',  ( 0.9956360040033426229, -0.09332174201254497814, 0.000000000000000000 ) ) ;
#37707=DIRECTION ( 'NONE',  ( 0.3688590060343596155, -0.9294853595766554566, 0.000000000000000000 ) ) ;
#37710=DIRECTION ( 'NONE',  ( 0.9687793358424819923, -0.2479245821708680464, 0.000000000000000000 ) ) ;
#37711=AXIS2_PLACEMENT_3D ( 'NONE', #31026, #46044, #12299 ) ;
#37714=DIRECTION ( 'NONE',  ( -3.071710424422018668E-17, 6.404604876783312462E-16, 1.000000000000000000 ) ) ;
#37732=CARTESIAN_POINT ( 'NONE',  ( -16.60134452727454146, -19.99433755013348701, 49.52966884056656482 ) ) ;
#37733=ORIENTED_EDGE ( 'NONE', *, *, #22073, .F. ) ;
#37740=CARTESIAN_POINT ( 'NONE',  ( -20.51116909090755769, -10.56274136881318526, 50.77966884056655772 ) ) ;
#37747=DIRECTION ( 'NONE',  ( 0.9687793358424821033, -0.2479245821708680464, 0.000000000000000000 ) ) ;
#37759=VECTOR ( 'NONE', #17888, 1000.000000000000000 ) ;
#37803=CARTESIAN_POINT ( 'NONE',  ( -21.02292652713908794, -10.98678540089889921, 50.77966884056655772 ) ) ;
#37806=DIRECTION ( 'NONE',  ( -3.071710424422018668E-17, 6.404604876783312462E-16, 1.000000000000000000 ) ) ;
#37809=FACE_OUTER_BOUND ( 'NONE', #46738, .T. ) ;
#37814=AXIS2_PLACEMENT_3D ( 'NONE', #25077, #43057, #5651 ) ;
#37816=CARTESIAN_POINT ( 'NONE',  ( -17.42409385541299471, -14.80920654474435771, 49.52966884056655772 ) ) ;
#37827=ORIENTED_EDGE ( 'NONE', *, *, #32856, .T. ) ;
#37834=DIRECTION ( 'NONE',  ( 0.06357898915123481876, -0.9979768094191904249, 0.000000000000000000 ) ) ;
#37844=AXIS2_PLACEMENT_3D ( 'NONE', #48646, #26244, #25510 ) ;
#37846=CARTESIAN_POINT ( 'NONE',  ( -16.87780900865216438, -10.15465445929086208, 49.52966884056655772 ) ) ;
#37859=CARTESIAN_POINT ( 'NONE',  ( -13.33852097861372421, -12.48893720396535478, 49.52966884056655772 ) ) ;
#37882=EDGE_LOOP ( 'NONE', ( #15619, #18217, #9104, #31697 ) ) ;
#37885=VECTOR ( 'NONE', #32471, 1000.000000000000000 ) ;
#37887=ORIENTED_EDGE ( 'NONE', *, *, #11515, .F. ) ;
#37890=DIRECTION ( 'NONE',  ( -3.071710424422018668E-17, 6.404604876783312462E-16, 1.000000000000000000 ) ) ;
#37932=DIRECTION ( 'NONE',  ( -3.071710424422018668E-17, 6.404604876783312462E-16, 1.000000000000000000 ) ) ;
#37941=EDGE_LOOP ( 'NONE', ( #43059, #6503, #37305, #39719 ) ) ;
#37944=DIRECTION ( 'NONE',  ( -0.8447509909909768355, 0.5351595679979597175, 0.000000000000000000 ) ) ;
#37952=CARTESIAN_POINT ( 'NONE',  ( -17.42409385541299471, -14.80920654474435594, 52.02966884056656482 ) ) ;
#37978=EDGE_CURVE ( 'NONE', #12756, #14479, #45849, .T. ) ;
#37979=ORIENTED_EDGE ( 'NONE', *, *, #1038, .T. ) ;
#37984=ORIENTED_EDGE ( 'NONE', *, *, #42422, .F. ) ;
#37995=CARTESIAN_POINT ( 'NONE',  ( -13.82526118368687307, -18.63162768858978779, 49.52966884056656482 ) ) ;
#38012=CARTESIAN_POINT ( 'NONE',  ( -12.82854046268865034, -13.89041861240101206, 49.52966884056655772 ) ) ;
#38015=VERTEX_POINT ( 'NONE', #26893 ) ;
#38020=ADVANCED_FACE ( 'NONE', ( #44881 ), #18752, .T. ) ;
#38031=EDGE_LOOP ( 'NONE', ( #33123, #41184, #5409, #17203 ) ) ;
#38039=VERTEX_POINT ( 'NONE', #42145 ) ;
#38046=CARTESIAN_POINT ( 'NONE',  ( -17.42409385541299471, -14.80920654474435771, 49.52966884056655772 ) ) ;
#38050=VERTEX_POINT ( 'NONE', #31296 ) ;
#38052=DIRECTION ( 'NONE',  ( -3.071710424422018668E-17, 6.404604876783312462E-16, 1.000000000000000000 ) ) ;
#38057=ORIENTED_EDGE ( 'NONE', *, *, #17632, .T. ) ;
#38071=DIRECTION ( 'NONE',  ( 0.9687793358424822143, -0.2479245821708672415, 0.000000000000000000 ) ) ;
#38074=ORIENTED_EDGE ( 'NONE', *, *, #32489, .T. ) ;
#38079=CIRCLE ( 'NONE', #47547, 5.249999999999998224 ) ;
#38092=DIRECTION ( 'NONE',  ( -3.071710424422018668E-17, 6.404604876783312462E-16, 1.000000000000000000 ) ) ;
#38093=ADVANCED_FACE ( 'NONE', ( #35697 ), #16253, .T. ) ;
#38103=CIRCLE ( 'NONE', #19250, 1.999999999999999112 ) ;
#38146=ORIENTED_EDGE ( 'NONE', *, *, #36525, .F. ) ;
#38150=ORIENTED_EDGE ( 'NONE', *, *, #37338, .T. ) ;
#38152=CARTESIAN_POINT ( 'NONE',  ( -17.42409385541299471, -14.80920654474434883, 62.02966884056656482 ) ) ;
#38157=ADVANCED_FACE ( 'NONE', ( #2936 ), #24653, .T. ) ;
#38165=DIRECTION ( 'NONE',  ( 3.071710424422018668E-17, -6.404604876783312462E-16, -1.000000000000000000 ) ) ;
#38169=DIRECTION ( 'NONE',  ( 0.9687793358424821033, -0.2479245821708679909, 0.000000000000000000 ) ) ;
#38177=VERTEX_POINT ( 'NONE', #36423 ) ;
#38190=CARTESIAN_POINT ( 'NONE',  ( -17.42409385541299471, -14.80920654474435771, 49.52966884056655772 ) ) ;
#38211=FACE_OUTER_BOUND ( 'NONE', #1726, .T. ) ;
#38216=ORIENTED_EDGE ( 'NONE', *, *, #29302, .T. ) ;
#38222=CARTESIAN_POINT ( 'NONE',  ( -20.35492123770571382, -11.13690394275196383, 52.02966884056656482 ) ) ;
#38226=CARTESIAN_POINT ( 'NONE',  ( -18.67235195658554403, -19.33882101600501713, 52.02966884056656482 ) ) ;
#38227=EDGE_CURVE ( 'NONE', #43698, #2810, #31024, .T. ) ;
#38245=CYLINDRICAL_SURFACE ( 'NONE', #7009, 4.686499999999997002 ) ;
#38263=CIRCLE ( 'NONE', #16266, 4.686499999999998778 ) ;
#38288=EDGE_LOOP ( 'NONE', ( #38598, #44215, #17381, #33516 ) ) ;
#38294=VERTEX_POINT ( 'NONE', #30288 ) ;
#38307=VECTOR ( 'NONE', #13163, 1000.000000000000000 ) ;
#38316=AXIS2_PLACEMENT_3D ( 'NONE', #20313, #24513, #28189 ) ;
#38322=CARTESIAN_POINT ( 'NONE',  ( -15.79771479060332240, -19.20445095063907104, 49.52966884056656482 ) ) ;
#38325=EDGE_LOOP ( 'NONE', ( #32758, #26819, #24497, #34460 ) ) ;
#38328=EDGE_CURVE ( 'NONE', #10862, #36372, #15718, .T. ) ;
#38329=FACE_OUTER_BOUND ( 'NONE', #20565, .T. ) ;
#38334=CYLINDRICAL_SURFACE ( 'NONE', #28436, 4.686499999999997002 ) ;
#38349=VECTOR ( 'NONE', #34668, 1000.000000000000000 ) ;
#38357=ORIENTED_EDGE ( 'NONE', *, *, #7248, .T. ) ;
#38367=ORIENTED_EDGE ( 'NONE', *, *, #18386, .T. ) ;
#38370=EDGE_CURVE ( 'NONE', #38839, #17452, #27888, .T. ) ;
#38377=VECTOR ( 'NONE', #15638, 1000.000000000000000 ) ;
#38387=CIRCLE ( 'NONE', #34450, 5.249999999999998224 ) ;
#38391=EDGE_CURVE ( 'NONE', #25725, #12617, #1435, .T. ) ;
#38394=DIRECTION ( 'NONE',  ( -3.071710424422018668E-17, 6.404604876783312462E-16, 1.000000000000000000 ) ) ;
#38419=ORIENTED_EDGE ( 'NONE', *, *, #21006, .F. ) ;
#38422=DIRECTION ( 'NONE',  ( -3.071710424422018668E-17, 6.404604876783312462E-16, 1.000000000000000000 ) ) ;
#38426=AXIS2_PLACEMENT_3D ( 'NONE', #25692, #10928, #10681 ) ;
#38433=CARTESIAN_POINT ( 'NONE',  ( -17.42409385541299471, -14.80920654474435771, 49.52966884056655772 ) ) ;
#38435=DIRECTION ( 'NONE',  ( -3.071710424422018668E-17, 6.404604876783312462E-16, 1.000000000000000000 ) ) ;
#38442=ADVANCED_FACE ( 'NONE', ( #6594 ), #25066, .T. ) ;
#38454=DIRECTION ( 'NONE',  ( -0.9979768094191907579, -0.06357898915123130767, 0.000000000000000000 ) ) ;
#38456=CARTESIAN_POINT ( 'NONE',  ( -19.66559402580761784, -10.06176755239059695, 50.77966884056655772 ) ) ;
#38460=AXIS2_PLACEMENT_3D ( 'NONE', #8833, #37932, #46960 ) ;
#38480=CYLINDRICAL_SURFACE ( 'NONE', #10281, 5.249999999999998224 ) ;
#38483=AXIS2_PLACEMENT_3D ( 'NONE', #27870, #24677, #16775 ) ;
#38486=ORIENTED_EDGE ( 'NONE', *, *, #39548, .F. ) ;
#38487=CARTESIAN_POINT ( 'NONE',  ( -13.84085632603101956, -17.84827948783496865, 49.52966884056656482 ) ) ;
#38489=CARTESIAN_POINT ( 'NONE',  ( -22.36602013069261119, -13.03724021049842996, 52.02966884056656482 ) ) ;
#38535=VERTEX_POINT ( 'NONE', #44511 ) ;
#38538=LINE ( 'NONE', #4821, #29405 ) ;
#38542=CARTESIAN_POINT ( 'NONE',  ( -17.42409385541299471, -14.80920654474435594, 52.02966884056656482 ) ) ;
#38555=ORIENTED_EDGE ( 'NONE', *, *, #19779, .F. ) ;
#38565=ORIENTED_EDGE ( 'NONE', *, *, #18074, .T. ) ;
#38567=EDGE_CURVE ( 'NONE', #26370, #6587, #13701, .T. ) ;
#38569=CARTESIAN_POINT ( 'NONE',  ( -16.15640231613377154, -10.29741749701175380, 49.52966884056655772 ) ) ;
#38571=ORIENTED_EDGE ( 'NONE', *, *, #48522, .F. ) ;
#38586=DIRECTION ( 'NONE',  ( -0.9687793358424819923, 0.2479245821708680464, 0.000000000000000000 ) ) ;
#38588=CIRCLE ( 'NONE', #29923, 1.999999999999999556 ) ;
#38598=ORIENTED_EDGE ( 'NONE', *, *, #36287, .T. ) ;
#38609=AXIS2_PLACEMENT_3D ( 'NONE', #45750, #12000, #42036 ) ;
#38614=VERTEX_POINT ( 'NONE', #26276 ) ;
#38616=DIRECTION ( 'NONE',  ( -0.3688590060343653887, 0.9294853595766531251, 0.000000000000000000 ) ) ;
#38617=ORIENTED_EDGE ( 'NONE', *, *, #14804, .T. ) ;
#38630=AXIS2_PLACEMENT_3D ( 'NONE', #8059, #3359, #19114 ) ;
#38638=ADVANCED_FACE ( 'NONE', ( #41290 ), #7575, .T. ) ;
#38647=VECTOR ( 'NONE', #9426, 1000.000000000000000 ) ;
#38650=CARTESIAN_POINT ( 'NONE',  ( -17.01690395770326347, -19.47798354061844961, 49.52966884056656482 ) ) ;
#38657=AXIS2_PLACEMENT_3D ( 'NONE', #19143, #15424, #30731 ) ;
#38665=CIRCLE ( 'NONE', #42594, 4.686499999999998778 ) ;
#38670=FACE_OUTER_BOUND ( 'NONE', #44241, .T. ) ;
#38674=ORIENTED_EDGE ( 'NONE', *, *, #34838, .T. ) ;
#38675=ORIENTED_EDGE ( 'NONE', *, *, #35231, .F. ) ;
#38723=DIRECTION ( 'NONE',  ( -3.071710424422018668E-17, 6.404604876783312462E-16, 1.000000000000000000 ) ) ;
#38724=CARTESIAN_POINT ( 'NONE',  ( -12.76954176995949197, -15.35549139150514186, 49.52966884056655772 ) ) ;
#38735=EDGE_LOOP ( 'NONE', ( #44074, #45789, #13401, #38804 ) ) ;
#38736=CYLINDRICAL_SURFACE ( 'NONE', #11154, 2.000000000000001776 ) ;
#38787=PRODUCT_CONTEXT ( 'NONE', #5489, 'mechanical' ) ;
#38790=CIRCLE ( 'NONE', #30935, 1.999999999999998446 ) ;
#38804=ORIENTED_EDGE ( 'NONE', *, *, #46680, .T. ) ;
#38812=DIRECTION ( 'NONE',  ( -3.071710424422018668E-17, 6.404604876783312462E-16, 1.000000000000000000 ) ) ;
#38822=VERTEX_POINT ( 'NONE', #33510 ) ;
#38832=CARTESIAN_POINT ( 'NONE',  ( -17.42409385541299471, -14.80920654474435594, 52.02966884056656482 ) ) ;
#38839=VERTEX_POINT ( 'NONE', #42990 ) ;
#38843=CARTESIAN_POINT ( 'NONE',  ( -20.32907747881911575, -11.13165948213017131, 49.52966884056655772 ) ) ;
#38845=CYLINDRICAL_SURFACE ( 'NONE', #27325, 5.249999999999998224 ) ;
#38846=EDGE_CURVE ( 'NONE', #21817, #20066, #15286, .T. ) ;
#38847=CARTESIAN_POINT ( 'NONE',  ( -17.81160558974998764, -14.71003671187603956, 2.029618040566568027 ) ) ;
#38848=ORIENTED_EDGE ( 'NONE', *, *, #34713, .T. ) ;
#38852=DIRECTION ( 'NONE',  ( -3.071710424422018668E-17, 6.404604876783312462E-16, 1.000000000000000000 ) ) ;
#38859=EDGE_CURVE ( 'NONE', #12742, #31052, #4003, .T. ) ;
#38872=ORIENTED_EDGE ( 'NONE', *, *, #40941, .F. ) ;
#38877=DIRECTION ( 'NONE',  ( 3.071710424422018668E-17, -6.404604876783312462E-16, -1.000000000000000000 ) ) ;
#38883=LINE ( 'NONE', #9100, #8771 ) ;
#38885=DIRECTION ( 'NONE',  ( -3.071710424422018668E-17, 6.404604876783312462E-16, 1.000000000000000000 ) ) ;
#38887=ORIENTED_EDGE ( 'NONE', *, *, #32046, .T. ) ;
#38903=ORIENTED_EDGE ( 'NONE', *, *, #19631, .T. ) ;
#38908=CARTESIAN_POINT ( 'NONE',  ( -17.42409385541299471, -14.80920654474434883, 62.02966884056656482 ) ) ;
#38919=ORIENTED_EDGE ( 'NONE', *, *, #8190, .F. ) ;
#38931=DIRECTION ( 'NONE',  ( -3.071710424422018668E-17, 6.404604876783312462E-16, 1.000000000000000000 ) ) ;
#38937=EDGE_CURVE ( 'NONE', #8715, #11147, #38103, .T. ) ;
#38944=ORIENTED_EDGE ( 'NONE', *, *, #42062, .F. ) ;
#38954=VERTEX_POINT ( 'NONE', #39423 ) ;
#38955=DIRECTION ( 'NONE',  ( -3.071710424422018668E-17, 6.404604876783312462E-16, 1.000000000000000000 ) ) ;
#38978=DIRECTION ( 'NONE',  ( -3.071710424422018668E-17, 6.404604876783312462E-16, 1.000000000000000000 ) ) ;
#38982=CARTESIAN_POINT ( 'NONE',  ( -13.07932274695846964, -16.56597809083076100, 49.52966884056655772 ) ) ;
#38987=ORIENTED_EDGE ( 'NONE', *, *, #18074, .F. ) ;
#38995=ORIENTED_EDGE ( 'NONE', *, *, #19985, .T. ) ;
#39007=VERTEX_POINT ( 'NONE', #27848 ) ;
#39016=CARTESIAN_POINT ( 'NONE',  ( -12.38445583493520630, -13.33796604008351316, 52.02966884056656482 ) ) ;
#39018=DIRECTION ( 'NONE',  ( 0.5351595679979623821, 0.8447509909909750592, 0.000000000000000000 ) ) ;
#39029=CARTESIAN_POINT ( 'NONE',  ( -17.42409385541299471, -14.80920654474435594, 52.02966884056656482 ) ) ;
#39038=ORIENTED_EDGE ( 'NONE', *, *, #13673, .F. ) ;
#39040=EDGE_LOOP ( 'NONE', ( #38887, #8728, #6606, #18978 ) ) ;
#39041=CARTESIAN_POINT ( 'NONE',  ( -15.46621039653938112, -10.55127575485719582, 52.02966884056656482 ) ) ;
#39050=CARTESIAN_POINT ( 'NONE',  ( -18.24390634433515856, -19.99480269976908176, 50.77966884056656482 ) ) ;
#39060=CARTESIAN_POINT ( 'NONE',  ( -21.68202464530013529, -12.85132308587069794, 49.52966884056655772 ) ) ;
#39061=AXIS2_PLACEMENT_3D ( 'NONE', #40318, #47473, #21376 ) ;
#39071=VERTEX_POINT ( 'NONE', #45531 ) ;
#39074=DIRECTION ( 'NONE',  ( 0.9687793358424822143, -0.2479245821708672415, 0.000000000000000000 ) ) ;
#39078=ORIENTED_EDGE ( 'NONE', *, *, #43236, .F. ) ;
#39092=CIRCLE ( 'NONE', #17070, 2.000000000000000888 ) ;
#39098=CARTESIAN_POINT ( 'NONE',  ( -20.43749099114212342, -18.39845715627588874, 52.02966884056656482 ) ) ;
#39099=DIRECTION ( 'NONE',  ( -3.071710424422018668E-17, 6.404604876783312462E-16, 1.000000000000000000 ) ) ;
#39105=DIRECTION ( 'NONE',  ( -3.071710424422018668E-17, 6.404604876783312462E-16, 1.000000000000000000 ) ) ;
#39108=VERTEX_POINT ( 'NONE', #41578 ) ;
#39148=CARTESIAN_POINT ( 'NONE',  ( -18.24390634433515856, -19.99480269976908176, 52.02966884056656482 ) ) ;
#39149=CARTESIAN_POINT ( 'NONE',  ( -19.36557164464469594, -19.08778335711046026, 49.52966884056656482 ) ) ;
#39153=VERTEX_POINT ( 'NONE', #705 ) ;
#39160=CYLINDRICAL_SURFACE ( 'NONE', #29472, 4.686499999999997002 ) ;
#39166=AXIS2_PLACEMENT_3D ( 'NONE', #31761, #39391, #20445 ) ;
#39176=EDGE_LOOP ( 'NONE', ( #17593, #33559, #10153, #8135 ) ) ;
#39192=ORIENTED_EDGE ( 'NONE', *, *, #20171, .T. ) ;
#39195=VECTOR ( 'NONE', #38052, 1000.000000000000000 ) ;
#39206=ADVANCED_FACE ( 'NONE', ( #35861 ), #31704, .T. ) ;
#39240=CARTESIAN_POINT ( 'NONE',  ( -21.93588290314558265, -13.54151500546508657, 49.52966884056655772 ) ) ;
#39243=CIRCLE ( 'NONE', #6192, 2.000000000000000444 ) ;
#39249=AXIS2_PLACEMENT_3D ( 'NONE', #28257, #20387, #13206 ) ;
#39259=DIRECTION ( 'NONE',  ( 0.9687793358424821033, -0.2479245821708677133, 0.000000000000000000 ) ) ;
#39263=CARTESIAN_POINT ( 'NONE',  ( -15.95285335075216970, -19.84884456522215146, 49.52966884056656482 ) ) ;
#39267=DIRECTION ( 'NONE',  ( 3.071710424422018668E-17, -6.404604876783312462E-16, -1.000000000000000000 ) ) ;
#39270=CARTESIAN_POINT ( 'NONE',  ( -18.50517187854146783, -19.38160480531894692, 49.52966884056656482 ) ) ;
#39274=VECTOR ( 'NONE', #14911, 1000.000000000000000 ) ;
#39280=DIRECTION ( 'NONE',  ( 0.9687793358424821033, -0.2479245821708679909, 0.000000000000000000 ) ) ;
#39286=DIRECTION ( 'NONE',  ( -3.071710424422018668E-17, 6.404604876783312462E-16, 1.000000000000000000 ) ) ;
#39290=VERTEX_POINT ( 'NONE', #17634 ) ;
#39325=EDGE_LOOP ( 'NONE', ( #35671, #12361, #41975, #1861 ) ) ;
#39331=DIRECTION ( 'NONE',  ( 0.9687793358424821033, -0.2479245821708677133, 0.000000000000000000 ) ) ;
#39334=ORIENTED_EDGE ( 'NONE', *, *, #29163, .F. ) ;
#39337=DIRECTION ( 'NONE',  ( -3.071710424422018668E-17, 6.404604876783312462E-16, 1.000000000000000000 ) ) ;
#39341=CIRCLE ( 'NONE', #25986, 2.000000000000003109 ) ;
#39344=DIRECTION ( 'NONE',  ( -3.071710424422018668E-17, 6.404604876783312462E-16, 1.000000000000000000 ) ) ;
#39356=CARTESIAN_POINT ( 'NONE',  ( -20.48780003469585154, -11.24700778661463474, 52.02966884056656482 ) ) ;
#39357=DIRECTION ( 'NONE',  ( -3.071710424422018668E-17, 6.404604876783312462E-16, 1.000000000000000000 ) ) ;
#39391=DIRECTION ( 'NONE',  ( -3.071710424422018668E-17, 6.404604876783312462E-16, 1.000000000000000000 ) ) ;
#39400=DIRECTION ( 'NONE',  ( 3.071710424422018668E-17, -6.404604876783312462E-16, -1.000000000000000000 ) ) ;
#39405=VERTEX_POINT ( 'NONE', #28872 ) ;
#39406=VERTEX_POINT ( 'NONE', #48069 ) ;
#39407=EDGE_CURVE ( 'NONE', #31360, #10683, #376, .T. ) ;
#39418=EDGE_LOOP ( 'NONE', ( #24643, #13452, #34868, #12093 ) ) ;
#39422=CIRCLE ( 'NONE', #4844, 5.249999999999998224 ) ;
#39423=CARTESIAN_POINT ( 'NONE',  ( -13.40763370604777371, -17.22402126197652805, 52.02966884056656482 ) ) ;
#39451=CARTESIAN_POINT ( 'NONE',  ( -12.76954176995949375, -15.35549139150514009, 52.02966884056656482 ) ) ;
#39462=DIRECTION ( 'NONE',  ( -3.071710424422018668E-17, 6.404604876783312462E-16, 1.000000000000000000 ) ) ;
#39489=VERTEX_POINT ( 'NONE', #47827 ) ;
#39512=CARTESIAN_POINT ( 'NONE',  ( -14.25548580596218429, -11.33998781794830535, 52.02966884056656482 ) ) ;
#39514=VERTEX_POINT ( 'NONE', #45359 ) ;
#39515=DIRECTION ( 'NONE',  ( -0.6380325334150320771, 0.7700094066334488563, 0.000000000000000000 ) ) ;
#39527=ORIENTED_EDGE ( 'NONE', *, *, #30292, .F. ) ;
#39532=ORIENTED_EDGE ( 'NONE', *, *, #29668, .T. ) ;
#39545=EDGE_CURVE ( 'NONE', #34400, #19139, #32633, .T. ) ;
#39548=EDGE_CURVE ( 'NONE', #45424, #20159, #46807, .T. ) ;
#39550=ADVANCED_FACE ( 'NONE', ( #7697 ), #37448, .T. ) ;
#39557=FACE_OUTER_BOUND ( 'NONE', #13378, .T. ) ;
#39560=AXIS2_PLACEMENT_3D ( 'NONE', #44200, #44426, #41202 ) ;
#39564=DIRECTION ( 'NONE',  ( 0.9687793358424821033, -0.2479245821708677133, 0.000000000000000000 ) ) ;
#39576=ORIENTED_EDGE ( 'NONE', *, *, #15721, .T. ) ;
#39581=CARTESIAN_POINT ( 'NONE',  ( -21.39914427356725213, -17.29159580171669219, 49.52966884056655772 ) ) ;
#39583=ORIENTED_EDGE ( 'NONE', *, *, #10234, .T. ) ;
#39587=EDGE_CURVE ( 'NONE', #22244, #42348, #22437, .T. ) ;
#39594=DIRECTION ( 'NONE',  ( -3.071710424422018668E-17, 6.404604876783312462E-16, 1.000000000000000000 ) ) ;
#39604=DIRECTION ( 'NONE',  ( -3.071710424422018668E-17, 6.404604876783312462E-16, 1.000000000000000000 ) ) ;
#39623=ORIENTED_EDGE ( 'NONE', *, *, #32489, .F. ) ;
#39639=DIRECTION ( 'NONE',  ( 3.071710424422018668E-17, -6.404604876783312462E-16, -1.000000000000000000 ) ) ;
#39640=CYLINDRICAL_SURFACE ( 'NONE', #3894, 2.000000000000000000 ) ;
#39649=CARTESIAN_POINT ( 'NONE',  ( -22.09287085128708839, -15.21639644245407119, 52.02966884056656482 ) ) ;
#39663=AXIS2_PLACEMENT_3D ( 'NONE', #32964, #48010, #21439 ) ;
#39670=DIRECTION ( 'NONE',  ( 0.9687793358424819923, -0.2479245821708680464, 0.000000000000000000 ) ) ;
#39684=CARTESIAN_POINT ( 'NONE',  ( -17.97037870217379307, -19.46375863019785513, 52.02966884056656482 ) ) ;
#39691=DIRECTION ( 'NONE',  ( -0.9687793358424822143, 0.2479245821708672415, 0.000000000000000000 ) ) ;
#39696=CARTESIAN_POINT ( 'NONE',  ( -17.80887632446114921, -10.12652590253629903, 49.52966884056655772 ) ) ;
#39697=CARTESIAN_POINT ( 'NONE',  ( -17.23552066371262725, -19.49191114800217406, 49.52966884056656482 ) ) ;
#39699=AXIS2_PLACEMENT_3D ( 'NONE', #17887, #39594, #32910 ) ;
#39702=DIRECTION ( 'NONE',  ( -0.9956360040033419567, 0.09332174201255245827, 0.000000000000000000 ) ) ;
#39709=CARTESIAN_POINT ( 'NONE',  ( -15.64104502085146642, -10.46221995643221270, 49.52966884056655772 ) ) ;
#39718=LINE ( 'NONE', #47599, #42488 ) ;
#39719=ORIENTED_EDGE ( 'NONE', *, *, #17244, .T. ) ;
#39751=CARTESIAN_POINT ( 'NONE',  ( -16.29155950929526497, -19.35680461458998280, 52.02966884056656482 ) ) ;
#39753=ORIENTED_EDGE ( 'NONE', *, *, #44807, .F. ) ;
#39760=CYLINDRICAL_SURFACE ( 'NONE', #22822, 5.249999999999998224 ) ;
#39768=ORIENTED_EDGE ( 'NONE', *, *, #45297, .T. ) ;
#39771=APPLICATION_CONTEXT ( 'automotive_design' ) ;
#39775=CARTESIAN_POINT ( 'NONE',  ( -12.75531685953890459, -14.40201664703460871, 52.02966884056656482 ) ) ;
#39786=ORIENTED_EDGE ( 'NONE', *, *, #15351, .T. ) ;
#39807=DIRECTION ( 'NONE',  ( -0.9687793358424822143, 0.2479245821708672415, 0.000000000000000000 ) ) ;
#39810=LINE ( 'NONE', #31940, #2840 ) ;
#39812=DIRECTION ( 'NONE',  ( 0.9687793358424821033, -0.2479245821708677133, 0.000000000000000000 ) ) ;
#39822=DIRECTION ( 'NONE',  ( 0.9687793358424821033, -0.2479245821708680464, 0.000000000000000000 ) ) ;
#39837=CIRCLE ( 'NONE', #21002, 2.000000000000001332 ) ;
#39838=AXIS2_PLACEMENT_3D ( 'NONE', #33704, #29802, #32976 ) ;
#39845=AXIS2_PLACEMENT_3D ( 'NONE', #46476, #19884, #42539 ) ;
#39851=CARTESIAN_POINT ( 'NONE',  ( -21.68202464530013529, -12.85132308587069794, 49.52966884056655772 ) ) ;
#39855=ADVANCED_FACE ( 'NONE', ( #1367 ), #23312, .T. ) ;
#39859=DIRECTION ( 'NONE',  ( 0.9687793358424819923, -0.2479245821708678243, 0.000000000000000000 ) ) ;
#39863=CIRCLE ( 'NONE', #15485, 4.686499999999998778 ) ;
#39881=DIRECTION ( 'NONE',  ( 0.9687793358424819923, -0.2479245821708680464, 0.000000000000000000 ) ) ;
#39901=CARTESIAN_POINT ( 'NONE',  ( -21.10164091802717223, -17.71419016815048764, 52.02966884056656482 ) ) ;
#39902=VECTOR ( 'NONE', #23871, 1000.000000000000000 ) ;
#39915=ORIENTED_EDGE ( 'NONE', *, *, #17147, .T. ) ;
#39926=ORIENTED_EDGE ( 'NONE', *, *, #40432, .T. ) ;
#39927=DIRECTION ( 'NONE',  ( -3.071710424422018668E-17, 6.404604876783312462E-16, 1.000000000000000000 ) ) ;
#39933=DIRECTION ( 'NONE',  ( -3.071710424422018668E-17, 6.404604876783312462E-16, 1.000000000000000000 ) ) ;
#39941=CARTESIAN_POINT ( 'NONE',  ( -17.42409385541299471, -14.80920654474435771, 49.52966884056655772 ) ) ;
#39945=ORIENTED_EDGE ( 'NONE', *, *, #30903, .T. ) ;
#39954=CIRCLE ( 'NONE', #29721, 1.999999999999999556 ) ;
#39964=ORIENTED_EDGE ( 'NONE', *, *, #17024, .T. ) ;
#39977=VECTOR ( 'NONE', #14106, 1000.000000000000000 ) ;
#39991=ORIENTED_EDGE ( 'NONE', *, *, #18753, .F. ) ;
#39994=ORIENTED_EDGE ( 'NONE', *, *, #38328, .F. ) ;
#40003=CARTESIAN_POINT ( 'NONE',  ( -20.51116909090755769, -10.56274136881318348, 52.02966884056656482 ) ) ;
#40008=AXIS2_PLACEMENT_3D ( 'NONE', #7990, #23003, #37747 ) ;
#40013=AXIS2_PLACEMENT_3D ( 'NONE', #20474, #38931, #5211 ) ;
#40017=DIRECTION ( 'NONE',  ( -3.071710424422018668E-17, 6.404604876783312462E-16, 1.000000000000000000 ) ) ;
#40023=EDGE_LOOP ( 'NONE', ( #3069, #25010, #48172, #29415 ) ) ;
#40024=EDGE_CURVE ( 'NONE', #21408, #8478, #48371, .T. ) ;
#40033=EDGE_CURVE ( 'NONE', #6071, #20751, #32628, .T. ) ;
#40041=AXIS2_PLACEMENT_3D ( 'NONE', #44620, #17759, #40661 ) ;
#40057=DIRECTION ( 'NONE',  ( 0.8447509909909733938, -0.5351595679979650466, 0.000000000000000000 ) ) ;
#40072=CARTESIAN_POINT ( 'NONE',  ( -17.42409385541299471, -14.80920654474435594, 52.02966884056656482 ) ) ;
#40075=ORIENTED_EDGE ( 'NONE', *, *, #33653, .F. ) ;
#40101=ORIENTED_EDGE ( 'NONE', *, *, #24490, .T. ) ;
#40104=CARTESIAN_POINT ( 'NONE',  ( -21.50966673221228120, -17.12947588552333045, 49.52966884056655772 ) ) ;
#40105=CARTESIAN_POINT ( 'NONE',  ( -17.26958401828953171, -19.65204229739824626, 49.52966884056656482 ) ) ;
#40112=AXIS2_PLACEMENT_3D ( 'NONE', #32936, #17198, #47982 ) ;
#40114=AXIS2_PLACEMENT_3D ( 'NONE', #30379, #3520, #44917 ) ;
#40118=AXIS2_PLACEMENT_3D ( 'NONE', #30414, #40993, #3317 ) ;
#40150=CIRCLE ( 'NONE', #41733, 1.999999999999999556 ) ;
#40152=CARTESIAN_POINT ( 'NONE',  ( -14.94170459844064780, -18.78425696289860269, 49.52966884056656482 ) ) ;
#40153=VECTOR ( 'NONE', #47836, 1000.000000000000000 ) ;
#40155=ORIENTED_EDGE ( 'NONE', *, *, #40024, .T. ) ;
#40164=ADVANCED_FACE ( 'NONE', ( #19811 ), #35048, .T. ) ;
#40166=AXIS2_PLACEMENT_3D ( 'NONE', #41016, #10978, #45213 ) ;
#40181=DIRECTION ( 'NONE',  ( -3.071710424422018668E-17, 6.404604876783312462E-16, 1.000000000000000000 ) ) ;
#40197=CYLINDRICAL_SURFACE ( 'NONE', #19584, 1.999999999999999556 ) ;
#40204=ORIENTED_EDGE ( 'NONE', *, *, #10108, .T. ) ;
#40211=AXIS2_PLACEMENT_3D ( 'NONE', #36563, #43516, #39564 ) ;
#40214=ADVANCED_FACE ( 'NONE', ( #34810 ), #15597, .F. ) ;
#40227=EDGE_CURVE ( 'NONE', #27599, #16869, #45428, .T. ) ;
#40239=EDGE_CURVE ( 'NONE', #22574, #36634, #30659, .T. ) ;
#40265=CARTESIAN_POINT ( 'NONE',  ( -20.63647318826268773, -18.96169002115701119, 52.02966884056656482 ) ) ;
#40269=DIRECTION ( 'NONE',  ( -3.071710424422018668E-17, 6.404604876783312462E-16, 1.000000000000000000 ) ) ;
#40272=DIRECTION ( 'NONE',  ( 3.071710424422018668E-17, -6.404604876783312462E-16, -1.000000000000000000 ) ) ;
#40276=DIRECTION ( 'NONE',  ( 0.9687793358424821033, -0.2479245821708677133, 0.000000000000000000 ) ) ;
#40280=VERTEX_POINT ( 'NONE', #28878 ) ;
#40288=CYLINDRICAL_SURFACE ( 'NONE', #43367, 1.999999999999999556 ) ;
#40302=CYLINDRICAL_SURFACE ( 'NONE', #43894, 1.999999999999999556 ) ;
#40318=CARTESIAN_POINT ( 'NONE',  ( -13.14551704304688684, -16.75068433397603940, 52.02966884056656482 ) ) ;
#40327=CARTESIAN_POINT ( 'NONE',  ( -19.05047292022263505, -10.41396213884962663, 52.02966884056656482 ) ) ;
#40348=CARTESIAN_POINT ( 'NONE',  ( -12.48216758013337113, -16.58117287899024461, 50.77966884056655772 ) ) ;
#40366=EDGE_CURVE ( 'NONE', #46408, #39071, #11436, .T. ) ;
#40396=VERTEX_POINT ( 'NONE', #22223 ) ;
#40408=CARTESIAN_POINT ( 'NONE',  ( -14.41069671968389265, -11.21995593321280360, 49.52966884056655772 ) ) ;
#40421=CARTESIAN_POINT ( 'NONE',  ( -22.60922486080212934, -15.63195587288279320, 52.02966884056656482 ) ) ;
#40432=EDGE_CURVE ( 'NONE', #16630, #43698, #43724, .T. ) ;
#40440=EDGE_LOOP ( 'NONE', ( #14786, #20534, #44545, #45264 ) ) ;
#40447=ORIENTED_EDGE ( 'NONE', *, *, #3603, .F. ) ;
#40466=DIRECTION ( 'NONE',  ( -3.071710424422018668E-17, 6.404604876783312462E-16, 1.000000000000000000 ) ) ;
#40490=VERTEX_POINT ( 'NONE', #42399 ) ;
#40494=CARTESIAN_POINT ( 'NONE',  ( -13.97958029355460852, -17.98703734140009303, 49.52966884056656482 ) ) ;
#40507=ADVANCED_FACE ( 'NONE', ( #11873 ), #41909, .T. ) ;
#40521=CYLINDRICAL_SURFACE ( 'NONE', #28213, 4.686499999999997002 ) ;
#40523=VERTEX_POINT ( 'NONE', #11378 ) ;
#40524=DIRECTION ( 'NONE',  ( -3.071710424422018668E-17, 6.404604876783312462E-16, 1.000000000000000000 ) ) ;
#40525=DIRECTION ( 'NONE',  ( 0.9687793358424821033, -0.2479245821708677133, 0.000000000000000000 ) ) ;
#40527=ORIENTED_EDGE ( 'NONE', *, *, #32729, .T. ) ;
#40528=AXIS2_PLACEMENT_3D ( 'NONE', #31122, #26706, #23026 ) ;
#40539=ORIENTED_EDGE ( 'NONE', *, *, #44878, .F. ) ;
#40542=EDGE_CURVE ( 'NONE', #28192, #8859, #17711, .T. ) ;
#40546=DIRECTION ( 'NONE',  ( -3.071710424422018668E-17, 6.404604876783312462E-16, 1.000000000000000000 ) ) ;
#40565=EDGE_LOOP ( 'NONE', ( #3180, #21780, #9675, #14665 ) ) ;
#40569=DIRECTION ( 'NONE',  ( -3.071710424422018668E-17, 6.404604876783312462E-16, 1.000000000000000000 ) ) ;
#40576=ORIENTED_EDGE ( 'NONE', *, *, #13897, .T. ) ;
#40585=CARTESIAN_POINT ( 'NONE',  ( -20.02395964528090033, -18.70843468947691690, 52.02966884056656482 ) ) ;
#40595=ORIENTED_EDGE ( 'NONE', *, *, #44149, .F. ) ;
#40644=ADVANCED_FACE ( 'NONE', ( #27612 ), #8911, .T. ) ;
#40645=DIRECTION ( 'NONE',  ( -0.06357898915124167438, 0.9979768094191900918, 0.000000000000000000 ) ) ;
#40656=VERTEX_POINT ( 'NONE', #20216 ) ;
#40661=DIRECTION ( 'NONE',  ( -0.9687793358424822143, 0.2479245821708672415, 0.000000000000000000 ) ) ;
#40669=VECTOR ( 'NONE', #7949, 1000.000000000000000 ) ;
#40670=DIRECTION ( 'NONE',  ( -0.06357898915124166050, 0.9979768094191900918, 0.000000000000000000 ) ) ;
#40672=CARTESIAN_POINT ( 'NONE',  ( -17.42260713176972686, -20.05920633423509258, 52.02966884056656482 ) ) ;
#40705=ORIENTED_EDGE ( 'NONE', *, *, #12216, .T. ) ;
#40715=DIRECTION ( 'NONE',  ( 0.8447509909909733938, -0.5351595679979650466, 0.000000000000000000 ) ) ;
#40727=DIRECTION ( 'NONE',  ( -3.071710424422018668E-17, 6.404604876783312462E-16, 1.000000000000000000 ) ) ;
#40736=VECTOR ( 'NONE', #29593, 1000.000000000000000 ) ;
#40740=AXIS2_PLACEMENT_3D ( 'NONE', #29762, #23112, #40831 ) ;
#40745=EDGE_CURVE ( 'NONE', #31233, #15954, #30335, .T. ) ;
#40752=DIRECTION ( 'NONE',  ( 0.9687793358424821033, -0.2479245821708677133, 0.000000000000000000 ) ) ;
#40754=ORIENTED_EDGE ( 'NONE', *, *, #675, .F. ) ;
#40772=LINE ( 'NONE', #22553, #48015 ) ;
#40776=ORIENTED_EDGE ( 'NONE', *, *, #38567, .F. ) ;
#40779=CARTESIAN_POINT ( 'NONE',  ( -17.21153000696512336, -19.50285887057015444, 49.52966884056656482 ) ) ;
#40804=EDGE_CURVE ( 'NONE', #18527, #25029, #20119, .T. ) ;
#40805=DIRECTION ( 'NONE',  ( -3.071710424422018668E-17, 6.404604876783312462E-16, 1.000000000000000000 ) ) ;
#40806=VECTOR ( 'NONE', #47802, 1000.000000000000000 ) ;
#40811=VERTEX_POINT ( 'NONE', #48489 ) ;
#40818=CARTESIAN_POINT ( 'NONE',  ( -15.95285335075216970, -19.84884456522215146, 50.77966884056656482 ) ) ;
#40824=EDGE_CURVE ( 'NONE', #3267, #8796, #33211, .T. ) ;
#40825=VERTEX_POINT ( 'NONE', #29796 ) ;
#40829=CARTESIAN_POINT ( 'NONE',  ( -19.04784696903935881, -9.816619457272704352, 50.77966884056655772 ) ) ;
#40831=DIRECTION ( 'NONE',  ( 0.3688590060343596155, -0.9294853595766554566, 0.000000000000000000 ) ) ;
#40844=CYLINDRICAL_SURFACE ( 'NONE', #46342, 4.686499999999997002 ) ;
#40847=AXIS2_PLACEMENT_3D ( 'NONE', #16679, #39344, #38616 ) ;
#40856=VECTOR ( 'NONE', #46857, 1000.000000000000000 ) ;
#40864=CIRCLE ( 'NONE', #32233, 2.000000000000000444 ) ;
#40866=DIRECTION ( 'NONE',  ( -3.071710424422018668E-17, 6.404604876783312462E-16, 1.000000000000000000 ) ) ;
#40874=ADVANCED_FACE ( 'NONE', ( #26336 ), #30295, .T. ) ;
#40883=CARTESIAN_POINT ( 'NONE',  ( -22.17153284776674482, -17.05070671513899683, 49.52966884056655772 ) ) ;
#40895=DIRECTION ( 'NONE',  ( 0.9687793358424821033, -0.2479245821708680464, 0.000000000000000000 ) ) ;
#40897=LINE ( 'NONE', #7186, #13282 ) ;
#40903=DIRECTION ( 'NONE',  ( 0.9687793358424821033, -0.2479245821708679909, 0.000000000000000000 ) ) ;
#40904=DIRECTION ( 'NONE',  ( -3.071710424422018668E-17, 6.404604876783312462E-16, 1.000000000000000000 ) ) ;
#40910=ORIENTED_EDGE ( 'NONE', *, *, #10973, .T. ) ;
#40914=CIRCLE ( 'NONE', #47977, 5.249999999999998224 ) ;
#40919=CARTESIAN_POINT ( 'NONE',  ( -19.05047292022263505, -10.41396213884962840, 49.52966884056655772 ) ) ;
#40939=AXIS2_PLACEMENT_3D ( 'NONE', #156, #45449, #29941 ) ;
#40941=EDGE_CURVE ( 'NONE', #38177, #40280, #17734, .T. ) ;
#40946=ORIENTED_EDGE ( 'NONE', *, *, #25630, .T. ) ;
#40948=LINE ( 'NONE', #15306, #9546 ) ;
#40969=DIRECTION ( 'NONE',  ( 0.9687793358424821033, -0.2479245821708677133, 0.000000000000000000 ) ) ;
#40983=ORIENTED_EDGE ( 'NONE', *, *, #17444, .F. ) ;
#40991=CARTESIAN_POINT ( 'NONE',  ( -21.67230677980763431, -11.72453687863643523, 50.77966884056655772 ) ) ;
#40993=DIRECTION ( 'NONE',  ( 3.071710424422018668E-17, -6.404604876783312462E-16, -1.000000000000000000 ) ) ;
#40996=AXIS2_PLACEMENT_3D ( 'NONE', #33466, #33716, #44123 ) ;
#40997=EDGE_CURVE ( 'NONE', #15954, #29084, #44522, .T. ) ;
#41007=CARTESIAN_POINT ( 'NONE',  ( -16.44703096029287437, -9.650926977002853846, 50.77966884056655772 ) ) ;
#41016=CARTESIAN_POINT ( 'NONE',  ( -17.42409385541299471, -14.80920654474435594, 52.02966884056656482 ) ) ;
#41018=AXIS2_PLACEMENT_3D ( 'NONE', #1857, #5567, #35578 ) ;
#41028=EDGE_LOOP ( 'NONE', ( #8116, #39192, #31422, #2143 ) ) ;
#41042=DIRECTION ( 'NONE',  ( 0.9687793358424821033, -0.2479245821708680464, 0.000000000000000000 ) ) ;
#41044=ORIENTED_EDGE ( 'NONE', *, *, #48683, .T. ) ;
#41057=ORIENTED_EDGE ( 'NONE', *, *, #25902, .T. ) ;
#41059=EDGE_CURVE ( 'NONE', #31013, #20972, #9589, .T. ) ;
#41063=DIRECTION ( 'NONE',  ( -3.071710424422018668E-17, 6.404604876783312462E-16, 1.000000000000000000 ) ) ;
#41080=CARTESIAN_POINT ( 'NONE',  ( -17.42409385541299471, -14.80920654474435771, 49.52966884056655772 ) ) ;
#41083=ORIENTED_EDGE ( 'NONE', *, *, #29163, .T. ) ;
#41113=EDGE_CURVE ( 'NONE', #17561, #6337, #5190, .T. ) ;
#41118=VERTEX_POINT ( 'NONE', #25794 ) ;
#41134=VERTEX_POINT ( 'NONE', #6111 ) ;
#41145=CARTESIAN_POINT ( 'NONE',  ( -13.97958029355460852, -17.98703734140009303, 52.02966884056656482 ) ) ;
#41151=DIRECTION ( 'NONE',  ( -3.071710424422018668E-17, 6.404604876783312462E-16, 1.000000000000000000 ) ) ;
#41180=EDGE_LOOP ( 'NONE', ( #29194, #39994, #4208, #2487 ) ) ;
#41184=ORIENTED_EDGE ( 'NONE', *, *, #42541, .F. ) ;
#41187=EDGE_CURVE ( 'NONE', #42844, #28760, #24869, .T. ) ;
#41194=ORIENTED_EDGE ( 'NONE', *, *, #28294, .T. ) ;
#41202=DIRECTION ( 'NONE',  ( 0.9687793358424822143, -0.2479245821708672415, 0.000000000000000000 ) ) ;
#41207=LINE ( 'NONE', #4041, #3632 ) ;
#41208=DIRECTION ( 'NONE',  ( 0.9687793358424821033, -0.2479245821708677133, 0.000000000000000000 ) ) ;
#41216=ORIENTED_EDGE ( 'NONE', *, *, #44587, .T. ) ;
#41225=ORIENTED_EDGE ( 'NONE', *, *, #155, .T. ) ;
#41229=CARTESIAN_POINT ( 'NONE',  ( -13.33738394060092070, -12.51528319768659436, 49.52966884056655772 ) ) ;
#41248=ORIENTED_EDGE ( 'NONE', *, *, #5616, .F. ) ;
#41250=ORIENTED_EDGE ( 'NONE', *, *, #44993, .F. ) ;
#41257=CARTESIAN_POINT ( 'NONE',  ( -17.26958401828953171, -19.65204229739824626, 49.52966884056656482 ) ) ;
#41268=CARTESIAN_POINT ( 'NONE',  ( -17.42409385541299471, -14.80920654474435771, 49.52966884056655772 ) ) ;
#41281=ORIENTED_EDGE ( 'NONE', *, *, #17651, .T. ) ;
#41283=EDGE_LOOP ( 'NONE', ( #237, #43437, #1856, #34674 ) ) ;
#41290=FACE_OUTER_BOUND ( 'NONE', #38325, .T. ) ;
#41298=LINE ( 'NONE', #14931, #14984 ) ;
#41306=DIRECTION ( 'NONE',  ( -3.071710424422018668E-17, 6.404604876783312462E-16, 1.000000000000000000 ) ) ;
#41310=AXIS2_PLACEMENT_3D ( 'NONE', #17105, #9982, #36310 ) ;
#41312=DIRECTION ( 'NONE',  ( -3.071710424422018668E-17, 6.404604876783312462E-16, 1.000000000000000000 ) ) ;
#41314=EDGE_CURVE ( 'NONE', #42407, #29156, #35844, .T. ) ;
#41315=DIRECTION ( 'NONE',  ( 0.9687793358424821033, -0.2479245821708680464, 0.000000000000000000 ) ) ;
#41317=ORIENTED_EDGE ( 'NONE', *, *, #12761, .F. ) ;
#41321=DIRECTION ( 'NONE',  ( -3.071710424422018668E-17, 6.404604876783312462E-16, 1.000000000000000000 ) ) ;
#41332=DIRECTION ( 'NONE',  ( -0.3688590060343657773, 0.9294853595766529031, 0.000000000000000000 ) ) ;
#41335=CARTESIAN_POINT ( 'NONE',  ( -17.42409385541299471, -14.80920654474435771, 49.52966884056655772 ) ) ;
#41337=ORIENTED_EDGE ( 'NONE', *, *, #22932, .T. ) ;
#41346=CARTESIAN_POINT ( 'NONE',  ( -17.42409385541299471, -14.80920654474434883, 62.02966884056656482 ) ) ;
#41351=CARTESIAN_POINT ( 'NONE',  ( -16.17583575424048092, -10.27959207348368764, 49.52966884056655772 ) ) ;
#41352=CYLINDRICAL_SURFACE ( 'NONE', #11963, 1.999999999999999556 ) ;
#41353=ORIENTED_EDGE ( 'NONE', *, *, #28625, .F. ) ;
#41356=CARTESIAN_POINT ( 'NONE',  ( -17.42409385541299471, -14.80920654474435594, 52.02966884056656482 ) ) ;
#41364=EDGE_LOOP ( 'NONE', ( #41337, #13616, #1281, #11286 ) ) ;
#41370=EDGE_CURVE ( 'NONE', #15782, #18613, #23267, .T. ) ;
#41379=CARTESIAN_POINT ( 'NONE',  ( -21.13535303541993926, -18.52256826949110646, 49.52966884056656482 ) ) ;
#41399=CARTESIAN_POINT ( 'NONE',  ( -13.10965166868813903, -12.97921450448603231, 52.02966884056656482 ) ) ;
#41416=EDGE_LOOP ( 'NONE', ( #46599, #44596, #2232, #27915 ) ) ;
#41417=AXIS2_PLACEMENT_3D ( 'NONE', #41869, #30310, #14740 ) ;
#41441=CARTESIAN_POINT ( 'NONE',  ( -17.94839601134439633, -19.47832453368858552, 49.52966884056656482 ) ) ;
#41443=CARTESIAN_POINT ( 'NONE',  ( -21.24651499925844078, -18.40803921647045982, 52.02966884056656482 ) ) ;
#41483=CIRCLE ( 'NONE', #578, 0.3999999999999978018 ) ;
#41494=ORIENTED_EDGE ( 'NONE', *, *, #22726, .T. ) ;
#41517=FACE_OUTER_BOUND ( 'NONE', #11517, .T. ) ;
#41528=CIRCLE ( 'NONE', #27362, 1.999999999999999334 ) ;
#41530=LINE ( 'NONE', #15399, #39274 ) ;
#41536=AXIS2_PLACEMENT_3D ( 'NONE', #8167, #30577, #26880 ) ;
#41543=CIRCLE ( 'NONE', #7743, 5.249999999999998224 ) ;
#41560=VERTEX_POINT ( 'NONE', #25443 ) ;
#41563=AXIS2_PLACEMENT_3D ( 'NONE', #16427, #27521, #23843 ) ;
#41567=AXIS2_PLACEMENT_3D ( 'NONE', #43954, #36041, #32606 ) ;
#41568=LINE ( 'NONE', #45520, #42274 ) ;
#41574=CARTESIAN_POINT ( 'NONE',  ( -12.85925802207596114, -13.69662874518197171, 49.52966884056655772 ) ) ;
#41577=CARTESIAN_POINT ( 'NONE',  ( -12.43150676794136089, -13.18545343111793855, 52.02966884056656482 ) ) ;
#41578=CARTESIAN_POINT ( 'NONE',  ( -20.60192465206874246, -18.25372010660273503, 49.52966884056656482 ) ) ;
#41593=AXIS2_PLACEMENT_3D ( 'NONE', #19784, #38723, #31098 ) ;
#41598=AXIS2_PLACEMENT_3D ( 'NONE', #32907, #29477, #13474 ) ;
#41599=DIRECTION ( 'NONE',  ( -3.071710424422018668E-17, 6.404604876783312462E-16, 1.000000000000000000 ) ) ;
#41620=EDGE_LOOP ( 'NONE', ( #19816, #32049, #7385, #38146 ) ) ;
#41622=CIRCLE ( 'NONE', #31391, 2.000000000000000444 ) ;
#41626=ORIENTED_EDGE ( 'NONE', *, *, #22288, .F. ) ;
#41628=AXIS2_PLACEMENT_3D ( 'NONE', #3871, #33891, #29715 ) ;
#41631=DIRECTION ( 'NONE',  ( -3.071710424422018668E-17, 6.404604876783312462E-16, 1.000000000000000000 ) ) ;
#41632=DIRECTION ( 'NONE',  ( -3.071710424422018668E-17, 6.404604876783312462E-16, 1.000000000000000000 ) ) ;
#41660=DIRECTION ( 'NONE',  ( -0.6380325334150318550, 0.7700094066334490783, 0.000000000000000000 ) ) ;
#41661=CIRCLE ( 'NONE', #48716, 5.249999999999998224 ) ;
#41670=ORIENTED_EDGE ( 'NONE', *, *, #14894, .T. ) ;
#41688=DIRECTION ( 'NONE',  ( -3.071710424422018668E-17, 6.404604876783312462E-16, 1.000000000000000000 ) ) ;
#41695=ADVANCED_FACE ( 'NONE', ( #27375 ), #27134, .T. ) ;
#41697=AXIS2_PLACEMENT_3D ( 'NONE', #17683, #6134, #13737 ) ;
#41717=EDGE_LOOP ( 'NONE', ( #44441, #4690, #14848, #8913 ) ) ;
#41721=VERTEX_POINT ( 'NONE', #46591 ) ;
#41731=ADVANCED_FACE ( 'NONE', ( #10116 ), #5465, .T. ) ;
#41733=AXIS2_PLACEMENT_3D ( 'NONE', #3227, #25880, #39515 ) ;
#41741=CARTESIAN_POINT ( 'NONE',  ( -13.75179125342063458, -11.87837916245159953, 49.52966884056655772 ) ) ;
#41757=DIRECTION ( 'NONE',  ( -3.071710424422018668E-17, 6.404604876783312462E-16, 1.000000000000000000 ) ) ;
#41769=CIRCLE ( 'NONE', #15798, 1.999999999999999556 ) ;
#41815=CYLINDRICAL_SURFACE ( 'NONE', #30587, 5.249999999999998224 ) ;
#41830=DIRECTION ( 'NONE',  ( -3.071710424422018668E-17, 6.404604876783312462E-16, 1.000000000000000000 ) ) ;
#41833=DIRECTION ( 'NONE',  ( 3.071710424422018668E-17, -6.404604876783312462E-16, -1.000000000000000000 ) ) ;
#41844=CARTESIAN_POINT ( 'NONE',  ( -21.77108044372514684, -13.02615771018284541, 49.52966884056655772 ) ) ;
#41853=EDGE_LOOP ( 'NONE', ( #15460, #37984, #12802, #26069 ) ) ;
#41869=CARTESIAN_POINT ( 'NONE',  ( -19.89283007060495123, -10.81159512726058836, 52.02966884056656482 ) ) ;
#41872=ADVANCED_FACE ( 'NONE', ( #2713 ), #25378, .T. ) ;
#41906=CARTESIAN_POINT ( 'NONE',  ( -20.59270190486383356, -18.27842527154038521, 49.52966884056656482 ) ) ;
#41909=CYLINDRICAL_SURFACE ( 'NONE', #20898, 4.686499999999997002 ) ;
#41915=( NAMED_UNIT ( * ) PLANE_ANGLE_UNIT ( ) SI_UNIT ( $, .RADIAN. ) );
#41924=ORIENTED_EDGE ( 'NONE', *, *, #28481, .F. ) ;
#41925=EDGE_CURVE ( 'NONE', #15450, #18903, #21914, .T. ) ;
#41926=FACE_OUTER_BOUND ( 'NONE', #30923, .T. ) ;
#41927=EDGE_CURVE ( 'NONE', #40396, #1942, #15729, .T. ) ;
#41930=DIRECTION ( 'NONE',  ( -3.071710424422018668E-17, 6.404604876783312462E-16, 1.000000000000000000 ) ) ;
#41943=ORIENTED_EDGE ( 'NONE', *, *, #35666, .F. ) ;
#41948=FACE_OUTER_BOUND ( 'NONE', #47964, .T. ) ;
#41949=DIRECTION ( 'NONE',  ( 0.9687793358424821033, -0.2479245821708677133, 0.000000000000000000 ) ) ;
#41956=ORIENTED_EDGE ( 'NONE', *, *, #9154, .T. ) ;
#41968=AXIS2_PLACEMENT_3D ( 'NONE', #1282, #8700, #23728 ) ;
#41975=ORIENTED_EDGE ( 'NONE', *, *, #45089, .T. ) ;
#41981=CARTESIAN_POINT ( 'NONE',  ( -17.42409385541299471, -14.80920654474435594, 52.02966884056656482 ) ) ;
#42003=CARTESIAN_POINT ( 'NONE',  ( -17.42409385541299471, -14.80920654474434883, 62.02966884056656482 ) ) ;
#42006=ADVANCED_FACE ( 'NONE', ( #1203 ), #34937, .T. ) ;
#42014=ORIENTED_EDGE ( 'NONE', *, *, #1912, .T. ) ;
#42030=ORIENTED_EDGE ( 'NONE', *, *, #26174, .T. ) ;
#42036=DIRECTION ( 'NONE',  ( -0.9687793358424819923, 0.2479245821708680464, 0.000000000000000000 ) ) ;
#42051=VERTEX_POINT ( 'NONE', #7649 ) ;
#42062=EDGE_CURVE ( 'NONE', #38050, #48382, #23326, .T. ) ;
#42065=CIRCLE ( 'NONE', #26343, 4.686499999999998778 ) ;
#42073=DIRECTION ( 'NONE',  ( -3.071710424422018668E-17, 6.404604876783312462E-16, 1.000000000000000000 ) ) ;
#42092=DIRECTION ( 'NONE',  ( -3.071710424422018668E-17, 6.404604876783312462E-16, 1.000000000000000000 ) ) ;
#42096=ORIENTED_EDGE ( 'NONE', *, *, #15656, .F. ) ;
#42111=EDGE_CURVE ( 'NONE', #36681, #30955, #9341, .T. ) ;
#42116=CARTESIAN_POINT ( 'NONE',  ( -21.97169192525862869, -15.94174089086207147, 49.52966884056655772 ) ) ;
#42117=ORIENTED_EDGE ( 'NONE', *, *, #40824, .F. ) ;
#42120=DIRECTION ( 'NONE',  ( -3.071710424422018668E-17, 6.404604876783312462E-16, 1.000000000000000000 ) ) ;
#42130=DIRECTION ( 'NONE',  ( -3.071710424422018668E-17, 6.404604876783312462E-16, 1.000000000000000000 ) ) ;
#42145=CARTESIAN_POINT ( 'NONE',  ( -12.74138925215518015, -14.62063335304397249, 52.02966884056656482 ) ) ;
#42150=DIRECTION ( 'NONE',  ( -3.071710424422018668E-17, 6.404604876783312462E-16, 1.000000000000000000 ) ) ;
#42157=ORIENTED_EDGE ( 'NONE', *, *, #46764, .T. ) ;
#42196=VERTEX_POINT ( 'NONE', #29493 ) ;
#42197=CARTESIAN_POINT ( 'NONE',  ( -15.77151528785019430, -19.20744933288474954, 49.52966884056656482 ) ) ;
#42198=CARTESIAN_POINT ( 'NONE',  ( -12.82020749880560651, -17.33244462614775827, 49.52966884056655772 ) ) ;
#42200=ORIENTED_EDGE ( 'NONE', *, *, #46838, .T. ) ;
#42205=EDGE_CURVE ( 'NONE', #7167, #25404, #2841, .T. ) ;
#42207=ORIENTED_EDGE ( 'NONE', *, *, #24826, .T. ) ;
#42232=AXIS2_PLACEMENT_3D ( 'NONE', #35876, #40546, #6097 ) ;
#42245=VERTEX_POINT ( 'NONE', #29009 ) ;
#42249=CARTESIAN_POINT ( 'NONE',  ( -13.50190746284422794, -17.39609839546894676, 49.52966884056655772 ) ) ;
#42250=DIRECTION ( 'NONE',  ( -3.071710424422018668E-17, 6.404604876783312462E-16, 1.000000000000000000 ) ) ;
#42253=DIRECTION ( 'NONE',  ( 0.9687793358424802159, -0.2479245821708745412, 0.000000000000000000 ) ) ;
#42267=EDGE_LOOP ( 'NONE', ( #32309, #15559, #42096, #42014 ) ) ;
#42270=DIRECTION ( 'NONE',  ( 0.9687793358424819923, -0.2479245821708680464, 0.000000000000000000 ) ) ;
#42274=VECTOR ( 'NONE', #48705, 1000.000000000000000 ) ;
#42275=VERTEX_POINT ( 'NONE', #2664 ) ;
#42295=ORIENTED_EDGE ( 'NONE', *, *, #14715, .F. ) ;
#42301=CIRCLE ( 'NONE', #48581, 4.686499999999998778 ) ;
#42305=DIRECTION ( 'NONE',  ( -3.071710424422018668E-17, 6.404604876783312462E-16, 1.000000000000000000 ) ) ;
#42310=CARTESIAN_POINT ( 'NONE',  ( -21.99019323879806365, -13.75373571565882713, 49.52966884056655772 ) ) ;
#42321=ORIENTED_EDGE ( 'NONE', *, *, #24056, .T. ) ;
#42330=DIRECTION ( 'NONE',  ( -0.9687793358424819923, 0.2479245821708680464, 0.000000000000000000 ) ) ;
#42332=ORIENTED_EDGE ( 'NONE', *, *, #37615, .F. ) ;
#42344=DIRECTION ( 'NONE',  ( -3.071710424422018668E-17, 6.404604876783312462E-16, 1.000000000000000000 ) ) ;
#42348=VERTEX_POINT ( 'NONE', #8087 ) ;
#42350=EDGE_CURVE ( 'NONE', #24257, #3170, #29993, .T. ) ;
#42362=CARTESIAN_POINT ( 'NONE',  ( -17.42409385541299471, -14.80920654474435771, 49.52966884056655772 ) ) ;
#42366=EDGE_CURVE ( 'NONE', #12617, #18903, #48473, .T. ) ;
#42389=CARTESIAN_POINT ( 'NONE',  ( -21.24651499925844078, -18.40803921647045982, 49.52966884056656482 ) ) ;
#42392=CARTESIAN_POINT ( 'NONE',  ( -17.09591293804728807, -10.13421140726271297, 52.02966884056656482 ) ) ;
#42394=CARTESIAN_POINT ( 'NONE',  ( -16.89979169948162863, -10.14008855580012636, 49.52966884056655772 ) ) ;
#42399=CARTESIAN_POINT ( 'NONE',  ( -19.18086540149941399, -19.15397765319887569, 49.52966884056656482 ) ) ;
#42407=VERTEX_POINT ( 'NONE', #4144 ) ;
#42414=CIRCLE ( 'NONE', #43188, 2.000000000000001332 ) ;
#42422=EDGE_CURVE ( 'NONE', #36361, #40825, #23096, .T. ) ;
#42431=CARTESIAN_POINT ( 'NONE',  ( -19.90648311238531676, -10.83415612659009319, 49.52966884056655772 ) ) ;
#42439=DIRECTION ( 'NONE',  ( 0.9687793358424821033, -0.2479245821708680464, 0.000000000000000000 ) ) ;
#42440=DIRECTION ( 'NONE',  ( -3.071710424422018668E-17, 6.404604876783312462E-16, 1.000000000000000000 ) ) ;
#42443=ORIENTED_EDGE ( 'NONE', *, *, #41113, .T. ) ;
#42445=CARTESIAN_POINT ( 'NONE',  ( -15.79771479060332240, -19.20445095063907104, 49.52966884056656482 ) ) ;
#42447=CYLINDRICAL_SURFACE ( 'NONE', #4068, 1.999999999999999112 ) ;
#42459=CARTESIAN_POINT ( 'NONE',  ( -12.74909871793134997, -15.13738746211001462, 49.52966884056655772 ) ) ;
#42460=CARTESIAN_POINT ( 'NONE',  ( -12.43058792219793141, -16.43013174195301218, 52.02966884056656482 ) ) ;
#42463=CYLINDRICAL_SURFACE ( 'NONE', #3172, 2.000000000000000000 ) ;
#42478=VECTOR ( 'NONE', #600, 1000.000000000000000 ) ;
#42480=ORIENTED_EDGE ( 'NONE', *, *, #37978, .F. ) ;
#42488=VECTOR ( 'NONE', #43673, 1000.000000000000000 ) ;
#42495=DIRECTION ( 'NONE',  ( -3.071710424422018668E-17, 6.404604876783312462E-16, 1.000000000000000000 ) ) ;
#42513=VERTEX_POINT ( 'NONE', #42771 ) ;
#42524=ORIENTED_EDGE ( 'NONE', *, *, #27908, .F. ) ;
#42525=CARTESIAN_POINT ( 'NONE',  ( -15.48261606618132546, -10.53062973237824096, 49.52966884056655772 ) ) ;
#42539=DIRECTION ( 'NONE',  ( -0.6380325334150322991, 0.7700094066334487453, 0.000000000000000000 ) ) ;
#42541=EDGE_CURVE ( 'NONE', #40656, #10333, #46706, .T. ) ;
#42560=ORIENTED_EDGE ( 'NONE', *, *, #28952, .F. ) ;
#42564=LINE ( 'NONE', #31945, #1493 ) ;
#42584=CARTESIAN_POINT ( 'NONE',  ( -16.36862302632751209, -10.24310716135927812, 49.52966884056655772 ) ) ;
#42594=AXIS2_PLACEMENT_3D ( 'NONE', #8460, #42691, #12390 ) ;
#42596=DIRECTION ( 'NONE',  ( -3.071710424422018668E-17, 6.404604876783312462E-16, 1.000000000000000000 ) ) ;
#42613=FACE_OUTER_BOUND ( 'NONE', #48218, .T. ) ;
#42614=ORIENTED_EDGE ( 'NONE', *, *, #5015, .F. ) ;
#42616=CIRCLE ( 'NONE', #12723, 5.249999999999998224 ) ;
#42620=CARTESIAN_POINT ( 'NONE',  ( -14.35043204381087101, -18.34698626059704551, 49.52966884056656482 ) ) ;
#42626=ORIENTED_EDGE ( 'NONE', *, *, #28090, .F. ) ;
#42649=CARTESIAN_POINT ( 'NONE',  ( -17.58219478024370730, -20.05682544264154288, 49.52966884056656482 ) ) ;
#42667=VERTEX_POINT ( 'NONE', #9450 ) ;
#42691=DIRECTION ( 'NONE',  ( -3.071710424422018668E-17, 6.404604876783312462E-16, 1.000000000000000000 ) ) ;
#42704=LINE ( 'NONE', #5030, #25871 ) ;
#42711=ORIENTED_EDGE ( 'NONE', *, *, #14804, .F. ) ;
#42730=CYLINDRICAL_SURFACE ( 'NONE', #38316, 2.000000000000001332 ) ;
#42737=CARTESIAN_POINT ( 'NONE',  ( -16.60134452727454146, -19.99433755013348701, 50.77966884056656482 ) ) ;
#42739=CARTESIAN_POINT ( 'NONE',  ( -17.75227477277866939, -19.48420168222600068, 49.52966884056656482 ) ) ;
#42752=ORIENTED_EDGE ( 'NONE', *, *, #37163, .T. ) ;
#42768=EDGE_CURVE ( 'NONE', #38822, #40490, #38263, .T. ) ;
#42771=CARTESIAN_POINT ( 'NONE',  ( -22.67171275331017810, -14.65110561991362559, 49.52966884056655772 ) ) ;
#42773=VECTOR ( 'NONE', #22817, 1000.000000000000000 ) ;
#42795=ORIENTED_EDGE ( 'NONE', *, *, #13139, .T. ) ;
#42799=EDGE_LOOP ( 'NONE', ( #7320, #4478, #32889, #17045 ) ) ;
#42825=ORIENTED_EDGE ( 'NONE', *, *, #5266, .F. ) ;
#42831=VERTEX_POINT ( 'NONE', #8369 ) ;
#42838=EDGE_CURVE ( 'NONE', #27599, #39007, #31228, .T. ) ;
#42843=DIRECTION ( 'NONE',  ( 0.9687793358424821033, -0.2479245821708677133, 0.000000000000000000 ) ) ;
#42844=VERTEX_POINT ( 'NONE', #20429 ) ;
#42857=CARTESIAN_POINT ( 'NONE',  ( -17.42409385541299471, -14.80920654474435594, 52.02966884056656482 ) ) ;
#42859=CARTESIAN_POINT ( 'NONE',  ( -12.88390949798720442, -15.97110509908812936, 49.52966884056655772 ) ) ;
#42867=CYLINDRICAL_SURFACE ( 'NONE', #15453, 1.999999999999999112 ) ;
#42875=ORIENTED_EDGE ( 'NONE', *, *, #12111, .F. ) ;
#42878=AXIS2_PLACEMENT_3D ( 'NONE', #25028, #17619, #35847 ) ;
#42885=ORIENTED_EDGE ( 'NONE', *, *, #7381, .F. ) ;
#42889=CARTESIAN_POINT ( 'NONE',  ( -19.74436319619195501, -10.72363366794506412, 49.52966884056655772 ) ) ;
#42893=EDGE_LOOP ( 'NONE', ( #23247, #5322, #14488, #18462 ) ) ;
#42898=ORIENTED_EDGE ( 'NONE', *, *, #13348, .T. ) ;
#42923=ORIENTED_EDGE ( 'NONE', *, *, #29235, .F. ) ;
#42929=ORIENTED_EDGE ( 'NONE', *, *, #4108, .T. ) ;
#42960=CYLINDRICAL_SURFACE ( 'NONE', #19110, 1.999999999999999556 ) ;
#42968=DIRECTION ( 'NONE',  ( -3.071710424422018668E-17, 6.404604876783312462E-16, 1.000000000000000000 ) ) ;
#42971=AXIS2_PLACEMENT_3D ( 'NONE', #15679, #48694, #208 ) ;
#42972=DIRECTION ( 'NONE',  ( -0.2479245821708777886, -0.9687793358424794388, 0.000000000000000000 ) ) ;
#42981=CYLINDRICAL_SURFACE ( 'NONE', #23541, 2.000000000000003109 ) ;
#42987=DIRECTION ( 'NONE',  ( -0.9687793358424819923, 0.2479245821708680464, 0.000000000000000000 ) ) ;
#42990=CARTESIAN_POINT ( 'NONE',  ( -21.68202464530013529, -12.85132308587069438, 52.02966884056656482 ) ) ;
#42998=ADVANCED_FACE ( 'NONE', ( #26726 ), #34578, .T. ) ;
#43025=FACE_OUTER_BOUND ( 'NONE', #16640, .T. ) ;
#43036=DIRECTION ( 'NONE',  ( -3.071710424422018668E-17, 6.404604876783312462E-16, 1.000000000000000000 ) ) ;
#43037=AXIS2_PLACEMENT_3D ( 'NONE', #41906, #42150, #37707 ) ;
#43050=ORIENTED_EDGE ( 'NONE', *, *, #40239, .T. ) ;
#43054=DIRECTION ( 'NONE',  ( 0.9687793358424821033, -0.2479245821708677133, 0.000000000000000000 ) ) ;
#43057=DIRECTION ( 'NONE',  ( -3.071710424422018668E-17, 6.404604876783312462E-16, 1.000000000000000000 ) ) ;
#43059=ORIENTED_EDGE ( 'NONE', *, *, #24493, .T. ) ;
#43066=AXIS2_PLACEMENT_3D ( 'NONE', #28631, #6222, #3245 ) ;
#43102=DIRECTION ( 'NONE',  ( 0.9687793358424821033, -0.2479245821708677133, 0.000000000000000000 ) ) ;
#43133=AXIS2_PLACEMENT_3D ( 'NONE', #48345, #26435, #41208 ) ;
#43135=CIRCLE ( 'NONE', #11681, 1.999999999999998890 ) ;
#43136=ORIENTED_EDGE ( 'NONE', *, *, #20472, .T. ) ;
#43140=VECTOR ( 'NONE', #19354, 1000.000000000000000 ) ;
#43143=DIRECTION ( 'NONE',  ( -3.071710424422018668E-17, 6.404604876783312462E-16, 1.000000000000000000 ) ) ;
#43162=ORIENTED_EDGE ( 'NONE', *, *, #39545, .F. ) ;
#43167=DIRECTION ( 'NONE',  ( 0.9687793358424822143, -0.2479245821708672415, 0.000000000000000000 ) ) ;
#43178=ADVANCED_FACE ( 'NONE', ( #3026 ), #44415, .T. ) ;
#43181=DIRECTION ( 'NONE',  ( 3.071710424422018668E-17, -6.404604876783312462E-16, -1.000000000000000000 ) ) ;
#43182=AXIS2_PLACEMENT_3D ( 'NONE', #29158, #7497, #40969 ) ;
#43186=DIRECTION ( 'NONE',  ( -3.071710424422018668E-17, 6.404604876783312462E-16, 1.000000000000000000 ) ) ;
#43188=AXIS2_PLACEMENT_3D ( 'NONE', #10653, #309, #14768 ) ;
#43210=ORIENTED_EDGE ( 'NONE', *, *, #31715, .T. ) ;
#43222=CARTESIAN_POINT ( 'NONE',  ( -21.32332200014554857, -12.20934075487643788, 52.02966884056656482 ) ) ;
#43225=FACE_OUTER_BOUND ( 'NONE', #39325, .T. ) ;
#43230=VECTOR ( 'NONE', #46127, 1000.000000000000000 ) ;
#43231=CARTESIAN_POINT ( 'NONE',  ( -22.63183829035100914, -15.47396055967928952, 50.77966884056655772 ) ) ;
#43232=CYLINDRICAL_SURFACE ( 'NONE', #2298, 1.999999999999999112 ) ;
#43235=ORIENTED_EDGE ( 'NONE', *, *, #32277, .T. ) ;
#43236=EDGE_CURVE ( 'NONE', #26989, #21060, #2121, .T. ) ;
#43259=ORIENTED_EDGE ( 'NONE', *, *, #18949, .T. ) ;
#43274=ORIENTED_EDGE ( 'NONE', *, *, #34342, .T. ) ;
#43275=CARTESIAN_POINT ( 'NONE',  ( -17.03931138636480824, -19.49188718695241462, 49.52966884056656482 ) ) ;
#43296=DIRECTION ( 'NONE',  ( -3.071710424422018668E-17, 6.404604876783312462E-16, 1.000000000000000000 ) ) ;
#43299=CIRCLE ( 'NONE', #11057, 4.686499999999998778 ) ;
#43313=EDGE_CURVE ( 'NONE', #19312, #48635, #6052, .T. ) ;
#43323=DIRECTION ( 'NONE',  ( -3.071710424422018668E-17, 6.404604876783312462E-16, 1.000000000000000000 ) ) ;
#43326=CIRCLE ( 'NONE', #29967, 1.999999999999999556 ) ;
#43337=EDGE_LOOP ( 'NONE', ( #48533, #10253, #5914, #23918 ) ) ;
#43349=ORIENTED_EDGE ( 'NONE', *, *, #4934, .T. ) ;
#43357=AXIS2_PLACEMENT_3D ( 'NONE', #30988, #16911, #19664 ) ;
#43367=AXIS2_PLACEMENT_3D ( 'NONE', #29441, #33111, #10256 ) ;
#43371=AXIS2_PLACEMENT_3D ( 'NONE', #46155, #16584, #9219 ) ;
#43375=ORIENTED_EDGE ( 'NONE', *, *, #1774, .F. ) ;
#43376=EDGE_LOOP ( 'NONE', ( #494, #39945, #23309, #34130 ) ) ;
#43378=ORIENTED_EDGE ( 'NONE', *, *, #3307, .F. ) ;
#43388=AXIS2_PLACEMENT_3D ( 'NONE', #116, #14588, #18304 ) ;
#43391=ORIENTED_EDGE ( 'NONE', *, *, #19223, .F. ) ;
#43400=ORIENTED_EDGE ( 'NONE', *, *, #9178, .T. ) ;
#43404=CIRCLE ( 'NONE', #35507, 5.249999999999998224 ) ;
#43407=DIRECTION ( 'NONE',  ( 0.9687793358424817702, -0.2479245821708686570, 0.000000000000000000 ) ) ;
#43415=DIRECTION ( 'NONE',  ( -0.9687793358424819923, 0.2479245821708680464, 0.000000000000000000 ) ) ;
#43418=CARTESIAN_POINT ( 'NONE',  ( -21.00733138479494855, -11.77013360165372013, 49.52966884056655772 ) ) ;
#43426=ORIENTED_EDGE ( 'NONE', *, *, #37266, .T. ) ;
#43432=AXIS2_PLACEMENT_3D ( 'NONE', #6417, #17484, #47307 ) ;
#43437=ORIENTED_EDGE ( 'NONE', *, *, #15861, .T. ) ;
#43452=EDGE_CURVE ( 'NONE', #4090, #13117, #47771, .T. ) ;
#43460=ORIENTED_EDGE ( 'NONE', *, *, #42205, .F. ) ;
#43487=VERTEX_POINT ( 'NONE', #2006 ) ;
#43491=DIRECTION ( 'NONE',  ( 0.9687793358424821033, -0.2479245821708677133, 0.000000000000000000 ) ) ;
#43516=DIRECTION ( 'NONE',  ( -3.071710424422018668E-17, 6.404604876783312462E-16, 1.000000000000000000 ) ) ;
#43517=ORIENTED_EDGE ( 'NONE', *, *, #5999, .T. ) ;
#43518=CARTESIAN_POINT ( 'NONE',  ( -15.61111608319569477, -19.14379616117205885, 52.02966884056656482 ) ) ;
#43519=VERTEX_POINT ( 'NONE', #6909 ) ;
#43616=DIRECTION ( 'NONE',  ( -3.071710424422018668E-17, 6.404604876783312462E-16, 1.000000000000000000 ) ) ;
#43633=ORIENTED_EDGE ( 'NONE', *, *, #44297, .T. ) ;
#43641=CARTESIAN_POINT ( 'NONE',  ( -17.03931138636480824, -19.49188718695241107, 52.02966884056656482 ) ) ;
#43647=DIRECTION ( 'NONE',  ( -0.8603395911234872351, -0.5097212845717460361, 0.000000000000000000 ) ) ;
#43650=AXIS2_PLACEMENT_3D ( 'NONE', #20135, #35142, #39331 ) ;
#43654=DIRECTION ( 'NONE',  ( -3.071710424422018668E-17, 6.404604876783312462E-16, 1.000000000000000000 ) ) ;
#43655=AXIS2_PLACEMENT_3D ( 'NONE', #45517, #4619, #30973 ) ;
#43656=VERTEX_POINT ( 'NONE', #29556 ) ;
#43657=VERTEX_POINT ( 'NONE', #40883 ) ;
#43658=DIRECTION ( 'NONE',  ( -0.2479245821708776221, -0.9687793358424795498, 0.000000000000000000 ) ) ;
#43673=DIRECTION ( 'NONE',  ( -3.071710424422018668E-17, 6.404604876783312462E-16, 1.000000000000000000 ) ) ;
#43694=ORIENTED_EDGE ( 'NONE', *, *, #11522, .F. ) ;
#43698=VERTEX_POINT ( 'NONE', #27573 ) ;
#43711=DIRECTION ( 'NONE',  ( -3.071710424422018668E-17, 6.404604876783312462E-16, 1.000000000000000000 ) ) ;
#43724=CIRCLE ( 'NONE', #4374, 5.249999999999998224 ) ;
#43755=DIRECTION ( 'NONE',  ( 0.9687793358424821033, -0.2479245821708679909, 0.000000000000000000 ) ) ;
#43758=DIRECTION ( 'NONE',  ( 3.071710424422018668E-17, -6.404604876783312462E-16, -1.000000000000000000 ) ) ;
#43773=DIRECTION ( 'NONE',  ( 0.6607190350373965959, 0.7506333037770516192, 0.000000000000000000 ) ) ;
#43774=VERTEX_POINT ( 'NONE', #38650 ) ;
#43788=AXIS2_PLACEMENT_3D ( 'NONE', #19182, #15713, #45792 ) ;
#43789=VECTOR ( 'NONE', #31015, 1000.000000000000000 ) ;
#43806=DIRECTION ( 'NONE',  ( 0.9687793358424821033, -0.2479245821708677133, 0.000000000000000000 ) ) ;
#43811=ADVANCED_FACE ( 'NONE', ( #28780 ), #17679, .T. ) ;
#43817=ORIENTED_EDGE ( 'NONE', *, *, #22792, .T. ) ;
#43822=DIRECTION ( 'NONE',  ( 0.8603395911234834603, 0.5097212845717520313, 0.000000000000000000 ) ) ;
#43826=EDGE_CURVE ( 'NONE', #6783, #22563, #20260, .T. ) ;
#43842=ORIENTED_EDGE ( 'NONE', *, *, #36329, .T. ) ;
#43843=DIRECTION ( 'NONE',  ( -3.071710424422018668E-17, 6.404604876783312462E-16, 1.000000000000000000 ) ) ;
#43854=EDGE_CURVE ( 'NONE', #25404, #7167, #41483, .T. ) ;
#43859=STYLED_ITEM ( 'NONE', ( #33779 ), #14655 ) ;
#43868=VECTOR ( 'NONE', #10208, 1000.000000000000000 ) ;
#43870=ORIENTED_EDGE ( 'NONE', *, *, #37472, .T. ) ;
#43871=CIRCLE ( 'NONE', #21082, 5.249999999999998224 ) ;
#43875=ORIENTED_EDGE ( 'NONE', *, *, #12071, .T. ) ;
#43883=CARTESIAN_POINT ( 'NONE',  ( -13.08950423898529891, -12.99622877252704001, 52.02966884056656482 ) ) ;
#43885=CARTESIAN_POINT ( 'NONE',  ( -17.42409385541299471, -14.80920654474435771, 49.52966884056655772 ) ) ;
#43889=CARTESIAN_POINT ( 'NONE',  ( -17.81160558974998764, -14.71003671187600936, 52.02966884056656482 ) ) ;
#43894=AXIS2_PLACEMENT_3D ( 'NONE', #17397, #31939, #47683 ) ;
#43897=DIRECTION ( 'NONE',  ( -3.071710424422018668E-17, 6.404604876783312462E-16, 1.000000000000000000 ) ) ;
#43901=EDGE_LOOP ( 'NONE', ( #33287, #16788, #43259, #10800 ) ) ;
#43932=VECTOR ( 'NONE', #6020, 1000.000000000000000 ) ;
#43936=VECTOR ( 'NONE', #36530, 1000.000000000000000 ) ;
#43943=EDGE_CURVE ( 'NONE', #24396, #12959, #41568, .T. ) ;
#43954=CARTESIAN_POINT ( 'NONE',  ( -21.50966673221228120, -17.12947588552333045, 49.52966884056655772 ) ) ;
#43960=DIRECTION ( 'NONE',  ( 0.9687793358424819923, -0.2479245821708680464, 0.000000000000000000 ) ) ;
#43973=AXIS2_PLACEMENT_3D ( 'NONE', #13783, #28596, #28359 ) ;
#43975=EDGE_LOOP ( 'NONE', ( #34857, #34544, #38987, #5780 ) ) ;
#43977=CARTESIAN_POINT ( 'NONE',  ( -18.47956468449850931, -19.37530592812942487, 52.02966884056656482 ) ) ;
#43978=CIRCLE ( 'NONE', #44782, 2.000000000000001332 ) ;
#43995=AXIS2_PLACEMENT_3D ( 'NONE', #6816, #10279, #43773 ) ;
#44010=DIRECTION ( 'NONE',  ( -3.071710424422018668E-17, 6.404604876783312462E-16, 1.000000000000000000 ) ) ;
#44016=ORIENTED_EDGE ( 'NONE', *, *, #19779, .T. ) ;
#44025=UNCERTAINTY_MEASURE_WITH_UNIT (LENGTH_MEASURE( 1.000000000000000082E-05 ), #31009, 'distance_accuracy_value', 'NONE');
#44032=VERTEX_POINT ( 'NONE', #26067 ) ;
#44034=DIRECTION ( 'NONE',  ( -3.071710424422018668E-17, 6.404604876783312462E-16, 1.000000000000000000 ) ) ;
#44038=DIRECTION ( 'NONE',  ( 0.9687793358424821033, -0.2479245821708677133, 0.000000000000000000 ) ) ;
#44050=CARTESIAN_POINT ( 'NONE',  ( -13.07710726710083193, -16.59225537930583982, 49.52966884056655772 ) ) ;
#44051=CIRCLE ( 'NONE', #22810, 1.999999999999999556 ) ;
#44056=ADVANCED_FACE ( 'NONE', ( #48451 ), #7850, .T. ) ;
#44059=CIRCLE ( 'NONE', #24394, 4.686499999999998778 ) ;
#44061=DIRECTION ( 'NONE',  ( -3.071710424422018668E-17, 6.404604876783312462E-16, 1.000000000000000000 ) ) ;
#44067=AXIS2_PLACEMENT_3D ( 'NONE', #28667, #2794, #21758 ) ;
#44072=CIRCLE ( 'NONE', #36922, 5.249999999999998224 ) ;
#44074=ORIENTED_EDGE ( 'NONE', *, *, #9498, .T. ) ;
#44081=ORIENTED_EDGE ( 'NONE', *, *, #24633, .F. ) ;
#44082=DIRECTION ( 'NONE',  ( 3.071710424422018668E-17, -6.404604876783312462E-16, -1.000000000000000000 ) ) ;
#44085=DIRECTION ( 'NONE',  ( -3.071710424422018668E-17, 6.404604876783312462E-16, 1.000000000000000000 ) ) ;
#44091=ORIENTED_EDGE ( 'NONE', *, *, #34000, .F. ) ;
#44092=LINE ( 'NONE', #6882, #35340 ) ;
#44123=DIRECTION ( 'NONE',  ( 0.9687793358424821033, -0.2479245821708680464, 0.000000000000000000 ) ) ;
#44148=DIRECTION ( 'NONE',  ( -3.071710424422018668E-17, 6.404604876783312462E-16, 1.000000000000000000 ) ) ;
#44149=EDGE_CURVE ( 'NONE', #20751, #32161, #2945, .T. ) ;
#44155=ORIENTED_EDGE ( 'NONE', *, *, #19631, .F. ) ;
#44160=CARTESIAN_POINT ( 'NONE',  ( -17.07160637253920044, -10.12398423200249553, 52.02966884056656482 ) ) ;
#44171=AXIS2_PLACEMENT_3D ( 'NONE', #8568, #23592, #39074 ) ;
#44187=DIRECTION ( 'NONE',  ( -3.071710424422018668E-17, 6.404604876783312462E-16, 1.000000000000000000 ) ) ;
#44188=VERTEX_POINT ( 'NONE', #31447 ) ;
#44191=AXIS2_PLACEMENT_3D ( 'NONE', #33048, #21518, #48091 ) ;
#44192=DIRECTION ( 'NONE',  ( -0.9687793358424819923, 0.2479245821708680464, 0.000000000000000000 ) ) ;
#44193=VERTEX_POINT ( 'NONE', #23338 ) ;
#44200=CARTESIAN_POINT ( 'NONE',  ( -21.42170527289675164, -17.27794275993632667, 49.52966884056655772 ) ) ;
#44215=ORIENTED_EDGE ( 'NONE', *, *, #11515, .T. ) ;
#44219=VERTEX_POINT ( 'NONE', #933 ) ;
#44234=ORIENTED_EDGE ( 'NONE', *, *, #28952, .T. ) ;
#44239=ORIENTED_EDGE ( 'NONE', *, *, #47184, .T. ) ;
#44241=EDGE_LOOP ( 'NONE', ( #10872, #32590, #44155, #9137 ) ) ;
#44267=ORIENTED_EDGE ( 'NONE', *, *, #22073, .T. ) ;
#44272=VERTEX_POINT ( 'NONE', #32423 ) ;
#44288=CARTESIAN_POINT ( 'NONE',  ( -13.17762867948185601, -11.72213130924974678, 49.52966884056655772 ) ) ;
#44289=ORIENTED_EDGE ( 'NONE', *, *, #36200, .F. ) ;
#44297=EDGE_CURVE ( 'NONE', #19689, #20521, #41528, .T. ) ;
#44298=ORIENTED_EDGE ( 'NONE', *, *, #38227, .T. ) ;
#44338=CARTESIAN_POINT ( 'NONE',  ( -14.33701861991840154, -19.05567172067550530, 52.02966884056656482 ) ) ;
#44342=EDGE_LOOP ( 'NONE', ( #46081, #12221, #25670, #45953 ) ) ;
#44352=CIRCLE ( 'NONE', #37252, 4.686499999999997002 ) ;
#44373=DIRECTION ( 'NONE',  ( 3.071710424422018668E-17, -6.404604876783312462E-16, -1.000000000000000000 ) ) ;
#44378=EDGE_LOOP ( 'NONE', ( #34531, #45641, #4359, #17155 ) ) ;
#44380=CARTESIAN_POINT ( 'NONE',  ( -21.39914427356725213, -17.29159580171668864, 52.02966884056656482 ) ) ;
#44391=VECTOR ( 'NONE', #10573, 1000.000000000000000 ) ;
#44392=FACE_OUTER_BOUND ( 'NONE', #21582, .T. ) ;
#44411=CARTESIAN_POINT ( 'NONE',  ( -17.42409385541299471, -14.80920654474435771, 49.52966884056655772 ) ) ;
#44415=CYLINDRICAL_SURFACE ( 'NONE', #4479, 2.000000000000001332 ) ;
#44418=DIRECTION ( 'NONE',  ( -3.071710424422018668E-17, 6.404604876783312462E-16, 1.000000000000000000 ) ) ;
#44426=DIRECTION ( 'NONE',  ( -3.071710424422018668E-17, 6.404604876783312462E-16, 1.000000000000000000 ) ) ;
#44429=DIRECTION ( 'NONE',  ( 3.071710424422018668E-17, -6.404604876783312462E-16, -1.000000000000000000 ) ) ;
#44441=ORIENTED_EDGE ( 'NONE', *, *, #16347, .F. ) ;
#44443=DIRECTION ( 'NONE',  ( -3.071710424422018668E-17, 6.404604876783312462E-16, 1.000000000000000000 ) ) ;
#44444=DIRECTION ( 'NONE',  ( 0.9979768094191903138, 0.06357898915123821881, 0.000000000000000000 ) ) ;
#44459=CARTESIAN_POINT ( 'NONE',  ( -21.75868347184070473, -16.62218431696164345, 49.52966884056655772 ) ) ;
#44464=CARTESIAN_POINT ( 'NONE',  ( -18.50517187854146783, -19.38160480531894336, 52.02966884056656482 ) ) ;
#44497=EDGE_LOOP ( 'NONE', ( #17071, #31613, #11855, #25045 ) ) ;
#44503=ORIENTED_EDGE ( 'NONE', *, *, #34420, .F. ) ;
#44511=CARTESIAN_POINT ( 'NONE',  ( -13.83484324388145481, -17.82260368047347043, 52.02966884056656482 ) ) ;
#44517=DIRECTION ( 'NONE',  ( -0.9687793358424819923, 0.2479245821708680464, 0.000000000000000000 ) ) ;
#44522=CIRCLE ( 'NONE', #485, 5.249999999999998224 ) ;
#44545=ORIENTED_EDGE ( 'NONE', *, *, #19448, .F. ) ;
#44552=CIRCLE ( 'NONE', #33471, 4.686499999999998778 ) ;
#44564=DIRECTION ( 'NONE',  ( 0.09332174201254204993, 0.9956360040033428449, 0.000000000000000000 ) ) ;
#44565=CYLINDRICAL_SURFACE ( 'NONE', #47321, 2.000000000000003109 ) ;
#44568=DIRECTION ( 'NONE',  ( 0.000000000000000000, 0.000000000000000000, 1.000000000000000000 ) ) ;
#44582=AXIS2_PLACEMENT_3D ( 'NONE', #2561, #32819, #44192 ) ;
#44585=ORIENTED_EDGE ( 'NONE', *, *, #46463, .T. ) ;
#44587=EDGE_CURVE ( 'NONE', #20159, #34400, #46236, .T. ) ;
#44588=AXIS2_PLACEMENT_3D ( 'NONE', #2076, #39267, #1337 ) ;
#44591=VERTEX_POINT ( 'NONE', #26739 ) ;
#44596=ORIENTED_EDGE ( 'NONE', *, *, #31850, .F. ) ;
#44611=DIRECTION ( 'NONE',  ( -0.9687793358424822143, 0.2479245821708672415, 0.000000000000000000 ) ) ;
#44620=CARTESIAN_POINT ( 'NONE',  ( -16.31151605585062825, -19.37404237808139484, 52.02966884056656482 ) ) ;
#44658=AXIS2_PLACEMENT_3D ( 'NONE', #11077, #8358, #45310 ) ;
#44665=DIRECTION ( 'NONE',  ( -3.071710424422018668E-17, 6.404604876783312462E-16, 1.000000000000000000 ) ) ;
#44702=AXIS2_PLACEMENT_3D ( 'NONE', #939, #24321, #23596 ) ;
#44707=CARTESIAN_POINT ( 'NONE',  ( -17.42409385541299471, -14.80920654474434883, 62.02966884056656482 ) ) ;
#44720=CYLINDRICAL_SURFACE ( 'NONE', #47300, 5.249999999999998224 ) ;
#44721=CARTESIAN_POINT ( 'NONE',  ( -17.42409385541299471, -14.80920654474434883, 62.02966884056656482 ) ) ;
#44724=ORIENTED_EDGE ( 'NONE', *, *, #15006, .T. ) ;
#44733=AXIS2_PLACEMENT_3D ( 'NONE', #15947, #39337, #13211 ) ;
#44743=DIRECTION ( 'NONE',  ( 3.071710424422018668E-17, -6.404604876783312462E-16, -1.000000000000000000 ) ) ;
#44749=LINE ( 'NONE', #11481, #43140 ) ;
#44758=CARTESIAN_POINT ( 'NONE',  ( -22.60969001043771698, -13.98939405582217255, 52.02966884056656482 ) ) ;
#44771=CIRCLE ( 'NONE', #40041, 1.999999999999999112 ) ;
#44778=ORIENTED_EDGE ( 'NONE', *, *, #36631, .T. ) ;
#44782=AXIS2_PLACEMENT_3D ( 'NONE', #28380, #40181, #5961 ) ;
#44790=DIRECTION ( 'NONE',  ( -3.071710424422018668E-17, 6.404604876783312462E-16, 1.000000000000000000 ) ) ;
#44800=CARTESIAN_POINT ( 'NONE',  ( -22.67171275331017810, -14.65110561991362381, 50.77966884056655772 ) ) ;
#44801=DIRECTION ( 'NONE',  ( -0.9294853595766571219, -0.3688590060343552857, 0.000000000000000000 ) ) ;
#44807=EDGE_CURVE ( 'NONE', #11839, #27248, #34403, .T. ) ;
#44810=VERTEX_POINT ( 'NONE', #41379 ) ;
#44816=CIRCLE ( 'NONE', #32960, 5.249999999999998224 ) ;
#44822=CARTESIAN_POINT ( 'NONE',  ( -17.75227477277866939, -19.48420168222600068, 49.52966884056656482 ) ) ;
#44824=CARTESIAN_POINT ( 'NONE',  ( -19.66559402580761784, -10.06176755239059695, 52.02966884056656482 ) ) ;
#44831=CARTESIAN_POINT ( 'NONE',  ( -21.13535303541994281, -18.52256826949110646, 50.77966884056655772 ) ) ;
#44833=DIRECTION ( 'NONE',  ( -0.9687793358424819923, 0.2479245821708680464, 0.000000000000000000 ) ) ;
#44846=ORIENTED_EDGE ( 'NONE', *, *, #41314, .T. ) ;
#44861=DIRECTION ( 'NONE',  ( -3.071710424422018668E-17, 6.404604876783312462E-16, 1.000000000000000000 ) ) ;
#44867=VERTEX_POINT ( 'NONE', #33733 ) ;
#44878=EDGE_CURVE ( 'NONE', #7346, #38535, #611, .T. ) ;
#44881=FACE_OUTER_BOUND ( 'NONE', #31416, .T. ) ;
#44907=CIRCLE ( 'NONE', #33877, 5.249999999999998224 ) ;
#44910=ORIENTED_EDGE ( 'NONE', *, *, #27926, .T. ) ;
#44917=DIRECTION ( 'NONE',  ( 0.9687793358424821033, -0.2479245821708679909, 0.000000000000000000 ) ) ;
#44926=EDGE_LOOP ( 'NONE', ( #21312, #11195, #12848, #27211 ) ) ;
#44929=EDGE_CURVE ( 'NONE', #20972, #40656, #32071, .T. ) ;
#44931=CARTESIAN_POINT ( 'NONE',  ( -21.76886496386750736, -13.05243499865792067, 49.52966884056655772 ) ) ;
#44940=DIRECTION ( 'NONE',  ( -3.071710424422018668E-17, 6.404604876783312462E-16, 1.000000000000000000 ) ) ;
#44944=CARTESIAN_POINT ( 'NONE',  ( -17.42409385541299471, -14.80920654474435594, 52.02966884056656482 ) ) ;
#44951=CARTESIAN_POINT ( 'NONE',  ( -21.76243611580424897, -17.76577320756515022, 52.02966884056656482 ) ) ;
#44963=EDGE_CURVE ( 'NONE', #45424, #39489, #35675, .T. ) ;
#44967=LINE ( 'NONE', #41007, #4189 ) ;
#44983=DIRECTION ( 'NONE',  ( 0.9757441136919974278, 0.2189141945955501434, 0.000000000000000000 ) ) ;
#44993=EDGE_CURVE ( 'NONE', #36884, #16630, #11641, .T. ) ;
#45001=CARTESIAN_POINT ( 'NONE',  ( -15.48261606618132546, -10.53062973237824096, 49.52966884056655772 ) ) ;
#45027=EDGE_CURVE ( 'NONE', #41560, #17399, #13745, .T. ) ;
#45057=CARTESIAN_POINT ( 'NONE',  ( -21.99649211598757859, -13.72812852161587038, 49.52966884056655772 ) ) ;
#45078=DIRECTION ( 'NONE',  ( -3.071710424422018668E-17, 6.404604876783312462E-16, 1.000000000000000000 ) ) ;
#45089=EDGE_CURVE ( 'NONE', #25765, #39405, #25805, .T. ) ;
#45101=EDGE_CURVE ( 'NONE', #19390, #9114, #29752, .T. ) ;
#45102=CIRCLE ( 'NONE', #16768, 4.686499999999999666 ) ;
#45113=CARTESIAN_POINT ( 'NONE',  ( -17.42409385541299471, -14.80920654474435594, 52.02966884056656482 ) ) ;
#45116=VERTEX_POINT ( 'NONE', #41577 ) ;
#45121=DIRECTION ( 'NONE',  ( 0.9687793358424821033, -0.2479245821708679909, 0.000000000000000000 ) ) ;
#45122=CARTESIAN_POINT ( 'NONE',  ( -12.74909871793134997, -15.13738746211001285, 52.02966884056656482 ) ) ;
#45140=ORIENTED_EDGE ( 'NONE', *, *, #34363, .F. ) ;
#45141=ORIENTED_EDGE ( 'NONE', *, *, #25022, .F. ) ;
#45143=ORIENTED_EDGE ( 'NONE', *, *, #25441, .F. ) ;
#45155=VERTEX_POINT ( 'NONE', #48461 ) ;
#45156=CARTESIAN_POINT ( 'NONE',  ( -17.09591293804728807, -10.13421140726271297, 49.52966884056655772 ) ) ;
#45160=CYLINDRICAL_SURFACE ( 'NONE', #21304, 1.999999999999999556 ) ;
#45166=EDGE_CURVE ( 'NONE', #15515, #16073, #14763, .T. ) ;
#45173=CYLINDRICAL_SURFACE ( 'NONE', #47077, 1.999999999999999556 ) ;
#45178=ORIENTED_EDGE ( 'NONE', *, *, #16958, .F. ) ;
#45184=ORIENTED_EDGE ( 'NONE', *, *, #38937, .T. ) ;
#45198=CARTESIAN_POINT ( 'NONE',  ( -17.42409385541299471, -14.80920654474435771, 49.52966884056655772 ) ) ;
#45213=DIRECTION ( 'NONE',  ( 0.7700094066334511878, 0.6380325334150290795, 0.000000000000000000 ) ) ;
#45235=CARTESIAN_POINT ( 'NONE',  ( -19.20714268997449281, -19.15619313305651161, 52.02966884056656482 ) ) ;
#45247=EDGE_LOOP ( 'NONE', ( #23285, #31950, #34615, #41216 ) ) ;
#45253=CARTESIAN_POINT ( 'NONE',  ( -14.90085577400961014, -10.20532018813695707, 50.77966884056655772 ) ) ;
#45254=DIRECTION ( 'NONE',  ( -3.071710424422018668E-17, 6.404604876783312462E-16, 1.000000000000000000 ) ) ;
#45264=ORIENTED_EDGE ( 'NONE', *, *, #13543, .T. ) ;
#45274=ORIENTED_EDGE ( 'NONE', *, *, #6819, .T. ) ;
#45281=VERTEX_POINT ( 'NONE', #8830 ) ;
#45294=ADVANCED_FACE ( 'NONE', ( #43025 ), #23348, .T. ) ;
#45297=EDGE_CURVE ( 'NONE', #33361, #45116, #17949, .T. ) ;
#45299=ORIENTED_EDGE ( 'NONE', *, *, #31847, .T. ) ;
#45300=VERTEX_POINT ( 'NONE', #38843 ) ;
#45307=CARTESIAN_POINT ( 'NONE',  ( -21.02292652713908794, -10.98678540089889921, 49.52966884056655772 ) ) ;
#45310=DIRECTION ( 'NONE',  ( 0.9687793358424819923, -0.2479245821708678243, 0.000000000000000000 ) ) ;
#45312=FACE_OUTER_BOUND ( 'NONE', #6533, .T. ) ;
#45315=EDGE_CURVE ( 'NONE', #19053, #30371, #5366, .T. ) ;
#45319=CARTESIAN_POINT ( 'NONE',  ( -19.80886856394220175, -10.13209743873032131, 50.77966884056655772 ) ) ;
#45330=AXIS2_PLACEMENT_3D ( 'NONE', #29744, #29258, #10545 ) ;
#45344=DIRECTION ( 'NONE',  ( 0.9687793358424817702, -0.2479245821708686570, 0.000000000000000000 ) ) ;
#45359=CARTESIAN_POINT ( 'NONE',  ( -13.44904343725875862, -12.32681728777199304, 52.02966884056656482 ) ) ;
#45362=LINE ( 'NONE', #8412, #40669 ) ;
#45363=DIRECTION ( 'NONE',  ( 3.071710424422018668E-17, -6.404604876783312462E-16, -1.000000000000000000 ) ) ;
#45371=SURFACE_STYLE_USAGE ( .BOTH. , #18769 ) ;
#45375=CARTESIAN_POINT ( 'NONE',  ( -22.58237342315448615, -13.83214364962418053, 50.77966884056655772 ) ) ;
#45376=AXIS2_PLACEMENT_3D ( 'NONE', #24818, #17157, #1682 ) ;
#45386=CARTESIAN_POINT ( 'NONE',  ( -17.42409385541299471, -14.80920654474435771, 49.52966884056655772 ) ) ;
#45393=DIRECTION ( 'NONE',  ( 3.071710424422018668E-17, -6.404604876783312462E-16, -1.000000000000000000 ) ) ;
#45395=EDGE_CURVE ( 'NONE', #33399, #31657, #17134, .T. ) ;
#45402=AXIS2_PLACEMENT_3D ( 'NONE', #25002, #40269, #35823 ) ;
#45406=CARTESIAN_POINT ( 'NONE',  ( -17.42409385541299471, -14.80920654474434883, 62.02966884056656482 ) ) ;
#45410=CARTESIAN_POINT ( 'NONE',  ( -15.59410181515468530, -19.12364873146921695, 52.02966884056656482 ) ) ;
#45411=CARTESIAN_POINT ( 'NONE',  ( -17.42409385541299471, -14.80920654474435594, 52.02966884056656482 ) ) ;
#45424=VERTEX_POINT ( 'NONE', #2139 ) ;
#45428=LINE ( 'NONE', #42459, #27956 ) ;
#45441=CYLINDRICAL_SURFACE ( 'NONE', #4876, 4.686499999999997002 ) ;
#45449=DIRECTION ( 'NONE',  ( -3.071710424422018668E-17, 6.404604876783312462E-16, 1.000000000000000000 ) ) ;
#45451=ORIENTED_EDGE ( 'NONE', *, *, #7848, .T. ) ;
#45455=EDGE_CURVE ( 'NONE', #40490, #15483, #15558, .T. ) ;
#45461=CARTESIAN_POINT ( 'NONE',  ( -19.71801720247071543, -10.72249662993226060, 49.52966884056655772 ) ) ;
#45465=DIRECTION ( 'NONE',  ( -3.071710424422018668E-17, 6.404604876783312462E-16, 1.000000000000000000 ) ) ;
#45477=CIRCLE ( 'NONE', #46278, 2.000000000000001332 ) ;
#45500=ORIENTED_EDGE ( 'NONE', *, *, #25907, .T. ) ;
#45517=CARTESIAN_POINT ( 'NONE',  ( -16.89979169948162863, -10.14008855580012636, 49.52966884056655772 ) ) ;
#45520=CARTESIAN_POINT ( 'NONE',  ( -13.10965166868813903, -12.97921450448603409, 49.52966884056655772 ) ) ;
#45523=DIRECTION ( 'NONE',  ( -3.071710424422018668E-17, 6.404604876783312462E-16, 1.000000000000000000 ) ) ;
#45526=ORIENTED_EDGE ( 'NONE', *, *, #22857, .T. ) ;
#45528=DIRECTION ( 'NONE',  ( -3.071710424422018668E-17, 6.404604876783312462E-16, 1.000000000000000000 ) ) ;
#45531=CARTESIAN_POINT ( 'NONE',  ( -14.96223302779666398, -10.63593772014186101, 49.52966884056655772 ) ) ;
#45533=VERTEX_POINT ( 'NONE', #18600 ) ;
#45543=CARTESIAN_POINT ( 'NONE',  ( -18.40115675053315059, -19.96748611248585448, 52.02966884056656482 ) ) ;
#45545=CIRCLE ( 'NONE', #21138, 1.999999999999999334 ) ;
#45552=AXIS2_PLACEMENT_3D ( 'NONE', #5943, #2239, #24899 ) ;
#45570=VERTEX_POINT ( 'NONE', #23061 ) ;
#45580=AXIS2_PLACEMENT_3D ( 'NONE', #10639, #33755, #37441 ) ;
#45586=AXIS2_PLACEMENT_3D ( 'NONE', #1006, #15270, #45344 ) ;
#45592=DIRECTION ( 'NONE',  ( -3.071710424422018668E-17, 6.404604876783312462E-16, 1.000000000000000000 ) ) ;
#45616=CARTESIAN_POINT ( 'NONE',  ( -15.61111608319569477, -19.14379616117205885, 49.52966884056656482 ) ) ;
#45620=AXIS2_PLACEMENT_3D ( 'NONE', #19941, #20672, #743 ) ;
#45621=DIRECTION ( 'NONE',  ( 3.071710424422018668E-17, -6.404604876783312462E-16, -1.000000000000000000 ) ) ;
#45637=AXIS2_PLACEMENT_3D ( 'NONE', #2809, #38852, #21306 ) ;
#45641=ORIENTED_EDGE ( 'NONE', *, *, #6855, .F. ) ;
#45644=VERTEX_POINT ( 'NONE', #1351 ) ;
#45647=FACE_OUTER_BOUND ( 'NONE', #423, .T. ) ;
#45654=AXIS2_PLACEMENT_3D ( 'NONE', #4688, #19710, #46551 ) ;
#45661=DIRECTION ( 'NONE',  ( -3.071710424422018668E-17, 6.404604876783312462E-16, 1.000000000000000000 ) ) ;
#45662=DIRECTION ( 'NONE',  ( 0.9687793358424819923, -0.2479245821708680464, 0.000000000000000000 ) ) ;
#45664=EDGE_CURVE ( 'NONE', #30036, #42348, #34847, .T. ) ;
#45690=CYLINDRICAL_SURFACE ( 'NONE', #15857, 2.000000000000001332 ) ;
#45691=ADVANCED_FACE ( 'NONE', ( #24029 ), #1605, .T. ) ;
#45700=DIRECTION ( 'NONE',  ( -3.071710424422018668E-17, 6.404604876783312462E-16, 1.000000000000000000 ) ) ;
#45704=AXIS2_PLACEMENT_3D ( 'NONE', #25392, #45523, #11778 ) ;
#45706=ORIENTED_EDGE ( 'NONE', *, *, #34258, .F. ) ;
#45709=EDGE_CURVE ( 'NONE', #35450, #3087, #19517, .T. ) ;
#45719=ORIENTED_EDGE ( 'NONE', *, *, #19122, .F. ) ;
#45723=ADVANCED_FACE ( 'NONE', ( #9966 ), #2087, .T. ) ;
#45725=CIRCLE ( 'NONE', #4827, 2.000000000000000000 ) ;
#45736=ORIENTED_EDGE ( 'NONE', *, *, #10973, .F. ) ;
#45740=CARTESIAN_POINT ( 'NONE',  ( -21.77108044372514684, -13.02615771018284541, 49.52966884056655772 ) ) ;
#45750=CARTESIAN_POINT ( 'NONE',  ( -13.42648243792925555, -12.34047032955235501, 52.02966884056656482 ) ) ;
#45762=LINE ( 'NONE', #15429, #47669 ) ;
#45764=ADVANCED_FACE ( 'NONE', ( #43225 ), #24268, .T. ) ;
#45765=ORIENTED_EDGE ( 'NONE', *, *, #41925, .T. ) ;
#45768=ADVANCED_FACE ( 'NONE', ( #35808 ), #46909, .T. ) ;
#45778=AXIS2_PLACEMENT_3D ( 'NONE', #15822, #30385, #19284 ) ;
#45779=DIRECTION ( 'NONE',  ( -3.071710424422018668E-17, 6.404604876783312462E-16, 1.000000000000000000 ) ) ;
#45789=ORIENTED_EDGE ( 'NONE', *, *, #40542, .F. ) ;
#45790=CIRCLE ( 'NONE', #27673, 1.999999999999999112 ) ;
#45792=DIRECTION ( 'NONE',  ( 0.9687793358424822143, -0.2479245821708672415, 0.000000000000000000 ) ) ;
#45794=DIRECTION ( 'NONE',  ( -3.071710424422018668E-17, 6.404604876783312462E-16, 1.000000000000000000 ) ) ;
#45802=DIRECTION ( 'NONE',  ( -3.071710424422018668E-17, 6.404604876783312462E-16, 1.000000000000000000 ) ) ;
#45811=EDGE_CURVE ( 'NONE', #45533, #25725, #39243, .T. ) ;
#45813=CYLINDRICAL_SURFACE ( 'NONE', #7079, 1.999999999999999556 ) ;
#45824=CARTESIAN_POINT ( 'NONE',  ( -17.42409385541299471, -14.80920654474435771, 49.52966884056655772 ) ) ;
#45827=CARTESIAN_POINT ( 'NONE',  ( -17.42409385541299471, -14.80920654474435771, 49.52966884056655772 ) ) ;
#45833=CARTESIAN_POINT ( 'NONE',  ( -17.42409385541299471, -14.80920654474435771, 49.52966884056655772 ) ) ;
#45849=LINE ( 'NONE', #40919, #17605 ) ;
#45852=ORIENTED_EDGE ( 'NONE', *, *, #16333, .T. ) ;
#45854=EDGE_CURVE ( 'NONE', #41721, #27154, #3058, .T. ) ;
#45860=VERTEX_POINT ( 'NONE', #27626 ) ;
#45865=DIRECTION ( 'NONE',  ( -3.071710424422018668E-17, 6.404604876783312462E-16, 1.000000000000000000 ) ) ;
#45870=VECTOR ( 'NONE', #44665, 1000.000000000000000 ) ;
#45875=DIRECTION ( 'NONE',  ( -3.071710424422018668E-17, 6.404604876783312462E-16, 1.000000000000000000 ) ) ;
#45878=FACE_OUTER_BOUND ( 'NONE', #17700, .T. ) ;
#45894=CARTESIAN_POINT ( 'NONE',  ( -19.38197731428664028, -19.06713733463150007, 49.52966884056656482 ) ) ;
#45908=CIRCLE ( 'NONE', #24670, 1.999999999999999778 ) ;
#45920=FACE_OUTER_BOUND ( 'NONE', #40565, .T. ) ;
#45933=CIRCLE ( 'NONE', #24716, 4.686499999999999666 ) ;
#45944=SHAPE_DEFINITION_REPRESENTATION ( #34663, #2486 ) ;
#45953=ORIENTED_EDGE ( 'NONE', *, *, #36235, .F. ) ;
#45968=EDGE_CURVE ( 'NONE', #26266, #17919, #22734, .T. ) ;
#45971=CIRCLE ( 'NONE', #8996, 4.686499999999998778 ) ;
#45986=CYLINDRICAL_SURFACE ( 'NONE', #4485, 4.686499999999997002 ) ;
#45998=VECTOR ( 'NONE', #34432, 1000.000000000000000 ) ;
#46001=ORIENTED_EDGE ( 'NONE', *, *, #34953, .T. ) ;
#46004=CIRCLE ( 'NONE', #2747, 2.000000000000000000 ) ;
#46010=ADVANCED_FACE ( 'NONE', ( #16995 ), #32044, .T. ) ;
#46016=EDGE_CURVE ( 'NONE', #34094, #25136, #7801, .T. ) ;
#46029=( NAMED_UNIT ( * ) SI_UNIT ( $, .STERADIAN. ) SOLID_ANGLE_UNIT ( ) );
#46032=DIRECTION ( 'NONE',  ( -0.6607190350374015919, -0.7506333037770474004, 0.000000000000000000 ) ) ;
#46040=LINE ( 'NONE', #12296, #25666 ) ;
#46041=EDGE_CURVE ( 'NONE', #45281, #15441, #5436, .T. ) ;
#46044=DIRECTION ( 'NONE',  ( -3.071710424422018668E-17, 6.404604876783312462E-16, 1.000000000000000000 ) ) ;
#46069=ORIENTED_EDGE ( 'NONE', *, *, #31293, .T. ) ;
#46079=CARTESIAN_POINT ( 'NONE',  ( -17.42409385541299471, -14.80920654474434883, 62.02966884056656482 ) ) ;
#46081=ORIENTED_EDGE ( 'NONE', *, *, #28530, .F. ) ;
#46086=DIRECTION ( 'NONE',  ( 0.9687793358424821033, -0.2479245821708679909, 0.000000000000000000 ) ) ;
#46089=ORIENTED_EDGE ( 'NONE', *, *, #14834, .F. ) ;
#46109=ORIENTED_EDGE ( 'NONE', *, *, #21294, .T. ) ;
#46123=CARTESIAN_POINT ( 'NONE',  ( -17.42409385541299471, -14.80920654474435771, 49.52966884056655772 ) ) ;
#46124=CARTESIAN_POINT ( 'NONE',  ( -12.26581428767149795, -15.78626943986449405, 52.02966884056656482 ) ) ;
#46127=DIRECTION ( 'NONE',  ( -3.071710424422018668E-17, 6.404604876783312462E-16, 1.000000000000000000 ) ) ;
#46134=ORIENTED_EDGE ( 'NONE', *, *, #18753, .T. ) ;
#46154=EDGE_CURVE ( 'NONE', #44219, #28192, #33694, .T. ) ;
#46155=CARTESIAN_POINT ( 'NONE',  ( -17.42409385541299471, -14.80920654474435771, 49.52966884056655772 ) ) ;
#46162=ADVANCED_FACE ( 'NONE', ( #41948 ), #45173, .T. ) ;
#46165=CIRCLE ( 'NONE', #45402, 2.000000000000001776 ) ;
#46170=EDGE_CURVE ( 'NONE', #8953, #37481, #46314, .T. ) ;
#46236=CIRCLE ( 'NONE', #25008, 5.249999999999998224 ) ;
#46240=EDGE_CURVE ( 'NONE', #27154, #45533, #34478, .T. ) ;
#46246=CYLINDRICAL_SURFACE ( 'NONE', #39249, 4.686499999999997002 ) ;
#46278=AXIS2_PLACEMENT_3D ( 'NONE', #24028, #35082, #1346 ) ;
#46293=DIRECTION ( 'NONE',  ( -0.7506333037770538397, 0.6607190350373941534, 0.000000000000000000 ) ) ;
#46303=EDGE_CURVE ( 'NONE', #36695, #15426, #21904, .T. ) ;
#46312=CYLINDRICAL_SURFACE ( 'NONE', #12152, 5.249999999999998224 ) ;
#46314=CIRCLE ( 'NONE', #35296, 1.999999999999999334 ) ;
#46326=DIRECTION ( 'NONE',  ( -3.071710424422018668E-17, 6.404604876783312462E-16, 1.000000000000000000 ) ) ;
#46342=AXIS2_PLACEMENT_3D ( 'NONE', #21424, #36406, #32491 ) ;
#46369=CARTESIAN_POINT ( 'NONE',  ( -17.42409385541299471, -14.80920654474435771, 49.52966884056655772 ) ) ;
#46371=CARTESIAN_POINT ( 'NONE',  ( -15.00927913818083859, -10.79274639537912783, 49.52966884056655772 ) ) ;
#46377=CARTESIAN_POINT ( 'NONE',  ( -17.42409385541299471, -14.80920654474434883, 62.02966884056656482 ) ) ;
#46380=DIRECTION ( 'NONE',  ( 0.9687793358424817702, -0.2479245821708686570, 0.000000000000000000 ) ) ;
#46388=VECTOR ( 'NONE', #2458, 1000.000000000000000 ) ;
#46393=VECTOR ( 'NONE', #35535, 1000.000000000000000 ) ;
#46395=CYLINDRICAL_SURFACE ( 'NONE', #32414, 4.686499999999997002 ) ;
#46408=VERTEX_POINT ( 'NONE', #46371 ) ;
#46427=ORIENTED_EDGE ( 'NONE', *, *, #47501, .F. ) ;
#46430=DIRECTION ( 'NONE',  ( 0.8603395911234834603, 0.5097212845717522534, 0.000000000000000000 ) ) ;
#46449=AXIS2_PLACEMENT_3D ( 'NONE', #43518, #43758, #39807 ) ;
#46458=EDGE_CURVE ( 'NONE', #1265, #41721, #31399, .T. ) ;
#46459=ORIENTED_EDGE ( 'NONE', *, *, #27817, .F. ) ;
#46462=EDGE_CURVE ( 'NONE', #22244, #35282, #47120, .T. ) ;
#46463=EDGE_CURVE ( 'NONE', #37281, #47436, #47914, .T. ) ;
#46472=AXIS2_PLACEMENT_3D ( 'NONE', #12849, #38955, #20499 ) ;
#46476=CARTESIAN_POINT ( 'NONE',  ( -15.48261606618132546, -10.53062973237823918, 52.02966884056656482 ) ) ;
#46482=CIRCLE ( 'NONE', #25249, 2.000000000000001332 ) ;
#46500=CARTESIAN_POINT ( 'NONE',  ( -22.41668094288463919, -16.43295965837073780, 52.02966884056656482 ) ) ;
#46501=VECTOR ( 'NONE', #25486, 1000.000000000000000 ) ;
#46527=DIRECTION ( 'NONE',  ( -3.071710424422018668E-17, 6.404604876783312462E-16, 1.000000000000000000 ) ) ;
#46531=ADVANCED_FACE ( 'NONE', ( #3235 ), #47808, .T. ) ;
#46551=DIRECTION ( 'NONE',  ( 0.9687793358424821033, -0.2479245821708680464, 0.000000000000000000 ) ) ;
#46591=CARTESIAN_POINT ( 'NONE',  ( -17.83128375312269753, -10.14042954887026049, 49.52966884056655772 ) ) ;
#46592=ADVANCED_FACE ( 'NONE', ( #26373 ), #11119, .T. ) ;
#46594=ADVANCED_FACE ( 'NONE', ( #7928 ), #22692, .T. ) ;
#46599=ORIENTED_EDGE ( 'NONE', *, *, #19708, .F. ) ;
#46628=CARTESIAN_POINT ( 'NONE',  ( -12.21634942047498384, -14.14445252980938861, 49.52966884056655772 ) ) ;
#46660=ORIENTED_EDGE ( 'NONE', *, *, #47184, .F. ) ;
#46662=DIRECTION ( 'NONE',  ( 0.09332174201254196666, 0.9956360040033428449, 0.000000000000000000 ) ) ;
#46669=DIRECTION ( 'NONE',  ( -3.071710424422018668E-17, 6.404604876783312462E-16, 1.000000000000000000 ) ) ;
#46671=DIRECTION ( 'NONE',  ( -3.071710424422018668E-17, 6.404604876783312462E-16, 1.000000000000000000 ) ) ;
#46672=LINE ( 'NONE', #5068, #38377 ) ;
#46673=DIRECTION ( 'NONE',  ( -3.071710424422018668E-17, 6.404604876783312462E-16, 1.000000000000000000 ) ) ;
#46680=EDGE_CURVE ( 'NONE', #47436, #15459, #36893, .T. ) ;
#46688=DIRECTION ( 'NONE',  ( 3.071710424422018668E-17, -6.404604876783312462E-16, -1.000000000000000000 ) ) ;
#46706=LINE ( 'NONE', #24303, #21770 ) ;
#46715=DIRECTION ( 'NONE',  ( 0.9687793358424821033, -0.2479245821708677133, 0.000000000000000000 ) ) ;
#46721=DIRECTION ( 'NONE',  ( 0.9687793358424821033, -0.2479245821708679909, 0.000000000000000000 ) ) ;
#46724=ADVANCED_FACE ( 'NONE', ( #38670 ), #39640, .T. ) ;
#46733=FACE_OUTER_BOUND ( 'NONE', #32347, .T. ) ;
#46738=EDGE_LOOP ( 'NONE', ( #33751, #3438, #43694, #33646 ) ) ;
#46739=CARTESIAN_POINT ( 'NONE',  ( -17.42409385541299471, -14.80920654474435771, 49.52966884056655772 ) ) ;
#46740=VECTOR ( 'NONE', #4062, 1000.000000000000000 ) ;
#46743=ORIENTED_EDGE ( 'NONE', *, *, #40033, .T. ) ;
#46754=VERTEX_POINT ( 'NONE', #34966 ) ;
#46759=FACE_OUTER_BOUND ( 'NONE', #18438, .T. ) ;
#46764=EDGE_CURVE ( 'NONE', #47392, #42844, #18021, .T. ) ;
#46766=FACE_OUTER_BOUND ( 'NONE', #17674, .T. ) ;
#46771=CIRCLE ( 'NONE', #25529, 5.249999999999998224 ) ;
#46781=EDGE_CURVE ( 'NONE', #22937, #3266, #3086, .T. ) ;
#46807=CIRCLE ( 'NONE', #35783, 2.000000000000001332 ) ;
#46808=EDGE_LOOP ( 'NONE', ( #15058, #48621, #38555, #18347 ) ) ;
#46811=AXIS2_PLACEMENT_3D ( 'NONE', #6878, #34858, #23555 ) ;
#46824=ORIENTED_EDGE ( 'NONE', *, *, #43943, .T. ) ;
#46838=EDGE_CURVE ( 'NONE', #23803, #8529, #16450, .T. ) ;
#46841=CYLINDRICAL_SURFACE ( 'NONE', #23439, 5.249999999999998224 ) ;
#46843=CARTESIAN_POINT ( 'NONE',  ( -13.14551704304688684, -16.75068433397604295, 49.52966884056655772 ) ) ;
#46857=DIRECTION ( 'NONE',  ( 3.071710424422018668E-17, -6.404604876783312462E-16, -1.000000000000000000 ) ) ;
#46869=EDGE_CURVE ( 'NONE', #44032, #10945, #1516, .T. ) ;
#46882=DIRECTION ( 'NONE',  ( 3.071710424422018668E-17, -6.404604876783312462E-16, -1.000000000000000000 ) ) ;
#46909=CYLINDRICAL_SURFACE ( 'NONE', #14803, 4.686499999999997002 ) ;
#46917=CARTESIAN_POINT ( 'NONE',  ( -19.20714268997449281, -19.15619313305651161, 49.52966884056656482 ) ) ;
#46919=DIRECTION ( 'NONE',  ( -3.071710424422018668E-17, 6.404604876783312462E-16, 1.000000000000000000 ) ) ;
#46925=CARTESIAN_POINT ( 'NONE',  ( -21.76243611580424897, -17.76577320756515022, 49.52966884056655772 ) ) ;
#46938=DIRECTION ( 'NONE',  ( -3.071710424422018668E-17, 6.404604876783312462E-16, 1.000000000000000000 ) ) ;
#46960=DIRECTION ( 'NONE',  ( 0.9687793358424821033, -0.2479245821708680464, 0.000000000000000000 ) ) ;
#46966=ORIENTED_EDGE ( 'NONE', *, *, #44929, .T. ) ;
#46976=AXIS2_PLACEMENT_3D ( 'NONE', #20241, #45875, #1525 ) ;
#46994=EDGE_LOOP ( 'NONE', ( #5139, #3456, #28747, #45274 ) ) ;
#47006=DIRECTION ( 'NONE',  ( -0.9687793358424817702, 0.2479245821708684905, 0.000000000000000000 ) ) ;
#47016=ORIENTED_EDGE ( 'NONE', *, *, #3307, .T. ) ;
#47023=ORIENTED_EDGE ( 'NONE', *, *, #42062, .T. ) ;
#47027=ADVANCED_FACE ( 'NONE', ( #17348 ), #43232, .T. ) ;
#47028=CARTESIAN_POINT ( 'NONE',  ( -17.42409385541299471, -14.80920654474435771, 49.52966884056655772 ) ) ;
#47036=AXIS2_PLACEMENT_3D ( 'NONE', #42362, #25282, #17861 ) ;
#47042=CIRCLE ( 'NONE', #16375, 4.686499999999998778 ) ;
#47043=CARTESIAN_POINT ( 'NONE',  ( -17.42409385541299471, -14.80920654474435771, 49.52966884056655772 ) ) ;
#47046=AXIS2_PLACEMENT_3D ( 'NONE', #36296, #43711, #9499 ) ;
#47055=ADVANCED_FACE ( 'NONE', ( #27953 ), #42981, .T. ) ;
#47056=VERTEX_POINT ( 'NONE', #20584 ) ;
#47065=CARTESIAN_POINT ( 'NONE',  ( -21.70267066777908838, -12.86772875551264050, 49.52966884056655772 ) ) ;
#47077=AXIS2_PLACEMENT_3D ( 'NONE', #26687, #12382, #45662 ) ;
#47082=ORIENTED_EDGE ( 'NONE', *, *, #15123, .T. ) ;
#47088=CARTESIAN_POINT ( 'NONE',  ( -15.18259368501833961, -19.55664553709809894, 49.52966884056656482 ) ) ;
#47091=DIRECTION ( 'NONE',  ( -0.9687793358424819923, 0.2479245821708680464, 0.000000000000000000 ) ) ;
#47092=LINE ( 'NONE', #13333, #18732 ) ;
#47102=DIRECTION ( 'NONE',  ( 3.071710424422018668E-17, -6.404604876783312462E-16, -1.000000000000000000 ) ) ;
#47120=CIRCLE ( 'NONE', #21177, 1.999999999999999112 ) ;
#47124=EDGE_CURVE ( 'NONE', #6337, #22785, #3546, .T. ) ;
#47138=ORIENTED_EDGE ( 'NONE', *, *, #25170, .T. ) ;
#47143=CARTESIAN_POINT ( 'NONE',  ( -12.85799447202792045, -15.86467737382985277, 52.02966884056656482 ) ) ;
#47163=CIRCLE ( 'NONE', #18824, 2.000000000000000000 ) ;
#47176=ORIENTED_EDGE ( 'NONE', *, *, #15990, .F. ) ;
#47178=EDGE_CURVE ( 'NONE', #43657, #35776, #646, .T. ) ;
#47184=EDGE_CURVE ( 'NONE', #35420, #33399, #30539, .T. ) ;
#47186=ORIENTED_EDGE ( 'NONE', *, *, #23072, .T. ) ;
#47203=ORIENTED_EDGE ( 'NONE', *, *, #30460, .T. ) ;
#47204=CARTESIAN_POINT ( 'NONE',  ( -19.04784696903935881, -9.816619457272704352, 52.02966884056656482 ) ) ;
#47214=ORIENTED_EDGE ( 'NONE', *, *, #16347, .T. ) ;
#47215=CARTESIAN_POINT ( 'NONE',  ( -17.42409385541299471, -14.80920654474435771, 49.52966884056655772 ) ) ;
#47216=AXIS2_PLACEMENT_3D ( 'NONE', #32994, #15257, #48513 ) ;
#47218=DIRECTION ( 'NONE',  ( -3.071710424422018668E-17, 6.404604876783312462E-16, 1.000000000000000000 ) ) ;
#47222=ORIENTED_EDGE ( 'NONE', *, *, #21938, .F. ) ;
#47223=ORIENTED_EDGE ( 'NONE', *, *, #6785, .T. ) ;
#47225=DIRECTION ( 'NONE',  ( -3.071710424422018668E-17, 6.404604876783312462E-16, 1.000000000000000000 ) ) ;
#47250=CIRCLE ( 'NONE', #33840, 4.686500000000000554 ) ;
#47266=ORIENTED_EDGE ( 'NONE', *, *, #38227, .F. ) ;
#47275=ORIENTED_EDGE ( 'NONE', *, *, #19760, .T. ) ;
#47300=AXIS2_PLACEMENT_3D ( 'NONE', #30677, #45700, #37055 ) ;
#47304=DIRECTION ( 'NONE',  ( -3.071710424422018668E-17, 6.404604876783312462E-16, 1.000000000000000000 ) ) ;
#47307=DIRECTION ( 'NONE',  ( 0.9687793358424821033, -0.2479245821708677133, 0.000000000000000000 ) ) ;
#47310=ORIENTED_EDGE ( 'NONE', *, *, #39545, .T. ) ;
#47321=AXIS2_PLACEMENT_3D ( 'NONE', #7639, #14718, #37387 ) ;
#47358=FACE_OUTER_BOUND ( 'NONE', #25515, .T. ) ;
#47367=DIRECTION ( 'NONE',  ( -3.071710424422018668E-17, 6.404604876783312462E-16, 1.000000000000000000 ) ) ;
#47369=CIRCLE ( 'NONE', #33948, 5.249999999999998224 ) ;
#47384=CARTESIAN_POINT ( 'NONE',  ( -17.42260713176972686, -20.05920633423509258, 50.77966884056656482 ) ) ;
#47392=VERTEX_POINT ( 'NONE', #23980 ) ;
#47408=DIRECTION ( 'NONE',  ( 0.9687793358424802159, -0.2479245821708749020, 0.000000000000000000 ) ) ;
#47435=DIRECTION ( 'NONE',  ( 0.9687793358424821033, -0.2479245821708680464, 0.000000000000000000 ) ) ;
#47436=VERTEX_POINT ( 'NONE', #38982 ) ;
#47442=VECTOR ( 'NONE', #15802, 1000.000000000000000 ) ;
#47443=ORIENTED_EDGE ( 'NONE', *, *, #19223, .T. ) ;
#47447=ORIENTED_EDGE ( 'NONE', *, *, #37163, .F. ) ;
#47461=CARTESIAN_POINT ( 'NONE',  ( -19.71801720247071543, -10.72249662993226060, 49.52966884056655772 ) ) ;
#47468=CARTESIAN_POINT ( 'NONE',  ( -15.65212752116712558, -9.867280269464721698, 52.02966884056656482 ) ) ;
#47473=DIRECTION ( 'NONE',  ( -3.071710424422018668E-17, 6.404604876783312462E-16, 1.000000000000000000 ) ) ;
#47484=CYLINDRICAL_SURFACE ( 'NONE', #32070, 1.999999999999999112 ) ;
#47495=DIRECTION ( 'NONE',  ( -3.071710424422018668E-17, 6.404604876783312462E-16, 1.000000000000000000 ) ) ;
#47501=EDGE_CURVE ( 'NONE', #30521, #38535, #14059, .T. ) ;
#47502=DIRECTION ( 'NONE',  ( -3.071710424422018668E-17, 6.404604876783312462E-16, 1.000000000000000000 ) ) ;
#47508=CARTESIAN_POINT ( 'NONE',  ( -12.87649578556737318, -13.67667219862661021, 49.52966884056655772 ) ) ;
#47516=CARTESIAN_POINT ( 'NONE',  ( -13.33738394060092070, -12.51528319768659436, 52.02966884056656482 ) ) ;
#47525=ORIENTED_EDGE ( 'NONE', *, *, #12416, .F. ) ;
#47527=CARTESIAN_POINT ( 'NONE',  ( -20.02395964528090033, -18.70843468947692045, 49.52966884056656482 ) ) ;
#47547=AXIS2_PLACEMENT_3D ( 'NONE', #40072, #3117, #48178 ) ;
#47558=VERTEX_POINT ( 'NONE', #4463 ) ;
#47580=CIRCLE ( 'NONE', #32636, 2.000000000000001332 ) ;
#47587=CARTESIAN_POINT ( 'NONE',  ( -22.10255287824656989, -12.42708119714673742, 50.77966884056655772 ) ) ;
#47599=CARTESIAN_POINT ( 'NONE',  ( -13.52486571068042487, -17.40907233461224735, 49.52966884056655772 ) ) ;
#47605=CARTESIAN_POINT ( 'NONE',  ( -18.69178539469224987, -19.32099559247695097, 49.52966884056656482 ) ) ;
#47633=CARTESIAN_POINT ( 'NONE',  ( -13.17588093101833557, -17.89387621085224822, 50.77966884056655772 ) ) ;
#47662=ORIENTED_EDGE ( 'NONE', *, *, #36235, .T. ) ;
#47669=VECTOR ( 'NONE', #38092, 1000.000000000000000 ) ;
#47680=DIRECTION ( 'NONE',  ( 0.5351595679979626041, 0.8447509909909748371, 0.000000000000000000 ) ) ;
#47682=ORIENTED_EDGE ( 'NONE', *, *, #12386, .T. ) ;
#47683=DIRECTION ( 'NONE',  ( 0.9687793358424819923, -0.2479245821708680464, 0.000000000000000000 ) ) ;
#47691=CARTESIAN_POINT ( 'NONE',  ( -12.73887154267113253, -15.16169402761810048, 49.52966884056655772 ) ) ;
#47699=ORIENTED_EDGE ( 'NONE', *, *, #3831, .T. ) ;
#47701=CARTESIAN_POINT ( 'NONE',  ( -16.47989802999360265, -19.41181990985090877, 49.52966884056656482 ) ) ;
#47704=DIRECTION ( 'NONE',  ( 0.9687793358424821033, -0.2479245821708677133, 0.000000000000000000 ) ) ;
#47711=ORIENTED_EDGE ( 'NONE', *, *, #32710, .T. ) ;
#47715=CARTESIAN_POINT ( 'NONE',  ( -17.42409385541299471, -14.80920654474435594, 52.02966884056656482 ) ) ;
#47716=CIRCLE ( 'NONE', #26486, 1.999999999999999556 ) ;
#47723=LINE ( 'NONE', #39851, #37885 ) ;
#47730=CARTESIAN_POINT ( 'NONE',  ( -12.73044152958719977, -14.59664269629646682, 49.52966884056655772 ) ) ;
#47737=DIRECTION ( 'NONE',  ( -0.9687793358424819923, 0.2479245821708680464, 0.000000000000000000 ) ) ;
#47746=DIRECTION ( 'NONE',  ( -0.9687793358424819923, 0.2479245821708680464, 0.000000000000000000 ) ) ;
#47769=AXIS2_PLACEMENT_3D ( 'NONE', #42525, #15911, #35109 ) ;
#47770=ORIENTED_EDGE ( 'NONE', *, *, #36623, .T. ) ;
#47771=CIRCLE ( 'NONE', #9231, 2.000000000000000444 ) ;
#47780=AXIS2_PLACEMENT_3D ( 'NONE', #13994, #18429, #7387 ) ;
#47783=CARTESIAN_POINT ( 'NONE',  ( -22.02798021202036693, -12.28596846334092163, 49.52966884056655772 ) ) ;
#47788=EDGE_CURVE ( 'NONE', #21704, #24396, #47042, .T. ) ;
#47800=CARTESIAN_POINT ( 'NONE',  ( -13.33852097861372421, -12.48893720396535301, 52.02966884056656482 ) ) ;
#47801=CARTESIAN_POINT ( 'NONE',  ( -14.23827708255551627, -10.77544123782542229, 52.02966884056656482 ) ) ;
#47802=DIRECTION ( 'NONE',  ( -3.071710424422018668E-17, 6.404604876783312462E-16, 1.000000000000000000 ) ) ;
#47808=CYLINDRICAL_SURFACE ( 'NONE', #20412, 2.000000000000001332 ) ;
#47827=CARTESIAN_POINT ( 'NONE',  ( -14.35043204381087101, -18.34698626059704551, 52.02966884056656482 ) ) ;
#47830=DIRECTION ( 'NONE',  ( -3.071710424422018668E-17, 6.404604876783312462E-16, 1.000000000000000000 ) ) ;
#47836=DIRECTION ( 'NONE',  ( -3.071710424422018668E-17, 6.404604876783312462E-16, 1.000000000000000000 ) ) ;
#47837=CARTESIAN_POINT ( 'NONE',  ( -19.90648311238531676, -10.83415612659008964, 52.02966884056656482 ) ) ;
#47848=AXIS2_PLACEMENT_3D ( 'NONE', #40779, #45465, #22314 ) ;
#47851=ORIENTED_EDGE ( 'NONE', *, *, #6876, .F. ) ;
#47853=LINE ( 'NONE', #47384, #10315 ) ;
#47855=CARTESIAN_POINT ( 'NONE',  ( -14.83720200468841810, -10.88702015217558206, 49.52966884056655772 ) ) ;
#47858=LINE ( 'NONE', #48580, #15699 ) ;
#47864=DIRECTION ( 'NONE',  ( -3.071710424422018668E-17, 6.404604876783312462E-16, 1.000000000000000000 ) ) ;
#47866=DIRECTION ( 'NONE',  ( 0.9687793358424821033, -0.2479245821708679909, 0.000000000000000000 ) ) ;
#47872=DIRECTION ( 'NONE',  ( 0.9687793358424819923, -0.2479245821708680464, 0.000000000000000000 ) ) ;
#47874=CARTESIAN_POINT ( 'NONE',  ( -12.48216758013336936, -16.58117287899024817, 49.52966884056655772 ) ) ;
#47878=DIRECTION ( 'NONE',  ( 0.9687793358424821033, -0.2479245821708677133, 0.000000000000000000 ) ) ;
#47886=AXIS2_PLACEMENT_3D ( 'NONE', #42889, #16038, #38454 ) ;
#47908=EDGE_CURVE ( 'NONE', #30479, #41134, #15226, .T. ) ;
#47909=CIRCLE ( 'NONE', #36883, 2.000000000000000444 ) ;
#47914=CIRCLE ( 'NONE', #14075, 4.686499999999998778 ) ;
#47921=CIRCLE ( 'NONE', #21989, 2.000000000000000888 ) ;
#47938=DIRECTION ( 'NONE',  ( -3.071710424422018668E-17, 6.404604876783312462E-16, 1.000000000000000000 ) ) ;
#47941=EDGE_CURVE ( 'NONE', #47436, #28192, #26829, .T. ) ;
#47964=EDGE_LOOP ( 'NONE', ( #11478, #17880, #15164, #17487 ) ) ;
#47970=CARTESIAN_POINT ( 'NONE',  ( -21.98892968875003717, -15.92178434430670642, 49.52966884056655772 ) ) ;
#47975=CARTESIAN_POINT ( 'NONE',  ( -17.42409385541299471, -14.80920654474435771, 49.52966884056655772 ) ) ;
#47977=AXIS2_PLACEMENT_3D ( 'NONE', #20974, #43143, #13795 ) ;
#47981=VERTEX_POINT ( 'NONE', #35409 ) ;
#47982=DIRECTION ( 'NONE',  ( -0.9687793358424819923, 0.2479245821708680464, 0.000000000000000000 ) ) ;
#47985=DIRECTION ( 'NONE',  ( 3.071710424422018668E-17, -6.404604876783312462E-16, -1.000000000000000000 ) ) ;
#48010=DIRECTION ( 'NONE',  ( -3.071710424422018668E-17, 6.404604876783312462E-16, 1.000000000000000000 ) ) ;
#48012=ORIENTED_EDGE ( 'NONE', *, *, #33783, .F. ) ;
#48015=VECTOR ( 'NONE', #33358, 1000.000000000000000 ) ;
#48025=AXIS2_PLACEMENT_3D ( 'NONE', #24054, #20105, #5338 ) ;
#48029=ORIENTED_EDGE ( 'NONE', *, *, #11497, .F. ) ;
#48051=CARTESIAN_POINT ( 'NONE',  ( -19.86520892150080897, -18.82374422416847182, 52.02966884056656482 ) ) ;
#48062=CARTESIAN_POINT ( 'NONE',  ( -17.42409385541299471, -14.80920654474435594, 52.02966884056656482 ) ) ;
#48069=CARTESIAN_POINT ( 'NONE',  ( -13.02884944951828494, -13.18282747993466764, 52.02966884056656482 ) ) ;
#48074=AXIS2_PLACEMENT_3D ( 'NONE', #25693, #15086, #22753 ) ;
#48083=ORIENTED_EDGE ( 'NONE', *, *, #36767, .F. ) ;
#48086=VECTOR ( 'NONE', #141, 1000.000000000000000 ) ;
#48091=DIRECTION ( 'NONE',  ( 0.9687793358424821033, -0.2479245821708680464, 0.000000000000000000 ) ) ;
#48095=CIRCLE ( 'NONE', #8022, 5.249999999999998224 ) ;
#48098=CARTESIAN_POINT ( 'NONE',  ( -15.77151528785019430, -19.20744933288474954, 49.52966884056656482 ) ) ;
#48117=AXIS2_PLACEMENT_3D ( 'NONE', #24658, #17716, #1757 ) ;
#48131=EDGE_CURVE ( 'NONE', #3170, #11147, #14027, .T. ) ;
#48156=ORIENTED_EDGE ( 'NONE', *, *, #34370, .T. ) ;
#48167=EDGE_LOOP ( 'NONE', ( #44091, #15950, #29507, #11795 ) ) ;
#48172=ORIENTED_EDGE ( 'NONE', *, *, #3137, .T. ) ;
#48176=CARTESIAN_POINT ( 'NONE',  ( -20.89331258220900978, -11.64059849529350643, 52.02966884056656482 ) ) ;
#48177=ORIENTED_EDGE ( 'NONE', *, *, #46463, .F. ) ;
#48178=DIRECTION ( 'NONE',  ( 0.9687793358424821033, -0.2479245821708677133, 0.000000000000000000 ) ) ;
#48183=ADVANCED_FACE ( 'NONE', ( #21610 ), #17884, .T. ) ;
#48191=ORIENTED_EDGE ( 'NONE', *, *, #15323, .T. ) ;
#48194=DIRECTION ( 'NONE',  ( -3.071710424422018668E-17, 6.404604876783312462E-16, 1.000000000000000000 ) ) ;
#48217=DIRECTION ( 'NONE',  ( -3.071710424422018668E-17, 6.404604876783312462E-16, 1.000000000000000000 ) ) ;
#48218=EDGE_LOOP ( 'NONE', ( #43817, #33227, #19471, #5195 ) ) ;
#48226=CARTESIAN_POINT ( 'NONE',  ( -21.44055400477819973, -12.39439182751215718, 52.02966884056656482 ) ) ;
#48228=CARTESIAN_POINT ( 'NONE',  ( -22.10679845867080928, -14.99777973644470919, 49.52966884056655772 ) ) ;
#48229=DIRECTION ( 'NONE',  ( -3.071710424422018668E-17, 6.404604876783312462E-16, 1.000000000000000000 ) ) ;
#48231=AXIS2_PLACEMENT_3D ( 'NONE', #43885, #39927, #10138 ) ;
#48239=DIRECTION ( 'NONE',  ( -3.071710424422018668E-17, 6.404604876783312462E-16, 1.000000000000000000 ) ) ;
#48242=ORIENTED_EDGE ( 'NONE', *, *, #9822, .F. ) ;
#48246=CARTESIAN_POINT ( 'NONE',  ( -18.40115675053315059, -19.96748611248585448, 50.77966884056656482 ) ) ;
#48250=ORIENTED_EDGE ( 'NONE', *, *, #34366, .T. ) ;
#48259=CIRCLE ( 'NONE', #14523, 4.686499999999997890 ) ;
#48263=EDGE_CURVE ( 'NONE', #42051, #35450, #43135, .T. ) ;
#48272=ORIENTED_EDGE ( 'NONE', *, *, #25302, .F. ) ;
#48298=CARTESIAN_POINT ( 'NONE',  ( -13.83484324388145303, -17.82260368047347399, 49.52966884056656482 ) ) ;
#48301=DIRECTION ( 'NONE',  ( -3.071710424422018668E-17, 6.404604876783312462E-16, 1.000000000000000000 ) ) ;
#48305=CIRCLE ( 'NONE', #32603, 5.249999999999998224 ) ;
#48320=DIRECTION ( 'NONE',  ( -0.5097212845717549179, 0.8603395911234820170, 0.000000000000000000 ) ) ;
#48331=ORIENTED_EDGE ( 'NONE', *, *, #18386, .F. ) ;
#48345=CARTESIAN_POINT ( 'NONE',  ( -17.42409385541299471, -14.80920654474434883, 62.02966884056656482 ) ) ;
#48356=FACE_OUTER_BOUND ( 'NONE', #48167, .T. ) ;
#48361=ORIENTED_EDGE ( 'NONE', *, *, #29316, .F. ) ;
#48365=DIRECTION ( 'NONE',  ( 3.071710424422018668E-17, -6.404604876783312462E-16, -1.000000000000000000 ) ) ;
#48366=LINE ( 'NONE', #15350, #8042 ) ;
#48371=CIRCLE ( 'NONE', #41310, 4.686499999999998778 ) ;
#48373=AXIS2_PLACEMENT_3D ( 'NONE', #2273, #21954, #39702 ) ;
#48382=VERTEX_POINT ( 'NONE', #6236 ) ;
#48392=EDGE_LOOP ( 'NONE', ( #370, #48272, #26923, #47275 ) ) ;
#48440=AXIS2_PLACEMENT_3D ( 'NONE', #29499, #41312, #18646 ) ;
#48446=ORIENTED_EDGE ( 'NONE', *, *, #4845, .F. ) ;
#48451=FACE_OUTER_BOUND ( 'NONE', #756, .T. ) ;
#48460=VERTEX_POINT ( 'NONE', #33769 ) ;
#48461=CARTESIAN_POINT ( 'NONE',  ( -22.02798021202036693, -12.28596846334092163, 52.02966884056656482 ) ) ;
#48467=CARTESIAN_POINT ( 'NONE',  ( -21.99649211598757859, -13.72812852161587038, 52.02966884056656482 ) ) ;
#48468=FACE_OUTER_BOUND ( 'NONE', #41180, .T. ) ;
#48473=CIRCLE ( 'NONE', #42971, 4.686499999999998778 ) ;
#48481=CARTESIAN_POINT ( 'NONE',  ( -17.42409385541299471, -14.80920654474435771, 49.52966884056655772 ) ) ;
#48483=CARTESIAN_POINT ( 'NONE',  ( -13.40955617598886995, -17.25032161083215954, 49.52966884056655772 ) ) ;
#48489=CARTESIAN_POINT ( 'NONE',  ( -21.57657733182563931, -11.59682721189465049, 49.52966884056655772 ) ) ;
#48490=CARTESIAN_POINT ( 'NONE',  ( -15.03931914688375571, -19.48631565075837457, 49.52966884056656482 ) ) ;
#48505=VERTEX_POINT ( 'NONE', #26396 ) ;
#48513=DIRECTION ( 'NONE',  ( -0.9687793358424821033, 0.2479245821708679909, 0.000000000000000000 ) ) ;
#48522=EDGE_CURVE ( 'NONE', #42196, #6295, #19553, .T. ) ;
#48525=ORIENTED_EDGE ( 'NONE', *, *, #15006, .F. ) ;
#48530=FACE_OUTER_BOUND ( 'NONE', #32033, .T. ) ;
#48533=ORIENTED_EDGE ( 'NONE', *, *, #26174, .F. ) ;
#48539=DIRECTION ( 'NONE',  ( 3.071710424422018668E-17, -6.404604876783312462E-16, -1.000000000000000000 ) ) ;
#48543=ADVANCED_FACE ( 'NONE', ( #4725 ), #19981, .T. ) ;
#48551=EDGE_CURVE ( 'NONE', #13129, #12455, #26619, .T. ) ;
#48570=LINE ( 'NONE', #11630, #18165 ) ;
#48572=ADVANCED_FACE ( 'NONE', ( #34016 ), #11870, .T. ) ;
#48576=CIRCLE ( 'NONE', #27353, 1.999999999999998668 ) ;
#48580=CARTESIAN_POINT ( 'NONE',  ( -22.02798021202036693, -12.28596846334092163, 50.77966884056655772 ) ) ;
#48581=AXIS2_PLACEMENT_3D ( 'NONE', #6624, #32709, #43822 ) ;
#48584=CARTESIAN_POINT ( 'NONE',  ( -17.42409385541299471, -14.80920654474435594, 52.02966884056656482 ) ) ;
#48590=DIRECTION ( 'NONE',  ( -3.071710424422018668E-17, 6.404604876783312462E-16, 1.000000000000000000 ) ) ;
#48600=ORIENTED_EDGE ( 'NONE', *, *, #44963, .F. ) ;
#48606=EDGE_CURVE ( 'NONE', #41721, #19733, #22716, .T. ) ;
#48614=VECTOR ( 'NONE', #22423, 1000.000000000000000 ) ;
#48617=CARTESIAN_POINT ( 'NONE',  ( -22.36602013069261119, -13.03724021049843174, 50.77966884056655772 ) ) ;
#48621=ORIENTED_EDGE ( 'NONE', *, *, #28138, .F. ) ;
#48625=CARTESIAN_POINT ( 'NONE',  ( -22.17153284776674482, -17.05070671513899683, 52.02966884056656482 ) ) ;
#48626=VECTOR ( 'NONE', #1108, 1000.000000000000000 ) ;
#48635=VERTEX_POINT ( 'NONE', #2227 ) ;
#48641=CARTESIAN_POINT ( 'NONE',  ( -17.42409385541299471, -14.80920654474438614, 2.029618040566568027 ) ) ;
#48646=CARTESIAN_POINT ( 'NONE',  ( -21.43863153483710349, -12.36809147865652925, 49.52966884056655772 ) ) ;
#48649=CARTESIAN_POINT ( 'NONE',  ( -17.42409385541299471, -14.80920654474435594, 52.02966884056656482 ) ) ;
#48659=DIRECTION ( 'NONE',  ( 3.071710424422018668E-17, -6.404604876783312462E-16, -1.000000000000000000 ) ) ;
#48663=DIRECTION ( 'NONE',  ( -0.6380325334150322991, 0.7700094066334487453, 0.000000000000000000 ) ) ;
#48683=EDGE_CURVE ( 'NONE', #13759, #8796, #33688, .T. ) ;
#48688=ADVANCED_FACE ( 'NONE', ( #2475 ), #32511, .T. ) ;
#48693=ORIENTED_EDGE ( 'NONE', *, *, #47178, .F. ) ;
#48694=DIRECTION ( 'NONE',  ( -3.071710424422018668E-17, 6.404604876783312462E-16, 1.000000000000000000 ) ) ;
#48697=LINE ( 'NONE', #14679, #4027 ) ;
#48705=DIRECTION ( 'NONE',  ( -3.071710424422018668E-17, 6.404604876783312462E-16, 1.000000000000000000 ) ) ;
#48716=AXIS2_PLACEMENT_3D ( 'NONE', #24738, #27929, #39259 ) ;
#48722=CARTESIAN_POINT ( 'NONE',  ( -14.46752719259218800, -19.14754880513559954, 49.52966884056656482 ) ) ;
#48723=ORIENTED_EDGE ( 'NONE', *, *, #19122, .T. ) ;
#48728=CARTESIAN_POINT ( 'NONE',  ( -17.42409385541299471, -14.80920654474435594, 52.02966884056656482 ) ) ;
ENDSEC;
END-ISO-10303-21;
